ISO-10303-21;
HEADER;
FILE_DESCRIPTION (('STEP AP214'),
    '1' );
FILE_NAME ('2. Holder.step',
    '2026-10-09T14:04:53',
    ( '' ),
    ( '' ),
    'SwSTEP 2.0',
    'SolidWorks 2021',
    '' );
FILE_SCHEMA (( 'AUTOMOTIVE_DESIGN' ));
ENDSEC;

DATA;
#7=CARTESIAN_POINT ( 'NONE',  ( -27.61887443722037716, 41.31835651977961987, -69.45683157427789922 ) ) ;
#14=CARTESIAN_POINT ( 'NONE',  ( -7.996668422911731078, -5.000000000000002665, -78.85453279917058467 ) ) ;
#15=CARTESIAN_POINT ( 'NONE',  ( -6.817720317547426134, 41.26212449704699026, -58.42655649050038136 ) ) ;
#19=FILL_AREA_STYLE ('',( #15706 ) ) ;
#20=VERTEX_POINT ( 'NONE', #83759 ) ;
#36=VERTEX_POINT ( 'NONE', #74603 ) ;
#75=CARTESIAN_POINT ( 'NONE',  ( -6.784953749642196108, 41.67963440881483450, -59.00226708758491156 ) ) ;
#76=CARTESIAN_POINT ( 'NONE',  ( 6.804948497510390659, 41.03925918793141392, -70.91872537021917822 ) ) ;
#96=CARTESIAN_POINT ( 'NONE',  ( 7.084743714275938409, 40.92373723548720221, -70.77066346801599650 ) ) ;
#103=CARTESIAN_POINT ( 'NONE',  ( -55.63518754872630012, 38.95383793071890466, 32.06611684419585373 ) ) ;
#113=AXIS2_PLACEMENT_3D ( 'NONE', #85690, #35566, #67375 ) ;
#117=CARTESIAN_POINT ( 'NONE',  ( 7.341136360785455395, 41.28570779223741738, -59.23704358728311092 ) ) ;
#136=PRESENTATION_STYLE_ASSIGNMENT (( #15825 ) ) ;
#139=CARTESIAN_POINT ( 'NONE',  ( -7.500000000000004441, -5.250000000000005329, -71.71180648257555390 ) ) ;
#149=CARTESIAN_POINT ( 'NONE',  ( -63.25915952246064222, 50.00000000000000000, 0.7870165385200997843 ) ) ;
#154=CARTESIAN_POINT ( 'NONE',  ( 14.90155535905845952, 42.58002643001236720, -90.01374837836192455 ) ) ;
#155=CARTESIAN_POINT ( 'NONE',  ( -5.308064226573042887, 41.67430808342687243, -70.56675994572434263 ) ) ;
#158=CARTESIAN_POINT ( 'NONE',  ( 50.94745919686198476, 50.00000000000000000, -37.05882352941176094 ) ) ;
#163=CARTESIAN_POINT ( 'NONE',  ( 6.716227136310304324, 41.28548593599064986, -58.40644136812132103 ) ) ;
#166=EDGE_CURVE ( 'NONE', #36397, #86892, #67028, .T. ) ;
#187=CARTESIAN_POINT ( 'NONE',  ( -7.855360403618689702, 48.00000000000000711, -97.83275449052109707 ) ) ;
#189=B_SPLINE_CURVE_WITH_KNOTS ( 'NONE', 3,
 ( #47704, #5149, #104909, #71456, #31568, #72522, #105428, #62864, #30501, #97856 ),
 .UNSPECIFIED., .F., .F.,
 ( 4, 2, 2, 2, 4 ),
 ( 0.000000000000000000, 0.1250000000000000000, 0.2500000000000000000, 0.5000000000000000000, 1.000000000000000000 ),
 .UNSPECIFIED. ) ;
#191=CARTESIAN_POINT ( 'NONE',  ( -7.245482512374693762, 40.92674694571729788, -70.53853366045179030 ) ) ;
#212=ORIENTED_EDGE ( 'NONE', *, *, #24427, .T. ) ;
#223=CARTESIAN_POINT ( 'NONE',  ( 12.50000000000000178, 35.75035848856805387, -55.58311287890759189 ) ) ;
#245=CARTESIAN_POINT ( 'NONE',  ( -4.175893272574851878, -3.000000000000000000, 7.137815226409915503 ) ) ;
#262=FILL_AREA_STYLE_COLOUR ( '', #16845 ) ;
#269=CARTESIAN_POINT ( 'NONE',  ( 19.49736279435683173, 49.99988902982553896, 59.96655211255940543 ) ) ;
#277=CARTESIAN_POINT ( 'NONE',  ( -6.615712822709019392, -4.357054607612187880, -16.81429077417682549 ) ) ;
#288=VERTEX_POINT ( 'NONE', #8688 ) ;
#304=CARTESIAN_POINT ( 'NONE',  ( -5.957442974701830707, 48.00000000000000000, 65.00000000000000000 ) ) ;
#318=CARTESIAN_POINT ( 'NONE',  ( -14.62309622336928783, 18.64284798593354964, -35.53993507408184627 ) ) ;
#346=SURFACE_SIDE_STYLE ('',( #64603 ) ) ;
#391=SURFACE_STYLE_USAGE ( .BOTH. , #82418 ) ;
#428=CARTESIAN_POINT ( 'NONE',  ( -7.125691916582565177, 41.67430808341742932, -69.26730091582949456 ) ) ;
#434=FACE_OUTER_BOUND ( 'NONE', #87709, .T. ) ;
#450=CARTESIAN_POINT ( 'NONE',  ( 72.41885610122542971, 42.00000000000000000, -55.65414010180089832 ) ) ;
#472=CARTESIAN_POINT ( 'NONE',  ( 4.905843853654985764, -4.999999999999999112, -16.52456679617690938 ) ) ;
#477=CARTESIAN_POINT ( 'NONE',  ( 18.14701115887386607, 45.00000000000001421, 62.47877254244827583 ) ) ;
#489=CARTESIAN_POINT ( 'NONE',  ( -2.617478844990611897, -3.000000000000002665, -75.26027323389583046 ) ) ;
#499=CARTESIAN_POINT ( 'NONE',  ( 4.905367688403428517, -5.000000000000055067, -16.52522736516917590 ) ) ;
#502=CARTESIAN_POINT ( 'NONE',  ( -38.79245513715870430, 42.07398859163519234, -57.16919138223752839 ) ) ;
#518=CARTESIAN_POINT ( 'NONE',  ( -17.50000000000280664, 49.91179365273242041, 61.97298340137167116 ) ) ;
#536=CARTESIAN_POINT ( 'NONE',  ( -19.50262057251149983, 41.86950174827330073, -80.38433612792447036 ) ) ;
#542=CARTESIAN_POINT ( 'NONE',  ( -3.140974613990845210, -5.000000000000002665, -73.31232788067644890 ) ) ;
#562=CARTESIAN_POINT ( 'NONE',  ( 30.80675973667872114, 38.95360674089970132, 55.79500139137103076 ) ) ;
#582=CARTESIAN_POINT ( 'NONE',  ( -10.82254083843020531, -4.995738461561603394, -12.56441722558348140 ) ) ;
#591=ORIENTED_EDGE ( 'NONE', *, *, #38683, .F. ) ;
#594=EDGE_CURVE ( 'NONE', #99282, #59690, #88439, .T. ) ;
#598=CARTESIAN_POINT ( 'NONE',  ( -1.727368016638141196E-09, 38.95322581935191408, 63.66965480466880223 ) ) ;
#640=CARTESIAN_POINT ( 'NONE',  ( 7.436486958462253050, 40.68079685609215801, -59.06589984255106174 ) ) ;
#648=EDGE_CURVE ( 'NONE', #57839, #9002, #34683, .T. ) ;
#659=FACE_OUTER_BOUND ( 'NONE', #11091, .T. ) ;
#712=VERTEX_POINT ( 'NONE', #58176 ) ;
#713=CARTESIAN_POINT ( 'NONE',  ( -6.930184079356135562, 41.27136532024966442, -70.62329956115780760 ) ) ;
#723=CARTESIAN_POINT ( 'NONE',  ( -2.583889972062225482, -5.000000000000000000, -9.742892617411701650 ) ) ;
#728=CARTESIAN_POINT ( 'NONE',  ( -5.079411765174640436, 41.99999999999998579, -70.14437560653188086 ) ) ;
#759=CARTESIAN_POINT ( 'NONE',  ( 62.01418705507710172, 38.95383793061004951, -16.66584972139569487 ) ) ;
#805=CARTESIAN_POINT ( 'NONE',  ( -5.902962327514317487, 41.87327319969161010, -59.02279321040224147 ) ) ;
#812=CARTESIAN_POINT ( 'NONE',  ( -6.797507374398395363, -5.000000000000177636, -15.30989363317748619 ) ) ;
#817=SURFACE_STYLE_USAGE ( .BOTH. , #99003 ) ;
#834=CARTESIAN_POINT ( 'NONE',  ( -62.59524157943269529, 48.00000000000000000, 18.50207713769755102 ) ) ;
#844=CARTESIAN_POINT ( 'NONE',  ( -34.12287332558172892, 18.64284798593243409, -17.67912453245623539 ) ) ;
#855=B_SPLINE_CURVE_WITH_KNOTS ( 'NONE', 3,
 ( #24973, #88624, #72434, #57824, #98304, #72948, #40595, #56218, #22856, #16316 ),
 .UNSPECIFIED., .F., .F.,
 ( 4, 2, 2, 2, 4 ),
 ( 0.000000000000000000, 0.2500000000000000000, 0.5000000000000000000, 0.7500000000000000000, 1.000000000000000000 ),
 .UNSPECIFIED. ) ;
#858=CARTESIAN_POINT ( 'NONE',  ( 18.35767182829701838, 41.91122692137232519, -81.93709609102950253 ) ) ;
#861=EDGE_CURVE ( 'NONE', #65010, #9732, #84119, .T. ) ;
#869=CARTESIAN_POINT ( 'NONE',  ( -6.457005523775564804, 41.52802923939503899, -70.63630686657118929 ) ) ;
#918=CARTESIAN_POINT ( 'NONE',  ( -12.50000000000000711, -3.000000000000000000, -80.60844091781802945 ) ) ;
#957=CARTESIAN_POINT ( 'NONE',  ( 9.500000000000005329, -5.000000000000000000, -52.94236561372726868 ) ) ;
#966=CARTESIAN_POINT ( 'NONE',  ( -6.674329190760282415, 41.70627400296338294, -58.97405543038894393 ) ) ;
#992=CARTESIAN_POINT ( 'NONE',  ( 6.563169452749920474, 41.73030697269559397, -58.95245962634098902 ) ) ;
#1008=CARTESIAN_POINT ( 'NONE',  ( 17.80908660213453132, 45.00000000000000711, 62.71861104723561198 ) ) ;
#1031=CARTESIAN_POINT ( 'NONE',  ( 28.60676286294167880, 48.00000000000000000, 58.59397763554171235 ) ) ;
#1042=CARTESIAN_POINT ( 'NONE',  ( 12.57956330987153848, -3.000000000000002665, -93.28077019087170640 ) ) ;
#1060=CARTESIAN_POINT ( 'NONE',  ( -17.50000000000073186, 50.01371676753186080, 60.25403804533437579 ) ) ;
#1066=EDGE_LOOP ( 'NONE', ( #69695, #66571, #74398, #89106 ) ) ;
#1071=CARTESIAN_POINT ( 'NONE',  ( -6.232496158895186156, 41.83455024993975968, -59.02481301687200244 ) ) ;
#1072=CARTESIAN_POINT ( 'NONE',  ( -24.40731547348265096, 41.58993316039871502, -73.75804528573827668 ) ) ;
#1156=CARTESIAN_POINT ( 'NONE',  ( -3.430943074671103599, -4.332661967060490227, -17.58450835315055372 ) ) ;
#1201=CARTESIAN_POINT ( 'NONE',  ( -4.852941176470593199, 41.41666666666666430, -70.80672828634229177 ) ) ;
#1222=CARTESIAN_POINT ( 'NONE',  ( -6.057904167604424295, 41.61856606222242760, -70.65344123333893833 ) ) ;
#1228=CARTESIAN_POINT ( 'NONE',  ( -51.76085035125569789, 42.00000000008225953, 29.83308852628617203 ) ) ;
#1235=ORIENTED_EDGE ( 'NONE', *, *, #9863, .T. ) ;
#1240=CARTESIAN_POINT ( 'NONE',  ( 15.02532841153920806, 41.95741965229949955, -84.73629853939195300 ) ) ;
#1255=CARTESIAN_POINT ( 'NONE',  ( -7.428752412959402918, 40.00000000001743672, -70.23138725920588854 ) ) ;
#1267=DIRECTION ( 'NONE',  ( 0.000000000000000000, 1.000000000000000000, 0.000000000000000000 ) ) ;
#1268=CARTESIAN_POINT ( 'NONE',  ( -9.999872502480485537, -5.000000000000000000, -1.308371270542921794 ) ) ;
#1293=CARTESIAN_POINT ( 'NONE',  ( 12.50000000000000711, 34.81126633643881974, -54.09195137927829933 ) ) ;
#1299=CARTESIAN_POINT ( 'NONE',  ( -7.500000000000007105, -3.000000000000000000, -68.91429205785459544 ) ) ;
#1303=CARTESIAN_POINT ( 'NONE',  ( 5.398220238549152228, 41.68867471179443385, -58.74408635829322378 ) ) ;
#1329=( BOUNDED_SURFACE ( )  B_SPLINE_SURFACE ( 2, 3, ( 
 ( #7055, #79884, #38919, #90642, #9705, #34034, #66907, #1608, #65831, #16751, #50175, #74970, #42615, #17832, #83080, #16212, #81998, #16353, #32961, #82550, #81460, #50683, #8651, #49641, #75514, #99792, #25963, #34570, #98710, #41557 ),
 ( #67443, #83600, #9169, #49098, #8117, #24864, #57719, #74440, #7575, #100319, #518, #41030, #98194, #33483, #26479, #66359, #42082, #17304, #73911, #1060, #58822, #89587, #99241, #15680, #32434, #57191, #90106, #24348, #91713, #48570 ),
 ( #25410, #58270, #91195, #40496, #73371, #106271, #65306, #43681, #79631, #44766, #35093, #10765, #27010, #38667, #69565, #11835, #102456, #77656, #84680, #76570, #3770, #101916, #44225, #77115, #28604, #18372, #92218, #51223, #52297, #60945 ) ),
 .UNSPECIFIED., .F., .F., .F. ) 
 B_SPLINE_SURFACE_WITH_KNOTS ( ( 3, 3 ),
 ( 4, 2, 2, 2, 2, 2, 2, 2, 2, 2, 2, 2, 2, 2, 4 ),
 ( 0.000000000000000000, 1.000000000000000000 ),
 ( 0.000000000000000000, 0.0008794597212716800472, 0.001758919442543360094, 0.002638379163815040250, 0.003078109024450880436, 0.003517838885086720189, 0.003957568745722559941, 0.004397298606358400128, 0.005276758327630080500, 0.006156218048901760873, 0.006595947909537601059, 0.006650914142117081082, 0.006705880374696561105, 0.006815812839855521152, 0.007035677770173440378 ),
 .UNSPECIFIED. ) 
 GEOMETRIC_REPRESENTATION_ITEM ( )  RATIONAL_B_SPLINE_SURFACE ( (
 ( 1.000000000000000000, 1.000000000000000000, 1.000000000000000000, 1.000000000000000000, 1.000000000000000000, 1.000000000000000000, 1.000000000000000000, 1.000000000000000000, 1.000000000000000000, 1.000000000000000000, 1.000000000000000000, 1.000000000000000000, 1.000000000000000000, 1.000000000000000000, 1.000000000000000000, 1.000000000000000000, 1.000000000000000000, 1.000000000000000000, 1.000000000000000000, 1.000000000000000000, 1.000000000000000000, 1.000000000000000000, 1.000000000000000000, 1.000000000000000000, 1.000000000000000000, 1.000000000000000000, 1.000000000000000000, 1.000000000000000000, 1.000000000000000000, 1.000000000000000000),
 ( 1.857142857142858317, 1.857142857142858317, 1.857142857142860093, 1.857142857142860093, 1.857142857142858317, 1.857142857142858317, 1.857142857142858317, 1.857142857142858317, 1.857142857142858317, 1.857142857142858317, 1.857142857142858317, 1.857142857142858317, 1.857142857142858317, 1.857142857142858317, 1.857142857142858317, 1.857142857142858317, 1.857142857142858317, 1.857142857142858317, 1.857142857142858317, 1.857142857142858317, 1.857142857142858317, 1.857142857142858317, 1.857142857142858317, 1.857142857142858317, 1.857142857142858317, 1.857142857142858317, 1.857142857142858317, 1.857142857142858317, 1.857142857142858317, 1.857142857142858317),
 ( 1.000000000000000000, 1.000000000000000000, 1.000000000000000000, 1.000000000000000000, 1.000000000000000000, 1.000000000000000000, 1.000000000000000000, 1.000000000000000000, 1.000000000000000000, 1.000000000000000000, 1.000000000000000000, 1.000000000000000000, 1.000000000000000000, 1.000000000000000000, 1.000000000000000000, 1.000000000000000000, 1.000000000000000000, 1.000000000000000000, 1.000000000000000000, 1.000000000000000000, 1.000000000000000000, 1.000000000000000000, 1.000000000000000000, 1.000000000000000000, 1.000000000000000000, 1.000000000000000000, 1.000000000000000000, 1.000000000000000000, 1.000000000000000000, 1.000000000000000000) ) ) 
 REPRESENTATION_ITEM ( '' )  SURFACE ( )  );
#1384=CARTESIAN_POINT ( 'NONE',  ( 57.09426686933954898, 50.00000000000000000, -27.25041924768392576 ) ) ;
#1418=SURFACE_STYLE_USAGE ( .BOTH. , #50506 ) ;
#1419=ORIENTED_EDGE ( 'NONE', *, *, #69551, .F. ) ;
#1424=VECTOR ( 'NONE', #7236, 1000.000000000000000 ) ;
#1433=CARTESIAN_POINT ( 'NONE',  ( -11.68767211932355465, 50.00000000000000000, -88.14097461399492772 ) ) ;
#1454=VECTOR ( 'NONE', #92157, 1000.000000000000000 ) ;
#1483=COLOUR_RGB ( '', 0.09019608, 0.27058824, 0.51372549) ;
#1538=CARTESIAN_POINT ( 'NONE',  ( -17.49999999999997513, 47.00000000000000000, 64.09953197959339377 ) ) ;
#1539=CARTESIAN_POINT ( 'NONE',  ( -79.13121736037263076, 42.00000000000000000, -45.60838156032659185 ) ) ;
#1565=CARTESIAN_POINT ( 'NONE',  ( 18.30269215000137351, 45.00000000000000000, 62.40549835204959805 ) ) ;
#1590=CARTESIAN_POINT ( 'NONE',  ( -1.347801180114141628, -3.000000000000002665, -99.99999999999927525 ) ) ;
#1608=CARTESIAN_POINT ( 'NONE',  ( -19.01558148378874691, 49.54233067771259869, 61.88543008401511258 ) ) ;
#1614=ORIENTED_EDGE ( 'NONE', *, *, #70657, .F. ) ;
#1630=CARTESIAN_POINT ( 'NONE',  ( -1.308996937483428491, -5.000000000000002665, -75.00000000000001421 ) ) ;
#1643=CARTESIAN_POINT ( 'NONE',  ( -5.420469775605654128, 41.88321586335170821, -59.04137891894603030 ) ) ;
#1648=CARTESIAN_POINT ( 'NONE',  ( -7.500000000000007105, -3.000000000000000000, -68.91429205785459544 ) ) ;
#1664=CARTESIAN_POINT ( 'NONE',  ( 16.06569373956322266, 42.44590539575593624, -88.41332270392955195 ) ) ;
#1688=MECHANICAL_DESIGN_GEOMETRIC_PRESENTATION_REPRESENTATION('',(#24143),#101559);
#1695=CARTESIAN_POINT ( 'NONE',  ( -7.439139359426217624, 41.00331351352566145, -59.84461297751296627 ) ) ;
#1715=CARTESIAN_POINT ( 'NONE',  ( -10.48543666094594862, -5.000000000000002665, -91.04342776276726568 ) ) ;
#1750=FILL_AREA_STYLE_COLOUR ( '', #27264 ) ;
#1755=CARTESIAN_POINT ( 'NONE',  ( 1.448103213439550618, -5.000000000000000888, -72.00403106213767046 ) ) ;
#1775=CARTESIAN_POINT ( 'NONE',  ( 90.56128410203886858, 42.00000000000000000, -11.85444436786857558 ) ) ;
#1784=CARTESIAN_POINT ( 'NONE',  ( 59.27219564965441378, 40.83785294361205587, 26.84540320310011197 ) ) ;
#1801=CARTESIAN_POINT ( 'NONE',  ( 4.644559862127829675, 48.00000000000000711, -99.31133601631377417 ) ) ;
#1803=CARTESIAN_POINT ( 'NONE',  ( -7.499934961134938405, 40.55407393519936221, -69.64904099334012244 ) ) ;
#1838=CARTESIAN_POINT ( 'NONE',  ( 12.50000000000000355, 27.37863077022358027, -44.93064604781708482 ) ) ;
#1866=CARTESIAN_POINT ( 'NONE',  ( -7.413000813362873309, 41.14546169070921877, -59.83891281791527916 ) ) ;
#1874=CARTESIAN_POINT ( 'NONE',  ( -7.500000000000007105, -3.000000000000000000, -68.91429205785459544 ) ) ;
#1890=CARTESIAN_POINT ( 'NONE',  ( -5.957442974701830707, 48.00000000000000000, 65.00000000000000000 ) ) ;
#1895=CARTESIAN_POINT ( 'NONE',  ( -6.232496158895186156, 41.83455024993975968, -59.02481301687200244 ) ) ;
#1909=DIRECTION ( 'NONE',  ( 0.000000000000000000, 1.000000000000000000, 0.000000000000000000 ) ) ;
#1921=UNCERTAINTY_MEASURE_WITH_UNIT (LENGTH_MEASURE( 1.000000000000000082E-05 ), #29795, 'distance_accuracy_value', 'NONE');
#1928=CARTESIAN_POINT ( 'NONE',  ( 28.89099332389485042, 49.99999999997997691, 58.53034795348389707 ) ) ;
#1941=CARTESIAN_POINT ( 'NONE',  ( -31.82717529008558799, 18.64284798593262593, -21.53956455646148527 ) ) ;
#1972=CARTESIAN_POINT ( 'NONE',  ( -10.48543666094731464, 50.00000000000000000, -91.04342776276725147 ) ) ;
#1975=ORIENTED_EDGE ( 'NONE', *, *, #64833, .F. ) ;
#1980=EDGE_CURVE ( 'NONE', #45703, #33011, #92308, .T. ) ;
#1995=B_SPLINE_CURVE_WITH_KNOTS ( 'NONE', 3,
 ( #67727, #45062, #77411, #20292, #27314, #10010, #18674, #3528, #43981, #92520, #36467, #51528, #102215, #93063, #84445, #4057, #28362, #53141, #102750, #61786, #10537, #18128, #50984, #2444, #63897, #37523, #31018, #96786, #22917, #104326, #13185, #86594, #4588, #55754, #21333, #88162, #12658, #55238, #30473, #5639, #46629, #62830, #38563, #94681, #72494, #105399, #53661, #31543, #95721, #21860, #20828, #95200, #13720, #63370, #45588, #54702, #87635, #78467, #88686, #14246, #14781, #70387, #47676, #5120 ),
 .UNSPECIFIED., .F., .F.,
 ( 4, 1, 1, 1, 1, 2, 2, 1, 1, 1, 2, 2, 1, 1, 2, 2, 1, 1, 1, 2, 2, 1, 1, 1, 2, 2, 1, 1, 1, 1, 2, 2, 1, 1, 1, 1, 2, 2, 1, 1, 1, 1, 1, 2, 2, 4 ),
 ( 0.000000000000000000, 0.06250000000002220446, 0.09375000000003327894, 0.1093750000000388162, 0.1171875000000364569, 0.1210937500000405925, 0.1250000000000447142, 0.1875000000000952571, 0.2187500000001203759, 0.2343750000001331713, 0.2421875000001395550, 0.2500000000001459388, 0.3125000000001888489, 0.3437500000002124967, 0.3593750000002264300, 0.3750000000002403633, 0.4062500000002738365, 0.4218750000002892686, 0.4296875000002963740, 0.4335937500002993161, 0.4375000000003022582, 0.4687500000003195777, 0.4843750000003300138, 0.4921875000003336220, 0.4960937500003369527, 0.5000000000003402834, 0.5625000000003637091, 0.5937500000003747003, 0.6093750000003824718, 0.6171875000003853584, 0.6210937500003826939, 0.6250000000003799183, 0.6875000000003140821, 0.7187500000002793321, 0.7343750000002625677, 0.7421875000002535749, 0.7460937500002484679, 0.7500000000002434719, 0.8125000000001709743, 0.8437500000001322276, 0.8593750000001146860, 0.8671875000001059153, 0.8710937500001014744, 0.8730468750001000311, 0.8750000000000984768, 1.000000000000000000 ),
 .UNSPECIFIED. ) ;
#2000=ORIENTED_EDGE ( 'NONE', *, *, #46736, .T. ) ;
#2026=DIRECTION ( 'NONE',  ( 0.000000000000000000, 1.000000000000000000, 0.000000000000000000 ) ) ;
#2036=CARTESIAN_POINT ( 'NONE',  ( -7.751476769693538493, 50.00000000000000711, -95.64149282985064815 ) ) ;
#2037=COLOUR_RGB ( '', 0.08235294, 0.09019608, 0.10196078) ;
#2053=CARTESIAN_POINT ( 'NONE',  ( 9.500000000000000000, -5.000000000000000000, -20.99851272547260095 ) ) ;
#2076=CARTESIAN_POINT ( 'NONE',  ( 23.70422451878993186, 42.00000000000000000, 88.20421627933662023 ) ) ;
#2079=( NAMED_UNIT ( * ) PLANE_ANGLE_UNIT ( ) SI_UNIT ( $, .RADIAN. ) );
#2122=CARTESIAN_POINT ( 'NONE',  ( 10.19007819943552562, -3.000000000000002665, -96.34610920172687543 ) ) ;
#2123=CARTESIAN_POINT ( 'NONE',  ( 2.695484166361491685, -3.000000000000002665, -99.81725120020546171 ) ) ;
#2137=( GEOMETRIC_REPRESENTATION_CONTEXT ( 3 ) GLOBAL_UNCERTAINTY_ASSIGNED_CONTEXT ( ( #77264 ) ) GLOBAL_UNIT_ASSIGNED_CONTEXT ( ( #2316, #93484, #26648 ) ) REPRESENTATION_CONTEXT ( 'NONE', 'WORKASPACE' ) );
#2195=CARTESIAN_POINT ( 'NONE',  ( 7.500000000000001776, -4.999999999999998224, -68.91429205785460965 ) ) ;
#2203=CARTESIAN_POINT ( 'NONE',  ( -11.44495203399156047, -4.945649015923802239, -12.56974089514457127 ) ) ;
#2207=CARTESIAN_POINT ( 'NONE',  ( 14.33580413386840213, 42.00000000000000000, -89.41414995614803729 ) ) ;
#2214=EDGE_LOOP ( 'NONE', ( #94723, #68154, #69718, #103687 ) ) ;
#2219=CARTESIAN_POINT ( 'NONE',  ( -7.217786764392071674, 41.17942498929775752, -58.69594858756412492 ) ) ;
#2220=CARTESIAN_POINT ( 'NONE',  ( 6.689297305232898339, 41.36669071814934284, -70.70516774953483718 ) ) ;
#2228=ADVANCED_FACE ( 'NONE', ( #29597 ), #82484, .T. ) ;
#2240=CARTESIAN_POINT ( 'NONE',  ( 11.68767211932491712, -5.000000000000002665, -88.14097461399492772 ) ) ;
#2306=CARTESIAN_POINT ( 'NONE',  ( -88.20421627925426833, 42.00000000000000000, -23.70422451879017345 ) ) ;
#2316=( LENGTH_UNIT ( ) NAMED_UNIT ( * ) SI_UNIT ( .MILLI., .METRE. ) );
#2337=CARTESIAN_POINT ( 'NONE',  ( -3.140974613988893882, 50.00000000000000000, -96.68767211932436112 ) ) ;
#2342=MECHANICAL_DESIGN_GEOMETRIC_PRESENTATION_REPRESENTATION('',(#81542),#38557);
#2364=ORIENTED_EDGE ( 'NONE', *, *, #44524, .F. ) ;
#2377=CARTESIAN_POINT ( 'NONE',  ( -17.49999999999997158, 45.00000000000000000, 63.96297035378971430 ) ) ;
#2398=B_SPLINE_CURVE_WITH_KNOTS ( 'NONE', 3,
 ( #27469, #59271, #100239, #68965 ),
 .UNSPECIFIED., .F., .F.,
 ( 4, 4 ),
 ( 0.000000000000000000, 1.000000000000000000 ),
 .UNSPECIFIED. ) ;
#2415=CARTESIAN_POINT ( 'NONE',  ( -7.500000000000000888, -3.000671055698259870, -20.99923901233272971 ) ) ;
#2444=CARTESIAN_POINT ( 'NONE',  ( 17.86116378879217947, 50.00000000000001421, 62.08262986194836941 ) ) ;
#2457=ORIENTED_EDGE ( 'NONE', *, *, #57891, .T. ) ;
#2462=( NAMED_UNIT ( * ) PLANE_ANGLE_UNIT ( ) SI_UNIT ( $, .RADIAN. ) );
#2464=CARTESIAN_POINT ( 'NONE',  ( 6.192999873758675555, 41.95244004319645370, -69.88362896166722749 ) ) ;
#2465=CARTESIAN_POINT ( 'NONE',  ( -43.69716417793774355, 49.99999999999999289, 48.48761666241306756 ) ) ;
#2476=CARTESIAN_POINT ( 'NONE',  ( -20.60725157157436271, 18.64284798593326897, -32.43860525506139680 ) ) ;
#2486=ORIENTED_EDGE ( 'NONE', *, *, #94247, .T. ) ;
#2488=CARTESIAN_POINT ( 'NONE',  ( 42.28239405630658609, 39.52470879392900116, -49.91881956612604654 ) ) ;
#2508=CARTESIAN_POINT ( 'NONE',  ( -7.996668422912395435, 49.99999999999999289, -78.85453279917057046 ) ) ;
#2520=CARTESIAN_POINT ( 'NONE',  ( 4.966176485634622217, 41.64999999999998437, -70.47555195150158625 ) ) ;
#2524=CARTESIAN_POINT ( 'NONE',  ( 5.448357755207406505, 41.97585525106359228, -59.38396075874230462 ) ) ;
#2551=CARTESIAN_POINT ( 'NONE',  ( -19.20992587373993743, 50.00000000000000000, 60.30093796704041154 ) ) ;
#2552=CARTESIAN_POINT ( 'NONE',  ( 6.618366600630484875, -4.380080200177189020, -16.79229307443605634 ) ) ;
#2594=CARTESIAN_POINT ( 'NONE',  ( -6.839476510410545274, 41.56703046073248231, -58.82533836030189178 ) ) ;
#2599=EDGE_LOOP ( 'NONE', ( #13977, #27475, #62002, #75144, #46558, #25817 ) ) ;
#2613=CARTESIAN_POINT ( 'NONE',  ( 6.814345205900305125, 41.80574652968896032, -59.39410049655393919 ) ) ;
#2616=( BOUNDED_CURVE ( )  B_SPLINE_CURVE ( 2, ( #37375, #70237, #94530 ),
 .UNSPECIFIED., .F., .F. ) 
 B_SPLINE_CURVE_WITH_KNOTS ( ( 3, 3 ),
 ( 0.000000000000000000, 1.000000000000000000 ),
 .UNSPECIFIED. ) 
 CURVE ( )  GEOMETRIC_REPRESENTATION_ITEM ( )  RATIONAL_B_SPLINE_CURVE ( ( 1.000000000000000000, 1.857142857142858317, 1.000000000000000000 ) ) 
 REPRESENTATION_ITEM ( '' )  );
#2623=CARTESIAN_POINT ( 'NONE',  ( 6.426573913663801818, 41.32130124522555548, -58.37301945749069887 ) ) ;
#2662=CARTESIAN_POINT ( 'NONE',  ( -11.46641754970852389, -3.000000000000002665, -75.26692388747358109 ) ) ;
#2705=CARTESIAN_POINT ( 'NONE',  ( -8.737863884121431113, -3.000000000000002665, -90.03618980231151170 ) ) ;
#2733=CARTESIAN_POINT ( 'NONE',  ( 15.92158449169821566, 43.99413677374014497, -88.61144016494736775 ) ) ;
#2735=CARTESIAN_POINT ( 'NONE',  ( 7.141975279376893582, -5.000000000001887379, -70.98863559356587416 ) ) ;
#2747=SURFACE_STYLE_FILL_AREA ( #52362 ) ;
#2758=CARTESIAN_POINT ( 'NONE',  ( -9.500000000000001776, -5.000000000000000000, -36.97043916959992771 ) ) ;
#2761=CARTESIAN_POINT ( 'NONE',  ( -18.94687734119027311, 49.29083859698900483, 62.03598969463124035 ) ) ;
#2762=CARTESIAN_POINT ( 'NONE',  ( -7.176875562314381618, 41.55694621307963388, -59.30926738746194360 ) ) ;
#2765=CARTESIAN_POINT ( 'NONE',  ( 6.561888995895321486, 40.92548677608137808, -71.07459853153341101 ) ) ;
#2778=CARTESIAN_POINT ( 'NONE',  ( 12.49694919028371842, -3.284571130112392545, -14.00564984344996411 ) ) ;
#2781=CARTESIAN_POINT ( 'NONE',  ( 6.738100180926640093, 41.71798714554645215, -59.05424661244425266 ) ) ;
#2783=( NAMED_UNIT ( * ) PLANE_ANGLE_UNIT ( ) SI_UNIT ( $, .RADIAN. ) );
#2797=CARTESIAN_POINT ( 'NONE',  ( 1.647285698089598460, -3.000000000000002665, -70.00000000000000000 ) ) ;
#2805=CARTESIAN_POINT ( 'NONE',  ( 35.39685905336809668, 18.64284798592731462, 14.96610495030122934 ) ) ;
#2822=CARTESIAN_POINT ( 'NONE',  ( -10.51296777078104050, 50.00000000000000000, -92.64705882352942012 ) ) ;
#2830=CARTESIAN_POINT ( 'NONE',  ( 19.50000000000170175, 50.00000000000003553, 59.91915230424470451 ) ) ;
#2846=CARTESIAN_POINT ( 'NONE',  ( 23.70422451878993186, 42.00000000000000000, 88.20421627933662023 ) ) ;
#2852=CARTESIAN_POINT ( 'NONE',  ( 63.17895952939625914, 40.83918185556188263, 15.56336160550995906 ) ) ;
#2877=CARTESIAN_POINT ( 'NONE',  ( -1.308996938995748316, 48.00000000000000711, -75.00000000000001421 ) ) ;
#2879=CARTESIAN_POINT ( 'NONE',  ( 6.701893401236465486, 41.44328394225253476, -70.59544911815949320 ) ) ;
#2891=CARTESIAN_POINT ( 'NONE',  ( -6.280859837934959167, 40.29318109963620032, -71.19386791582113005 ) ) ;
#2939=( LENGTH_UNIT ( ) NAMED_UNIT ( * ) SI_UNIT ( .MILLI., .METRE. ) );
#2946=CARTESIAN_POINT ( 'NONE',  ( 10.50000000000000178, -5.000000000000000000, -12.52300748975612166 ) ) ;
#2950=CARTESIAN_POINT ( 'NONE',  ( -1.757245493087633337, -4.333298119783843383, 17.83319508841453427 ) ) ;
#2953=CARTESIAN_POINT ( 'NONE',  ( 1.308996938995746984, 47.99999999999999289, -75.00000000000000000 ) ) ;
#2957=CARTESIAN_POINT ( 'NONE',  ( 5.036189803708992940, -3.000000000000003109, -76.26213611645744095 ) ) ;
#2960=CARTESIAN_POINT ( 'NONE',  ( -10.51296777078104050, 50.00000000000000000, -92.64705882352942012 ) ) ;
#2961=CARTESIAN_POINT ( 'NONE',  ( 52.56483885390522204, 48.00000000000000000, -38.23529411764705799 ) ) ;
#3006=CARTESIAN_POINT ( 'NONE',  ( 6.701893401236465486, 41.44328394225253476, -70.59544911815949320 ) ) ;
#3007=CARTESIAN_POINT ( 'NONE',  ( 5.957442974701733007, 49.99999999999999289, 65.00000000000000000 ) ) ;
#3031=CARTESIAN_POINT ( 'NONE',  ( 33.09766195399677713, 40.69685746902134582, -62.13808003497683075 ) ) ;
#3032=UNCERTAINTY_MEASURE_WITH_UNIT (LENGTH_MEASURE( 1.000000000000000082E-05 ), #5940, 'distance_accuracy_value', 'NONE');
#3038=ORIENTED_EDGE ( 'NONE', *, *, #37140, .T. ) ;
#3047=( NAMED_UNIT ( * ) PLANE_ANGLE_UNIT ( ) SI_UNIT ( $, .RADIAN. ) );
#3050=CARTESIAN_POINT ( 'NONE',  ( 2.617478844991759868, 50.00000000000001421, -94.73972676610910071 ) ) ;
#3104=VERTEX_POINT ( 'NONE', #48653 ) ;
#3108=CARTESIAN_POINT ( 'NONE',  ( -17.49999999999997513, 45.00000000000000711, -500000.0000000000582 ) ) ;
#3114=CARTESIAN_POINT ( 'NONE',  ( 9.289992159469221633, 50.00000000000000711, -94.32837231712201742 ) ) ;
#3136=CARTESIAN_POINT ( 'NONE',  ( -6.528714966258958974, 41.70354536991147398, -70.35321464783143597 ) ) ;
#3161=CARTESIAN_POINT ( 'NONE',  ( 7.754160006507071046, 42.00000000000000711, -59.23741894013591036 ) ) ;
#3165=STYLED_ITEM ( 'NONE', ( #87753 ), #44467 ) ;
#3190=CARTESIAN_POINT ( 'NONE',  ( 7.121430446328069763, 40.29466766088835072, -71.00332351279642751 ) ) ;
#3215=CARTESIAN_POINT ( 'NONE',  ( 15.04647843581836497, -3.000000000000002665, -85.64811627162752927 ) ) ;
#3247=VECTOR ( 'NONE', #91322, 1000.000000000000000 ) ;
#3258=CARTESIAN_POINT ( 'NONE',  ( 6.642722263319527087, 41.46658730130243953, -70.60825968728163105 ) ) ;
#3262=CARTESIAN_POINT ( 'NONE',  ( 17.55833715088428093, -4.999999999999999112, -1.075502477178110317 ) ) ;
#3294=CARTESIAN_POINT ( 'NONE',  ( -5.365535441410388628, 42.28877518162276061, -59.25308630239388208 ) ) ;
#3305=CARTESIAN_POINT ( 'NONE',  ( -18.97587827957842066, 49.43159474368409434, 61.96476824398673955 ) ) ;
#3308=CARTESIAN_POINT ( 'NONE',  ( 6.870942159525867510, 40.00000000392758182, -71.15487301629636363 ) ) ;
#3321=CARTESIAN_POINT ( 'NONE',  ( 5.293250127137346439, 18.43355203274099807, -37.80931412032270345 ) ) ;
#3326=CARTESIAN_POINT ( 'NONE',  ( 0.000000000000000000, -5.000000000000002665, -73.00000000000001421 ) ) ;
#3335=EDGE_CURVE ( 'NONE', #21469, #9002, #30130, .T. ) ;
#3360=CARTESIAN_POINT ( 'NONE',  ( 9.999872502480483760, -5.000000000000000000, 1.308371270547806331 ) ) ;
#3378=CARTESIAN_POINT ( 'NONE',  ( 19.50000000000146017, 49.99999999999911893, 59.56761335716116434 ) ) ;
#3394=CARTESIAN_POINT ( 'NONE',  ( -79.13121736037263076, 42.00000000000000000, -45.60838156032659185 ) ) ;
#3403=CARTESIAN_POINT ( 'NONE',  ( -39.07690614691289710, 40.83957160057924796, 52.28546855715760699 ) ) ;
#3411=ORIENTED_EDGE ( 'NONE', *, *, #32747, .F. ) ;
#3423=CARTESIAN_POINT ( 'NONE',  ( -7.374560640982810611, 50.00000000000000000, -75.40399789251387119 ) ) ;
#3432=AXIS2_PLACEMENT_3D ( 'NONE', #101971, #83136, #84736 ) ;
#3438=CARTESIAN_POINT ( 'NONE',  ( -7.500000000000007105, -4.999999999999999112, -68.91429205785460965 ) ) ;
#3446=CARTESIAN_POINT ( 'NONE',  ( -6.541889698517638685, 41.04792438554813572, -71.02384096075095954 ) ) ;
#3479=CARTESIAN_POINT ( 'NONE',  ( -33.14701693048364461, 42.84762493505142089, -64.93038575622274777 ) ) ;
#3501=CARTESIAN_POINT ( 'NONE',  ( -17.91929324317234418, -4.333298119783932201, -0.09842992240431641671 ) ) ;
#3508=CARTESIAN_POINT ( 'NONE',  ( 2.617478843592802029, -3.000000000000003109, -94.73972676668317661 ) ) ;
#3517=CARTESIAN_POINT ( 'NONE',  ( -7.040972322291190189, 41.74416393942964731, -59.82830748482982841 ) ) ;
#3528=CARTESIAN_POINT ( 'NONE',  ( 17.51640565573907438, 49.99999999999999289, 63.26730910660373297 ) ) ;
#3539=CARTESIAN_POINT ( 'NONE',  ( -7.347171990171222689, -3.439186728100687596, -18.43985286355804831 ) ) ;
#3550=CARTESIAN_POINT ( 'NONE',  ( 6.583551125402590465, 41.48989066035234430, -70.62107025640376889 ) ) ;
#3551=CARTESIAN_POINT ( 'NONE',  ( 28.00203968317441294, 50.00000000000000000, 56.72941417029700517 ) ) ;
#3574=CARTESIAN_POINT ( 'NONE',  ( 39.47751996913581252, 39.86337285071881809, -53.66483119571051930 ) ) ;
#3590=FACE_OUTER_BOUND ( 'NONE', #50591, .T. ) ;
#3592=CARTESIAN_POINT ( 'NONE',  ( 10.48543666094731996, 50.00000000000000000, -91.04342776276723725 ) ) ;
#3604=CARTESIAN_POINT ( 'NONE',  ( -9.739726766683149961, -3.000000000000003109, -87.61747884359282068 ) ) ;
#3610=ORIENTED_EDGE ( 'NONE', *, *, #77241, .F. ) ;
#3611=( NAMED_UNIT ( * ) SI_UNIT ( $, .STERADIAN. ) SOLID_ANGLE_UNIT ( ) );
#3626=CARTESIAN_POINT ( 'NONE',  ( -7.004291982367331748, 40.56179000230169862, -71.01843131766943884 ) ) ;
#3637=CARTESIAN_POINT ( 'NONE',  ( -19.18847942102290105, 50.00000000000000711, 60.33013323338799694 ) ) ;
#3653=EDGE_LOOP ( 'NONE', ( #14102, #42548, #16534, #14308, #83937 ) ) ;
#3663=CARTESIAN_POINT ( 'NONE',  ( 11.69514296591890634, 50.00000000000000000, -81.87740575805389653 ) ) ;
#3676=CARTESIAN_POINT ( 'NONE',  ( -6.491942716630055621, 41.63185015298623171, -70.49544021750806166 ) ) ;
#3681=CARTESIAN_POINT ( 'NONE',  ( 16.39435414257611257, -5.000000000000000000, -0.9786479702816777149 ) ) ;
#3682=CARTESIAN_POINT ( 'NONE',  ( -5.945588682461652397, 41.44588094979337001, -58.45240144925728032 ) ) ;
#3692=B_SPLINE_CURVE_WITH_KNOTS ( 'NONE', 3,
 ( #2415, #84942, #11562, #1874 ),
 .UNSPECIFIED., .F., .F.,
 ( 4, 4 ),
 ( 0.000000000000000000, 1.000000000000000000 ),
 .UNSPECIFIED. ) ;
#3702=CYLINDRICAL_SURFACE ( 'NONE', #50246, 65.00000000000000000 ) ;
#3706=CARTESIAN_POINT ( 'NONE',  ( -30.67950393662606956, 18.64316884711714906, 23.57730434126661834 ) ) ;
#3714=CARTESIAN_POINT ( 'NONE',  ( 6.315605428199792648, 41.49696752016053836, -58.51869397248536586 ) ) ;
#3715=CARTESIAN_POINT ( 'NONE',  ( -5.500000000000007994, 42.00000000000000000, -65.90297133633691828 ) ) ;
#3752=CARTESIAN_POINT ( 'NONE',  ( -9.891797161801507698, -3.000000000000002665, -73.72381496649796873 ) ) ;
#3770=CARTESIAN_POINT ( 'NONE',  ( -17.49999999999997513, 51.99872764530893932, 60.15967750826234806 ) ) ;
#3779=FILL_AREA_STYLE ('',( #77667 ) ) ;
#3785=CARTESIAN_POINT ( 'NONE',  ( -1.797870618338381465, 41.33266196706689755, -58.72278032361812450 ) ) ;
#3796=CARTESIAN_POINT ( 'NONE',  ( -14.22021666642130455, -5.000000000000000000, 8.714242330525310720 ) ) ;
#3797=EDGE_CURVE ( 'NONE', #57829, #3104, #30563, .T. ) ;
#3815=LINE ( 'NONE', #36753, #62674 ) ;
#3818=CARTESIAN_POINT ( 'NONE',  ( 19.49389532278797432, 49.99942041210562849, 60.03759455525020883 ) ) ;
#3830=CARTESIAN_POINT ( 'NONE',  ( -7.500000000000002665, 1.559114133231479071, -21.99325844590496004 ) ) ;
#3831=UNCERTAINTY_MEASURE_WITH_UNIT (LENGTH_MEASURE( 1.000000000000000082E-05 ), #29524, 'distance_accuracy_value', 'NONE');
#3847=CARTESIAN_POINT ( 'NONE',  ( 4.872636759907720716, 41.00341855746686548, -70.74912513459382524 ) ) ;
#3858=ORIENTED_EDGE ( 'NONE', *, *, #61215, .F. ) ;
#3864=CARTESIAN_POINT ( 'NONE',  ( 6.043427762770655853, -5.000000000000002665, -95.48543666094731464 ) ) ;
#3876=SURFACE_STYLE_USAGE ( .BOTH. , #45405 ) ;
#3891=CARTESIAN_POINT ( 'NONE',  ( 2.583982984169515440, -5.000000000000000000, -9.743117168495876612 ) ) ;
#3892=CARTESIAN_POINT ( 'NONE',  ( 7.360438360658586809, -5.000000000000000000, -75.39006186636561324 ) ) ;
#3903=CARTESIAN_POINT ( 'NONE',  ( 4.707696486722537266, 48.00000000000000000, -99.43546650846083423 ) ) ;
#3911=CARTESIAN_POINT ( 'NONE',  ( 19.50000000000126832, 49.99999999999980815, 59.82664205501161092 ) ) ;
#3915=B_SPLINE_CURVE_WITH_KNOTS ( 'NONE', 3,
 ( #96102, #6535, #87488, #71281, #23289, #95571, #62166, #47530 ),
 .UNSPECIFIED., .F., .F.,
 ( 4, 2, 2, 4 ),
 ( 0.000000000000000000, 0.5000000000000000000, 0.7500000000000000000, 1.000000000000000000 ),
 .UNSPECIFIED. ) ;
#3917=CARTESIAN_POINT ( 'NONE',  ( 42.97360691268208654, 41.50767547277785496, -51.42105803120703911 ) ) ;
#3926=CARTESIAN_POINT ( 'NONE',  ( 10.04205104292330475, 18.64316884715076839, 37.36680950592799633 ) ) ;
#3953=CARTESIAN_POINT ( 'NONE',  ( 1.469576158976823356E-15, 50.00000000000000000, -73.00000000000001421 ) ) ;
#3969=CARTESIAN_POINT ( 'NONE',  ( -7.500000000000001776, -3.000000000000000000, -36.97043916959987087 ) ) ;
#3979=CARTESIAN_POINT ( 'NONE',  ( -6.661998917891360783, 40.29425637337637767, -71.19925390475410154 ) ) ;
#4017=CARTESIAN_POINT ( 'NONE',  ( 5.025684061874351016, -6.606954474312070502, -14.98089720656572688 ) ) ;
#4024=CARTESIAN_POINT ( 'NONE',  ( 10.68521086147759647, -5.000000000000001776, -12.55427425704376887 ) ) ;
#4045=CARTESIAN_POINT ( 'NONE',  ( -7.054523059426880849, 41.71556238290650498, -59.55896278357374740 ) ) ;
#4057=CARTESIAN_POINT ( 'NONE',  ( 17.59424591481818823, 50.00000000000000711, 62.71031934002806452 ) ) ;
#4069=CARTESIAN_POINT ( 'NONE',  ( 58.26690781281054399, 50.00000000000000711, 24.09029710667956081 ) ) ;
#4079=CARTESIAN_POINT ( 'NONE',  ( 6.241999248351493002, 41.80321055404989039, -70.33316251798440533 ) ) ;
#4083=B_SPLINE_CURVE_WITH_KNOTS ( 'NONE', 3,
 ( #21348, #101824, #5136, #85119 ),
 .UNSPECIFIED., .F., .F.,
 ( 4, 4 ),
 ( 0.000000000000000000, 1.000000000000000000 ),
 .UNSPECIFIED. ) ;
#4103=( LENGTH_UNIT ( ) NAMED_UNIT ( * ) SI_UNIT ( .MILLI., .METRE. ) );
#4105=CARTESIAN_POINT ( 'NONE',  ( 42.29310172631443976, 39.52350749398639351, -49.90450179939642084 ) ) ;
#4119=CARTESIAN_POINT ( 'NONE',  ( 25.60851123651794836, 48.00000000000000000, -75.29411764705879762 ) ) ;
#4130=B_SPLINE_CURVE_WITH_KNOTS ( 'NONE', 3,
 ( #47060, #37964, #62741, #21248 ),
 .UNSPECIFIED., .F., .F.,
 ( 4, 4 ),
 ( 0.000000000000000000, 1.000000000000000000 ),
 .UNSPECIFIED. ) ;
#4138=CARTESIAN_POINT ( 'NONE',  ( -6.573529411764777564, 40.00000000000032685, -71.39502911389392636 ) ) ;
#4150=CARTESIAN_POINT ( 'NONE',  ( -5.292102851260739094, 18.18885909246420596, -37.58867055452670769 ) ) ;
#4165=CARTESIAN_POINT ( 'NONE',  ( -17.81569236505151466, 50.00000000000000000, 62.15697636927347247 ) ) ;
#4190=ORIENTED_EDGE ( 'NONE', *, *, #5905, .F. ) ;
#4194=( BOUNDED_SURFACE ( )  B_SPLINE_SURFACE ( 2, 3, ( 
 ( #48594, #49121, #23302, #40519, #32986, #73397 ),
 ( #8678, #72356, #97154, #106296, #32459, #65331 ),
 ( #80435, #82022, #57743, #41580, #98219, #33510 ) ),
 .UNSPECIFIED., .F., .F., .F. ) 
 B_SPLINE_SURFACE_WITH_KNOTS ( ( 3, 3 ),
 ( 4, 2, 4 ),
 ( 0.000000000000000000, 1.000000000000000000 ),
 ( 0.07468083296558609974, 0.1199308329655860983, 0.1241808329655861021 ),
 .UNSPECIFIED. ) 
 GEOMETRIC_REPRESENTATION_ITEM ( )  RATIONAL_B_SPLINE_SURFACE ( (
 ( 1.000000000000000000, 1.000000000000000000, 1.000000000000000000, 1.000000000000000000, 1.000000000000000000, 1.000000000000000000),
 ( 1.857142857142858317, 1.857142857142858317, 1.857142857142858317, 1.857142857142858317, 1.857142857142858317, 1.857142857142858317),
 ( 1.000000000000000000, 1.000000000000000000, 1.000000000000000000, 1.000000000000000000, 1.000000000000000000, 1.000000000000000000) ) ) 
 REPRESENTATION_ITEM ( '' )  SURFACE ( )  );
#4201=CARTESIAN_POINT ( 'NONE',  ( -6.602502349679192584, 41.80321055419442899, -70.07543150438399948 ) ) ;
#4206=CARTESIAN_POINT ( 'NONE',  ( -6.524042246343456419, -4.999999999999999112, 15.07235311481336559 ) ) ;
#4207=CARTESIAN_POINT ( 'NONE',  ( -6.670526998832738919, 41.45458147225290446, -58.55660974155367171 ) ) ;
#4223=CARTESIAN_POINT ( 'NONE',  ( 6.883638421508285532, 41.77293051532582524, -59.38142182129858071 ) ) ;
#4224=CARTESIAN_POINT ( 'NONE',  ( -29.83308852624522345, 41.99999999999999289, 51.76085035109112198 ) ) ;
#4269=EDGE_CURVE ( 'NONE', #712, #17802, #57090, .T. ) ;
#4274=CARTESIAN_POINT ( 'NONE',  ( 14.61924042696704440, -5.000000000000005329, -89.34162378225812517 ) ) ;
#4282=FACE_OUTER_BOUND ( 'NONE', #88766, .T. ) ;
#4303=DIRECTION ( 'NONE',  ( 0.000000000000000000, 0.000000000000000000, 1.000000000000000000 ) ) ;
#4319=CARTESIAN_POINT ( 'NONE',  ( -8.354779502917955014, -5.000000000000000000, -14.10835818931678176 ) ) ;
#4342=CARTESIAN_POINT ( 'NONE',  ( 19.12649177053515714, 49.70304845705965846, 61.69455185923964535 ) ) ;
#4353=CARTESIAN_POINT ( 'NONE',  ( -5.347321875081102682, 33.30354557871893206, -51.19160682728892908 ) ) ;
#4364=CARTESIAN_POINT ( 'NONE',  ( -18.93411340542660426, 49.15937788526225205, 62.07943494194688583 ) ) ;
#4365=CARTESIAN_POINT ( 'NONE',  ( 17.50000000000002842, 50.00000000000000000, -500000.0000000000582 ) ) ;
#4366=CARTESIAN_POINT ( 'NONE',  ( 6.716520184430065044, 41.04202977371297578, -70.96212004294623910 ) ) ;
#4379=CARTESIAN_POINT ( 'NONE',  ( 5.075566108724593128, -4.332661967060489339, -17.09624963492156269 ) ) ;
#4380=CARTESIAN_POINT ( 'NONE',  ( 12.49999999999999289, -3.156328017129524266, -14.15649578910353412 ) ) ;
#4381=CARTESIAN_POINT ( 'NONE',  ( -1.047197551196596521, -3.000000000000000888, -8.000000000000003553 ) ) ;
#4385=CARTESIAN_POINT ( 'NONE',  ( -7.996668422906947349, -3.000000000000002665, -91.14546720082398679 ) ) ;
#4403=EDGE_CURVE ( 'NONE', #64826, #93842, #88234, .T. ) ;
#4422=( NAMED_UNIT ( * ) PLANE_ANGLE_UNIT ( ) SI_UNIT ( $, .RADIAN. ) );
#4425=CARTESIAN_POINT ( 'NONE',  ( 7.717304146821367894, 50.00000000000000000, -95.65871486498016907 ) ) ;
#4434=FILL_AREA_STYLE_COLOUR ( '', #50862 ) ;
#4436=STYLED_ITEM ( 'NONE', ( #31381 ), #65343 ) ;
#4437=CARTESIAN_POINT ( 'NONE',  ( 26.15549530965961011, 43.57015600928786370, -74.54213887132672767 ) ) ;
#4448=CARTESIAN_POINT ( 'NONE',  ( -23.57730434129643626, 18.64316884713158728, -30.67950393661452679 ) ) ;
#4457=CARTESIAN_POINT ( 'NONE',  ( 56.10215434529457923, 39.42619182473122663, -33.37226973483742398 ) ) ;
#4470=CARTESIAN_POINT ( 'NONE',  ( -6.821717117272705799, 41.99999999999999289, -69.36621149908677353 ) ) ;
#4479=CARTESIAN_POINT ( 'NONE',  ( 5.036189802311931807, 48.00000000000000000, -93.73786388412125348 ) ) ;
#4491=CARTESIAN_POINT ( 'NONE',  ( -1.308996938995744541, 48.00000000000000711, -95.00000000000001421 ) ) ;
#4494=CARTESIAN_POINT ( 'NONE',  ( -12.50000000000000178, -3.000000000000000888, -35.13068384735336736 ) ) ;
#4496=CARTESIAN_POINT ( 'NONE',  ( -9.500000000000007105, -5.000000000000000000, -52.94236561372732552 ) ) ;
#4504=CARTESIAN_POINT ( 'NONE',  ( -4.881098102818297590, 41.14559805159954919, -70.72437845145068991 ) ) ;
#4514=CARTESIAN_POINT ( 'NONE',  ( -17.98970702557545920, 45.00000000000000711, 62.57427701062805170 ) ) ;
#4523=ORIENTED_EDGE ( 'NONE', *, *, #28462, .T. ) ;
#4524=CARTESIAN_POINT ( 'NONE',  ( -12.50000000000000533, 34.36268320169224921, -53.42085938171843651 ) ) ;
#4526=( BOUNDED_CURVE ( )  B_SPLINE_CURVE ( 2, ( #88091, #14171, #47075 ),
 .UNSPECIFIED., .F., .F. ) 
 B_SPLINE_CURVE_WITH_KNOTS ( ( 3, 3 ),
 ( 0.000000000000000000, 1.000000000000000000 ),
 .UNSPECIFIED. ) 
 CURVE ( )  GEOMETRIC_REPRESENTATION_ITEM ( )  RATIONAL_B_SPLINE_CURVE ( ( 1.000000000000000000, 1.857142857142858317, 1.000000000000000000 ) ) 
 REPRESENTATION_ITEM ( '' )  );
#4534=CARTESIAN_POINT ( 'NONE',  ( 7.039599551806973388, 41.52217469061105959, -58.93052221769676891 ) ) ;
#4543=VECTOR ( 'NONE', #18409, 1000.000000000000000 ) ;
#4545=B_SPLINE_CURVE_WITH_KNOTS ( 'NONE', 3,
 ( #77954, #63385, #36998, #21342, #20840, #87121, #14257, #21872, #96280, #95732, #13195, #12669, #103813, #4069, #22405, #29957, #37535, #54714, #86071, #53670, #55249, #45600, #30484, #78476, #4600, #70399, #70920, #46639, #87649, #13731, #45072 ),
 .UNSPECIFIED., .F., .F.,
 ( 4, 2, 2, 2, 1, 1, 2, 2, 2, 2, 1, 2, 2, 1, 1, 2, 2, 4 ),
 ( 0.5714977658632183211, 0.6250605451303161697, 0.6786233243974139073, 0.6920140192141883695, 0.7054047140309627206, 0.7321861036645116450, 0.7455767984812859961, 0.7589674932980604583, 0.7857488829316092716, 0.8125302725651581959, 0.8393116621987070092, 0.8660930518322558225, 0.8794837466490301736, 0.8928744414658046358, 0.9196558310993534491, 0.9330465259161280223, 0.9464372207329023734, 1.000000000000000000 ),
 .UNSPECIFIED. ) ;
#4546=CARTESIAN_POINT ( 'NONE',  ( 5.693345022498909280, -2.999999999999138467, -71.09407784968016131 ) ) ;
#4553=CARTESIAN_POINT ( 'NONE',  ( 11.59420250832448218, -4.918022519855804298, -12.56327219346357893 ) ) ;
#4558=CARTESIAN_POINT ( 'NONE',  ( 7.500000000000007994, 40.00000000000000000, -71.41947339647144588 ) ) ;
#4572=CARTESIAN_POINT ( 'NONE',  ( 58.76133767613618630, 50.00000000000000000, 23.44026136864407306 ) ) ;
#4579=CARTESIAN_POINT ( 'NONE',  ( -6.883638564027164009, 41.77293021818198326, -59.38142135283953138 ) ) ;
#4588=CARTESIAN_POINT ( 'NONE',  ( 18.10339634169226741, 50.00000000000001421, 61.75574722958666740 ) ) ;
#4600=CARTESIAN_POINT ( 'NONE',  ( 61.03799250145893751, 50.00000000000002132, -15.95017878592576110 ) ) ;
#4613=CARTESIAN_POINT ( 'NONE',  ( 5.892296920977983632, 42.00785640420587441, -69.46301655925690000 ) ) ;
#4631=CARTESIAN_POINT ( 'NONE',  ( 7.380473217280480114, 40.84000775496618729, -58.87770853468460075 ) ) ;
#4638=PRESENTATION_STYLE_ASSIGNMENT (( #53705 ) ) ;
#4656=CARTESIAN_POINT ( 'NONE',  ( 8.737863884125493641, 48.00000000000000000, -90.03618980230170621 ) ) ;
#4682=EDGE_CURVE ( 'NONE', #80415, #83228, #77908, .T. ) ;
#4683=CARTESIAN_POINT ( 'NONE',  ( -5.307398959431215424, 21.45645744618504480, -40.53500383443203248 ) ) ;
#4697=( BOUNDED_SURFACE ( )  B_SPLINE_SURFACE ( 2, 3, ( 
 ( #36224, #77173, #84201, #60483, #35143, #69093, #68565, #59408, #85817, #61542 ),
 ( #2195, #69620, #12417, #102512, #2735, #18425, #28127, #53433, #101967, #92816 ),
 ( #84732, #77707, #43210, #93363, #51280, #27603, #10297, #61004, #76095, #19516 ) ),
 .UNSPECIFIED., .F., .F., .F. ) 
 B_SPLINE_SURFACE_WITH_KNOTS ( ( 3, 3 ),
 ( 4, 2, 2, 2, 4 ),
 ( 0.000000000000000000, 1.000000000000000000 ),
 ( -0.000000000000000000, 0.001626978433639921992, 0.003253956867279843984, 0.004880935300919765976, 0.006507913734559687968 ),
 .UNSPECIFIED. ) 
 GEOMETRIC_REPRESENTATION_ITEM ( )  RATIONAL_B_SPLINE_SURFACE ( (
 ( 1.000000000000000000, 1.000000000000000000, 1.000000000000000000, 1.000000000000000000, 1.000000000000000000, 1.000000000000000000, 1.000000000000000000, 1.000000000000000000, 1.000000000000000000, 1.000000000000000000),
 ( 1.857142857142858317, 1.857142857142858317, 1.857142857142858317, 1.857142857142858317, 1.857142857142858317, 1.857142857142858317, 1.857142857142858317, 1.857142857142858317, 1.857142857142858317, 1.857142857142858317),
 ( 1.000000000000000000, 1.000000000000000000, 1.000000000000000000, 1.000000000000000000, 1.000000000000000000, 1.000000000000000000, 1.000000000000000000, 1.000000000000000000, 1.000000000000000000, 1.000000000000000000) ) ) 
 REPRESENTATION_ITEM ( '' )  SURFACE ( )  );
#4724=ORIENTED_EDGE ( 'NONE', *, *, #10691, .T. ) ;
#4733=CARTESIAN_POINT ( 'NONE',  ( -6.762666706417072682, 41.72339003058417006, -70.10115393879142687 ) ) ;
#4738=CARTESIAN_POINT ( 'NONE',  ( -6.492510984469592294, 41.78432685485347520, -59.03546988472429291 ) ) ;
#4744=CARTESIAN_POINT ( 'NONE',  ( -7.054523059426880849, 41.71556238290650498, -59.55896278357374740 ) ) ;
#4757=CARTESIAN_POINT ( 'NONE',  ( 5.022013495303141006, 18.64316884711713840, 38.36535705883633796 ) ) ;
#4782=FACE_OUTER_BOUND ( 'NONE', #21638, .T. ) ;
#4792=CARTESIAN_POINT ( 'NONE',  ( -11.94276309775233003, -4.800907179085195153, -76.87753680762691033 ) ) ;
#4806=CARTESIAN_POINT ( 'NONE',  ( 3.514268259868478683, -4.333298119783825619, 17.57158721863739004 ) ) ;
#4813=SURFACE_STYLE_FILL_AREA ( #11823 ) ;
#4832=DIRECTION ( 'NONE',  ( -0.5882352941176471894, 0.000000000000000000, 0.8086898285216187476 ) ) ;
#4841=CIRCLE ( 'NONE', #80585, 65.00000000000000000 ) ;
#4843=CARTESIAN_POINT ( 'NONE',  ( 7.305752995879768896, 41.99999999999663913, -58.79284008964064157 ) ) ;
#4854=CARTESIAN_POINT ( 'NONE',  ( 13.76503154704518472, -4.999999999999999112, -10.95334723230558716 ) ) ;
#4878=CARTESIAN_POINT ( 'NONE',  ( 19.44528390683268171, 49.97407526609521256, 60.67034508904624346 ) ) ;
#4893=STYLED_ITEM ( 'NONE', ( #73662 ), #76291 ) ;
#4906=CARTESIAN_POINT ( 'NONE',  ( 6.122251204096708754, 40.00000000294605940, -71.16543156461924013 ) ) ;
#4926=CARTESIAN_POINT ( 'NONE',  ( 0.000000000000000000, -3.000000000000002665, -75.00000000000001421 ) ) ;
#4946=EDGE_CURVE ( 'NONE', #71163, #103692, #4545, .T. ) ;
#4949=CARTESIAN_POINT ( 'NONE',  ( 5.500000000000641265, 42.00000000000000000, -59.88032989331720302 ) ) ;
#4954=CARTESIAN_POINT ( 'NONE',  ( 6.145999768513189743, -5.000000000000000000, -7.996316163939230393 ) ) ;
#4957=DIRECTION ( 'NONE',  ( 0.000000000000000000, -0.000000000000000000, 1.000000000000000000 ) ) ;
#4960=ADVANCED_FACE ( 'NONE', ( #103298 ), #104335, .T. ) ;
#4969=CARTESIAN_POINT ( 'NONE',  ( -42.30916052715512166, 39.52170759503056985, -49.88302887289012233 ) ) ;
#4996=CARTESIAN_POINT ( 'NONE',  ( -61.56154494590426651, 38.95379437484910312, -16.50053755318738880 ) ) ;
#5014=CARTESIAN_POINT ( 'NONE',  ( 6.145467200821944864, 49.99999999999999289, -77.00333157708759302 ) ) ;
#5022=CARTESIAN_POINT ( 'NONE',  ( -15.48058112917927431, 42.57620948808565942, -89.21771955211514182 ) ) ;
#5033=FILL_AREA_STYLE_COLOUR ( '', #61893 ) ;
#5059=( GEOMETRIC_REPRESENTATION_CONTEXT ( 3 ) GLOBAL_UNCERTAINTY_ASSIGNED_CONTEXT ( ( #1921 ) ) GLOBAL_UNIT_ASSIGNED_CONTEXT ( ( #29795, #4422, #78830 ) ) REPRESENTATION_CONTEXT ( 'NONE', 'WORKASPACE' ) );
#5063=CARTESIAN_POINT ( 'NONE',  ( -12.50000000000000711, 39.69996554813628364, -64.82567002250831933 ) ) ;
#5080=CARTESIAN_POINT ( 'NONE',  ( 7.500000000000007105, -3.000000000000000000, -68.91429205785459544 ) ) ;
#5086=CARTESIAN_POINT ( 'NONE',  ( 12.06346645439106524, -4.728929080163736920, -12.59383595214006135 ) ) ;
#5095=CARTESIAN_POINT ( 'NONE',  ( -3.514268259821786700, -4.333298119783847824, 17.57158721864471573 ) ) ;
#5106=CARTESIAN_POINT ( 'NONE',  ( 64.91565662643154155, 50.00000000002004441, 6.815324757472883910 ) ) ;
#5111=CARTESIAN_POINT ( 'NONE',  ( -6.648507154639723638, 41.85229584295817062, -59.35075352205862487 ) ) ;
#5113=CARTESIAN_POINT ( 'NONE',  ( 12.49999999999996092, -3.165118404323130630, -76.70900766830892792 ) ) ;
#5120=CARTESIAN_POINT ( 'NONE',  ( 19.50011280463133545, 50.00000000000000000, 59.90639435984937222 ) ) ;
#5127=ORIENTED_EDGE ( 'NONE', *, *, #59720, .F. ) ;
#5136=CARTESIAN_POINT ( 'NONE',  ( 7.500000000000007105, 39.99999999999998579, -65.90297133634152260 ) ) ;
#5149=CARTESIAN_POINT ( 'NONE',  ( -7.099152841014172211, 41.70084716954765724, -59.82719248405098256 ) ) ;
#5175=ORIENTED_EDGE ( 'NONE', *, *, #78369, .T. ) ;
#5189=SURFACE_STYLE_USAGE ( .BOTH. , #104392 ) ;
#5195=CARTESIAN_POINT ( 'NONE',  ( -7.412969763095563103, 41.14559726925956085, -68.91429205793708945 ) ) ;
#5211=CARTESIAN_POINT ( 'NONE',  ( -5.134976600207776798, -1.158348134558966791, -20.02593271448602863 ) ) ;
#5228=CARTESIAN_POINT ( 'NONE',  ( -17.96553647165958623, 50.00000000000000000, 61.93371160714927726 ) ) ;
#5243=CARTESIAN_POINT ( 'NONE',  ( -7.500000000000007105, -3.000000000000000000, -68.91429205785459544 ) ) ;
#5244=SURFACE_SIDE_STYLE ('',( #88287 ) ) ;
#5255=CARTESIAN_POINT ( 'NONE',  ( -10.50000000000000711, -5.000000000000000000, -77.33514508527181874 ) ) ;
#5260=EDGE_LOOP ( 'NONE', ( #105112, #11609 ) ) ;
#5264=VERTEX_POINT ( 'NONE', #8829 ) ;
#5267=CARTESIAN_POINT ( 'NONE',  ( -6.840796741955091242, 41.85687303122205805, -69.25136139280520808 ) ) ;
#5273=CARTESIAN_POINT ( 'NONE',  ( -5.363597346086541151, 41.33266196706063056, -58.39526881795520552 ) ) ;
#5276=EDGE_CURVE ( 'NONE', #54991, #60656, #95859, .T. ) ;
#5293=CARTESIAN_POINT ( 'NONE',  ( 6.849721346867525540, 41.84384207023756375, -59.83401400531045056 ) ) ;
#5295=CARTESIAN_POINT ( 'NONE',  ( -38.36535705883633085, 18.64316884711714195, -5.022013495247519721 ) ) ;
#5305=ORIENTED_EDGE ( 'NONE', *, *, #73333, .T. ) ;
#5309=DIRECTION ( 'NONE',  ( -1.000000000000000000, 0.000000000000000000, 0.000000000000000000 ) ) ;
#5355=PRESENTATION_STYLE_ASSIGNMENT (( #6925 ) ) ;
#5361=PRODUCT_DEFINITION_SHAPE ( 'NONE', 'NONE',  #65408 ) ;
#5377=CARTESIAN_POINT ( 'NONE',  ( 6.362990258380369468, 41.99999999999664624, -58.90232955951054095 ) ) ;
#5389=AXIS2_PLACEMENT_3D ( 'NONE', #12183, #28413, #102265 ) ;
#5408=CARTESIAN_POINT ( 'NONE',  ( 19.45402185089408320, 49.97988350549956493, 60.58872670499978597 ) ) ;
#5417=DIRECTION ( 'NONE',  ( 0.000000000000000000, 1.000000000000000000, 0.000000000000000000 ) ) ;
#5452=CARTESIAN_POINT ( 'NONE',  ( 9.739726766104286781, -3.000000000000002665, -87.61747884499031613 ) ) ;
#5481=CARTESIAN_POINT ( 'NONE',  ( 0.000000000000000000, 0.000000000000000000, 0.000000000000000000 ) ) ;
#5482=CARTESIAN_POINT ( 'NONE',  ( 1.797870618166049539, 41.33266196706049556, -58.72278032362722655 ) ) ;
#5496=CARTESIAN_POINT ( 'NONE',  ( -36.42954435870697694, 40.26420082970585668, -57.71663982892543032 ) ) ;
#5503=EDGE_CURVE ( 'NONE', #11528, #25938, #21172, .T. ) ;
#5504=CARTESIAN_POINT ( 'NONE',  ( 43.56300790393845546, 41.43655928470000305, -50.61076563407275586 ) ) ;
#5513=CARTESIAN_POINT ( 'NONE',  ( 38.36535705883633796, 18.64316884711713840, 5.022013495247446890 ) ) ;
#5519=CARTESIAN_POINT ( 'NONE',  ( 60.45584459710401859, 39.42448681592218662, 24.06197592465746382 ) ) ;
#5534=CARTESIAN_POINT ( 'NONE',  ( 1.308996937480704004, 49.99999999999999289, -75.00000000000001421 ) ) ;
#5560=CARTESIAN_POINT ( 'NONE',  ( -10.49999999997808331, -5.000000000000000000, -12.52300748972991506 ) ) ;
#5594=CARTESIAN_POINT ( 'NONE',  ( 7.262243063959841649, 41.41224388735756179, -59.17677670479952212 ) ) ;
#5601=CARTESIAN_POINT ( 'NONE',  ( 7.500000000000006217, 31.97088361167178050, -52.67517300286424131 ) ) ;
#5620=CARTESIAN_POINT ( 'NONE',  ( 52.56483885390523625, 40.83906611471594061, -38.23529411764706509 ) ) ;
#5626=CARTESIAN_POINT ( 'NONE',  ( -52.56483885390515098, 49.99999999999999289, -38.23529411764716457 ) ) ;
#5632=CARTESIAN_POINT ( 'NONE',  ( 12.48044894998498044, -3.649665456918604001, -76.71620004746286270 ) ) ;
#5639=CARTESIAN_POINT ( 'NONE',  ( 18.45801141833800330, 50.00000000000000000, 61.31179837014410339 ) ) ;
#5662=CARTESIAN_POINT ( 'NONE',  ( 7.040971602393473638, 41.74416448739698637, -59.82830749617803434 ) ) ;
#5700=CARTESIAN_POINT ( 'NONE',  ( 6.145467200819017428, 48.00000000000000000, -92.99666842291193802 ) ) ;
#5724=CARTESIAN_POINT ( 'NONE',  ( -7.137815226412437930, -4.999999999998865796, -4.175893272574592530 ) ) ;
#5726=CARTESIAN_POINT ( 'NONE',  ( -5.217392907308656014, 6.510766470966031783, -27.02462356418083544 ) ) ;
#5731=CARTESIAN_POINT ( 'NONE',  ( -4.205882352941162416, -5.000000000000000000, -72.69916451482997388 ) ) ;
#5744=CARTESIAN_POINT ( 'NONE',  ( -46.50260707299666763, 39.63181819133366446, -46.56948492247389737 ) ) ;
#5745=CARTESIAN_POINT ( 'NONE',  ( -17.55366314213746648, 50.00000000000000000, 62.90659931622097645 ) ) ;
#5753=CARTESIAN_POINT ( 'NONE',  ( 17.50000000000466827, 49.88162284957544301, 62.03084827767128218 ) ) ;
#5762=CARTESIAN_POINT ( 'NONE',  ( 0.000000000000000000, -79.93083296558610584, -75.00000000000001421 ) ) ;
#5769=CARTESIAN_POINT ( 'NONE',  ( 6.701893401236465486, 41.44328394225253476, -70.59544911815949320 ) ) ;
#5778=( BOUNDED_CURVE ( )  B_SPLINE_CURVE ( 2, ( #104715, #28762, #21196 ),
 .UNSPECIFIED., .F., .F. ) 
 B_SPLINE_CURVE_WITH_KNOTS ( ( 3, 3 ),
 ( 0.000000000000000000, 1.000000000000000000 ),
 .UNSPECIFIED. ) 
 CURVE ( )  GEOMETRIC_REPRESENTATION_ITEM ( )  RATIONAL_B_SPLINE_CURVE ( ( 1.000000000000000000, 1.857142857142858317, 1.000000000000000000 ) ) 
 REPRESENTATION_ITEM ( '' )  );
#5780=ORIENTED_EDGE ( 'NONE', *, *, #54250, .F. ) ;
#5818=ORIENTED_EDGE ( 'NONE', *, *, #57618, .T. ) ;
#5825=B_SPLINE_CURVE_WITH_KNOTS ( 'NONE', 3,
 ( #22248, #103667, #72359, #79387 ),
 .UNSPECIFIED., .F., .F.,
 ( 4, 4 ),
 ( 0.000000000000000000, 1.000000000000000000 ),
 .UNSPECIFIED. ) ;
#5832=CARTESIAN_POINT ( 'NONE',  ( -12.49955057333833253, -4.332870170146376765, -12.71907580221295220 ) ) ;
#5833=CARTESIAN_POINT ( 'NONE',  ( 9.500000000000003553, -5.000000000000000000, -68.91429205785459544 ) ) ;
#5857=CARTESIAN_POINT ( 'NONE',  ( -10.00000000000000000, -5.000000000000000000, -2.617993873628155832 ) ) ;
#5890=CARTESIAN_POINT ( 'NONE',  ( 13.05035048251043150, -5.000000000000000000, -10.38464894538376448 ) ) ;
#5899=CARTESIAN_POINT ( 'NONE',  ( -58.13370862442636877, 48.00000000000000711, -29.53088244907756632 ) ) ;
#5905=EDGE_CURVE ( 'NONE', #101469, #59690, #41128, .T. ) ;
#5916=CARTESIAN_POINT ( 'NONE',  ( 19.45509070582273026, 49.98058642384193462, 60.57852761549106191 ) ) ;
#5917=COLOUR_RGB ( '', 0.09019608, 0.27058824, 0.51372549) ;
#5938=CARTESIAN_POINT ( 'NONE',  ( -19.35841150692190737, 49.90777322328655430, 61.14767751163149967 ) ) ;
#5940=( LENGTH_UNIT ( ) NAMED_UNIT ( * ) SI_UNIT ( .MILLI., .METRE. ) );
#5945=SURFACE_SIDE_STYLE ('',( #56069 ) ) ;
#5964=CARTESIAN_POINT ( 'NONE',  ( 9.739726766100236688, -3.000000000000002665, -82.38252115499993522 ) ) ;
#5966=ORIENTED_EDGE ( 'NONE', *, *, #104867, .F. ) ;
#5970=VERTEX_POINT ( 'NONE', #73232 ) ;
#5972=CARTESIAN_POINT ( 'NONE',  ( 7.543027128868171616, -4.999999999993999467, -20.22853049137519221 ) ) ;
#5974=CARTESIAN_POINT ( 'NONE',  ( -11.99986829839305535, 50.00000000000000711, -83.40936345627086723 ) ) ;
#5975=CARTESIAN_POINT ( 'NONE',  ( -34.54222097329575547, 42.66635145815377683, -63.01229731539426382 ) ) ;
#5987=( GEOMETRIC_REPRESENTATION_CONTEXT ( 3 ) GLOBAL_UNCERTAINTY_ASSIGNED_CONTEXT ( ( #27201 ) ) GLOBAL_UNIT_ASSIGNED_CONTEXT ( ( #35919, #19737, #28344 ) ) REPRESENTATION_CONTEXT ( 'NONE', 'WORKASPACE' ) );
#6000=SURFACE_STYLE_USAGE ( .BOTH. , #14084 ) ;
#6014=CARTESIAN_POINT ( 'NONE',  ( 0.000000000000000000, -5.000000000000002665, -73.00000000000001421 ) ) ;
#6017=CARTESIAN_POINT ( 'NONE',  ( 32.93128443270173022, 42.88088526003227940, -65.22696890650703949 ) ) ;
#6034=CARTESIAN_POINT ( 'NONE',  ( 2.972029323994034744, 39.42457582143072159, 64.99968642937007246 ) ) ;
#6052=CARTESIAN_POINT ( 'NONE',  ( 1.224646799147352665E-15, 48.00000000000000000, -75.00000000000001421 ) ) ;
#6064=FACE_OUTER_BOUND ( 'NONE', #23128, .T. ) ;
#6103=CARTESIAN_POINT ( 'NONE',  ( -12.49999999999999645, 22.75697755191607641, -40.20656553242739051 ) ) ;
#6120=CARTESIAN_POINT ( 'NONE',  ( 7.500000000000007105, 40.95611321456068055, -60.73832539154659571 ) ) ;
#6132=CARTESIAN_POINT ( 'NONE',  ( 5.500000000000007994, 42.00000000000000000, -72.67206406577979294 ) ) ;
#6145=CARTESIAN_POINT ( 'NONE',  ( 58.90678327788049273, 50.00000000002003731, -28.11551192221532247 ) ) ;
#6168=FILL_AREA_STYLE ('',( #54181 ) ) ;
#6185=FACE_OUTER_BOUND ( 'NONE', #66952, .T. ) ;
#6189=EDGE_LOOP ( 'NONE', ( #47432, #36007, #92113, #39203 ) ) ;
#6202=CARTESIAN_POINT ( 'NONE',  ( -1.590636543681222870, -4.999999999999999112, -97.00013170161253129 ) ) ;
#6209=PLANE ( 'NONE',  #26981 ) ;
#6218=CARTESIAN_POINT ( 'NONE',  ( -8.737863884121635394, 48.00000000000000000, -90.03618980231102853 ) ) ;
#6238=CARTESIAN_POINT ( 'NONE',  ( 4.175893272574712434, -3.000000000000000000, 7.137815226410047842 ) ) ;
#6243=( NAMED_UNIT ( * ) PLANE_ANGLE_UNIT ( ) SI_UNIT ( $, .RADIAN. ) );
#6257=SURFACE_STYLE_FILL_AREA ( #71531 ) ;
#6266=CARTESIAN_POINT ( 'NONE',  ( 17.50000000000002842, 49.17341269448252206, 64.03715209375951645 ) ) ;
#6273=CARTESIAN_POINT ( 'NONE',  ( -7.500000000000007105, 25.66666666666800012, -68.91429205785459544 ) ) ;
#6274=CARTESIAN_POINT ( 'NONE',  ( -9.060614273896861803, -4.999999999999993783, -17.33913672108680259 ) ) ;
#6322=CARTESIAN_POINT ( 'NONE',  ( 6.611590817483814497, 41.87945146461261459, -59.42330382799539024 ) ) ;
#6344=DIRECTION ( 'NONE',  ( -0.000000000000000000, 1.000000000000000000, -0.000000000000000000 ) ) ;
#6345=ADVANCED_FACE ( 'NONE', ( #104968 ), #87201, .T. ) ;
#6374=( GEOMETRIC_REPRESENTATION_CONTEXT ( 3 ) GLOBAL_UNCERTAINTY_ASSIGNED_CONTEXT ( ( #103059 ) ) GLOBAL_UNIT_ASSIGNED_CONTEXT ( ( #88173, #62317, #79011 ) ) REPRESENTATION_CONTEXT ( 'NONE', 'WORKASPACE' ) );
#6382=CARTESIAN_POINT ( 'NONE',  ( 4.175893272574712434, -3.000000000000000000, 7.137815226410047842 ) ) ;
#6389=CARTESIAN_POINT ( 'NONE',  ( 1.590636543681225312, -5.000000000000000000, -96.99986829838745450 ) ) ;
#6426=CARTESIAN_POINT ( 'NONE',  ( -23.85217781305828311, 47.99999999999999289, 60.68504519422551624 ) ) ;
#6443=CARTESIAN_POINT ( 'NONE',  ( 18.93966886101837233, 49.22383349382435824, 62.05948745186926629 ) ) ;
#6469=CARTESIAN_POINT ( 'NONE',  ( -19.45212154763352430, 49.97862309486527721, 60.60657320435567641 ) ) ;
#6490=CARTESIAN_POINT ( 'NONE',  ( -9.797174393178825657E-16, -3.000000000000000000, 8.000000000000000000 ) ) ;
#6494=CARTESIAN_POINT ( 'NONE',  ( -7.996668422911731078, -5.000000000000002665, -78.85453279917058467 ) ) ;
#6501=CARTESIAN_POINT ( 'NONE',  ( 7.253185102479642765, -3.609892095615550467, -18.04361009492445689 ) ) ;
#6503=CARTESIAN_POINT ( 'NONE',  ( -10.47772246152093700, 50.00000000000000711, -78.93829266524170407 ) ) ;
#6507=B_SPLINE_CURVE_WITH_KNOTS ( 'NONE', 3,
 ( #10662, #77545, #61373, #69459, #70518, #11187, #52724, #19885, #20428, #36065, #3663, #85101, #86191, #78588, #94265, #12265, #93730, #44119 ),
 .UNSPECIFIED., .F., .F.,
 ( 4, 2, 2, 2, 2, 2, 2, 2, 4 ),
 ( 0.5000000000000000000, 0.5625000000000000000, 0.6250000000000000000, 0.6875000000000000000, 0.7500000000000000000, 0.8125000000000000000, 0.8750000000000000000, 0.9375000000000000000, 1.000000000000000000 ),
 .UNSPECIFIED. ) ;
#6535=CARTESIAN_POINT ( 'NONE',  ( 7.109733078360420677, 41.69026692163959069, -59.69141567447950081 ) ) ;
#6542=CARTESIAN_POINT ( 'NONE',  ( -1.570796324976843295, -5.000000000000002665, -97.00000000000000000 ) ) ;
#6545=( NAMED_UNIT ( * ) PLANE_ANGLE_UNIT ( ) SI_UNIT ( $, .RADIAN. ) );
#6562=CARTESIAN_POINT ( 'NONE',  ( -11.84577904457109376, 39.42593554084623975, 63.98138733196459782 ) ) ;
#6581=CARTESIAN_POINT ( 'NONE',  ( 6.145467200814584530, 50.00000000000543565, -92.99666842292452884 ) ) ;
#6588=CARTESIAN_POINT ( 'NONE',  ( -15.92248761028720949, 43.99412595793401692, -88.61019858215870215 ) ) ;
#6593=( GEOMETRIC_REPRESENTATION_CONTEXT ( 3 ) GLOBAL_UNCERTAINTY_ASSIGNED_CONTEXT ( ( #74288 ) ) GLOBAL_UNIT_ASSIGNED_CONTEXT ( ( #25168, #51533, #83368 ) ) REPRESENTATION_CONTEXT ( 'NONE', 'WORKASPACE' ) );
#6613=EDGE_CURVE ( 'NONE', #26386, #88824, #60901, .T. ) ;
#6628=CARTESIAN_POINT ( 'NONE',  ( 7.312789351686414641, 41.37363122699996865, -69.62136458039658748 ) ) ;
#6638=CARTESIAN_POINT ( 'NONE',  ( -12.50000000000000711, 39.72724458256214319, -64.92461122767875281 ) ) ;
#6648=CARTESIAN_POINT ( 'NONE',  ( 31.82717529009398305, 18.64284798592574433, -21.53956455643801604 ) ) ;
#6668=CARTESIAN_POINT ( 'NONE',  ( 5.500000000000007105, 42.00000000000000000, -70.16688272716299934 ) ) ;
#6681=CARTESIAN_POINT ( 'NONE',  ( 37.84772257691316355, 50.00000000000000000, 50.69408796163846631 ) ) ;
#6686=CARTESIAN_POINT ( 'NONE',  ( 12.48746907676921047, -3.545640499968000459, -76.71370838498249611 ) ) ;
#6690=CARTESIAN_POINT ( 'NONE',  ( 7.347880794884118356E-15, 0.000000000000000000, -60.00000000000000000 ) ) ;
#6715=CARTESIAN_POINT ( 'NONE',  ( -16.52732684424165654, 43.98685724163156863, -87.77868211029610279 ) ) ;
#6719=( BOUNDED_SURFACE ( )  B_SPLINE_SURFACE ( 2, 3, ( 
 ( #83543, #27493, #20481, #9644, #3715, #18863, #42554, #67902 ),
 ( #34515, #10187, #100789, #53321, #93243, #75455, #11240, #85148 ),
 ( #10709, #92166, #11776, #44166, #43624, #51166, #68446, #26951 ) ),
 .UNSPECIFIED., .F., .F., .F. ) 
 B_SPLINE_SURFACE_WITH_KNOTS ( ( 3, 3 ),
 ( 4, 2, 2, 4 ),
 ( 0.000000000000000000, 1.000000000000000000 ),
 ( 0.001098271369759734172, 0.002880329893317254419, 0.01191429205785460299, 0.01567206406577980465 ),
 .UNSPECIFIED. ) 
 GEOMETRIC_REPRESENTATION_ITEM ( )  RATIONAL_B_SPLINE_SURFACE ( (
 ( 1.000000000000000000, 1.000000000000000000, 1.000000000000000000, 1.000000000000000000, 1.000000000000000000, 1.000000000000000000, 1.000000000000000000, 1.000000000000000000),
 ( 1.857142857142858317, 1.857142857142858317, 1.857142857142858317, 1.857142857142858317, 1.857142857142858317, 1.857142857142858317, 1.857142857142858317, 1.857142857142858317),
 ( 1.000000000000000000, 1.000000000000000000, 1.000000000000000000, 1.000000000000000000, 1.000000000000000000, 1.000000000000000000, 1.000000000000000000, 1.000000000000000000) ) ) 
 REPRESENTATION_ITEM ( '' )  SURFACE ( )  );
#6721=CARTESIAN_POINT ( 'NONE',  ( 6.917892303299533197, 41.82074860089118573, -68.91429206365098992 ) ) ;
#6745=CARTESIAN_POINT ( 'NONE',  ( -11.99986829839165203, -5.000000000000000000, -86.59063654369539620 ) ) ;
#6797=CARTESIAN_POINT ( 'NONE',  ( 5.420470438621123321, 41.88321586334136981, -59.04137885805280916 ) ) ;
#6800=CARTESIAN_POINT ( 'NONE',  ( -22.51022956527200947, 41.90417131191598799, -79.55355073162097312 ) ) ;
#6809=CARTESIAN_POINT ( 'NONE',  ( 17.49999999999998934, 50.03360497985808308, 63.82236279034708559 ) ) ;
#6817=CARTESIAN_POINT ( 'NONE',  ( -7.261743840243895853, -3.634783834963452698, -18.04052776593958285 ) ) ;
#6838=CARTESIAN_POINT ( 'NONE',  ( 56.06936961874005476, 50.00000000006009770, -33.41736086627872027 ) ) ;
#6853=CARTESIAN_POINT ( 'NONE',  ( -8.786988139152953468E-15, 18.64300841652315910, 38.36521369532682257 ) ) ;
#6854=EDGE_LOOP ( 'NONE', ( #42023, #50113, #47329, #52349 ) ) ;
#6865=CARTESIAN_POINT ( 'NONE',  ( 6.511374583785752179, 41.81949009030999775, -59.12906284281419289 ) ) ;
#6920=CARTESIAN_POINT ( 'NONE',  ( 0.000000000000000000, -5.000000000000000000, 10.00000000000000000 ) ) ;
#6925=SURFACE_STYLE_USAGE ( .BOTH. , #79228 ) ;
#6926=CARTESIAN_POINT ( 'NONE',  ( -10.50000000000000711, -5.000000000000000000, -80.60844091781802945 ) ) ;
#6944=CARTESIAN_POINT ( 'NONE',  ( 12.13034742782427955, 48.00000000000000000, -93.82352941176471006 ) ) ;
#6958=CARTESIAN_POINT ( 'NONE',  ( 14.92208856357891911, -5.000000000000000000, -7.448748508018040226 ) ) ;
#6966=CARTESIAN_POINT ( 'NONE',  ( -41.61668529618729195, 48.00000000000000711, 50.19614130198706192 ) ) ;
#6973=MECHANICAL_DESIGN_GEOMETRIC_PRESENTATION_REPRESENTATION('',(#67291),#20834);
#6975=EDGE_LOOP ( 'NONE', ( #24585, #60326 ) ) ;
#6990=SURFACE_STYLE_USAGE ( .BOTH. , #91650 ) ;
#6991=( GEOMETRIC_REPRESENTATION_CONTEXT ( 3 ) GLOBAL_UNCERTAINTY_ASSIGNED_CONTEXT ( ( #16056 ) ) GLOBAL_UNIT_ASSIGNED_CONTEXT ( ( #76106, #93902, #85273 ) ) REPRESENTATION_CONTEXT ( 'NONE', 'WORKASPACE' ) );
#6995=CARTESIAN_POINT ( 'NONE',  ( 5.411617511166468830, 41.81753644224158251, -58.91471485095114247 ) ) ;
#7003=CARTESIAN_POINT ( 'NONE',  ( -19.38698831337739747, 49.93019163697051965, 61.03974490994094282 ) ) ;
#7009=CARTESIAN_POINT ( 'NONE',  ( 12.49999999999999822, -4.999999999999999112, -9.904958390907012244 ) ) ;
#7013=COLOUR_RGB ( '', 0.66274510, 0.83137255, 0.94901961) ;
#7028=CARTESIAN_POINT ( 'NONE',  ( -17.49999999999996803, 45.90000000000000568, 64.09953197957064219 ) ) ;
#7032=CARTESIAN_POINT ( 'NONE',  ( 55.59873597034290071, 48.00000000000000711, -34.06437516161191326 ) ) ;
#7039=CARTESIAN_POINT ( 'NONE',  ( 7.499997280422757484, -2.963001255694796665, -20.99866594763298266 ) ) ;
#7049=CARTESIAN_POINT ( 'NONE',  ( 7.500000000000005329, 40.28748004600710431, -68.91429205818927528 ) ) ;
#7055=CARTESIAN_POINT ( 'NONE',  ( -18.91772294278450772, 48.00000000000000000, 62.18609455171461065 ) ) ;
#7058=CARTESIAN_POINT ( 'NONE',  ( -5.096247963242958257, -4.999999999999998224, -73.00359695307524532 ) ) ;
#7074=CARTESIAN_POINT ( 'NONE',  ( -14.88296169672398328, 41.91403674972022486, -82.91973998541202207 ) ) ;
#7077=CARTESIAN_POINT ( 'NONE',  ( 10.48543666094731996, -5.000000000000002665, -78.95657223723277696 ) ) ;
#7121=( NAMED_UNIT ( * ) PLANE_ANGLE_UNIT ( ) SI_UNIT ( $, .RADIAN. ) );
#7126=EDGE_CURVE ( 'NONE', #51961, #69383, #99452, .T. ) ;
#7155=CARTESIAN_POINT ( 'NONE',  ( 7.096116585776479191, 40.56175638390114813, -70.95279415343941309 ) ) ;
#7163=CARTESIAN_POINT ( 'NONE',  ( -59.16624074119484078, 50.00000000000000000, 21.79082393248474503 ) ) ;
#7174=CARTESIAN_POINT ( 'NONE',  ( 7.425374080001780008, 41.07993796427307842, -59.67056350572800483 ) ) ;
#7236=DIRECTION ( 'NONE',  ( -0.000000000000000000, 1.000000000000000000, -0.000000000000000000 ) ) ;
#7244=VERTEX_POINT ( 'NONE', #26883 ) ;
#7260=ORIENTED_EDGE ( 'NONE', *, *, #92514, .F. ) ;
#7271=FILL_AREA_STYLE ('',( #65529 ) ) ;
#7280=EDGE_CURVE ( 'NONE', #71976, #78701, #27296, .T. ) ;
#7284=CARTESIAN_POINT ( 'NONE',  ( 50.94745919686198476, 50.00000000000000000, -37.05882352941176094 ) ) ;
#7287=EDGE_CURVE ( 'NONE', #56205, #86892, #59558, .T. ) ;
#7290=ORIENTED_EDGE ( 'NONE', *, *, #1980, .F. ) ;
#7299=CARTESIAN_POINT ( 'NONE',  ( -10.00000000000000000, -5.000000000000000000, -2.617993873628155832 ) ) ;
#7314=STYLED_ITEM ( 'NONE', ( #97087 ), #21210 ) ;
#7328=CARTESIAN_POINT ( 'NONE',  ( 17.49999999999542410, 50.03176226080812228, 60.82931034966990325 ) ) ;
#7332=( NAMED_UNIT ( * ) SI_UNIT ( $, .STERADIAN. ) SOLID_ANGLE_UNIT ( ) );
#7333=( BOUNDED_CURVE ( )  B_SPLINE_CURVE ( 2, ( #69248, #53054, #73721 ),
 .UNSPECIFIED., .F., .F. ) 
 B_SPLINE_CURVE_WITH_KNOTS ( ( 3, 3 ),
 ( 0.000000000000000000, 1.000000000000000000 ),
 .UNSPECIFIED. ) 
 CURVE ( )  GEOMETRIC_REPRESENTATION_ITEM ( )  RATIONAL_B_SPLINE_CURVE ( ( 1.428571428571429269, 1.428571428571436375, 1.000000000000000000 ) ) 
 REPRESENTATION_ITEM ( '' )  );
#7341=CARTESIAN_POINT ( 'NONE',  ( -7.701342750610986165, -4.999999999998212985, -18.36411236461060881 ) ) ;
#7362=EDGE_LOOP ( 'NONE', ( #53550, #7290, #44171, #21213 ) ) ;
#7363=CARTESIAN_POINT ( 'NONE',  ( -56.06936961864204250, 48.00000000000000000, -33.41736086623469504 ) ) ;
#7375=CARTESIAN_POINT ( 'NONE',  ( -2.245730763533316132, 18.64284798592927217, 38.36507033181739246 ) ) ;
#7389=CARTESIAN_POINT ( 'NONE',  ( 6.645514545840788934, 41.91298724924220664, -59.84148600294046361 ) ) ;
#7392=STYLED_ITEM ( 'NONE', ( #16237 ), #52538 ) ;
#7396=ORIENTED_EDGE ( 'NONE', *, *, #37314, .F. ) ;
#7399=CARTESIAN_POINT ( 'NONE',  ( -6.581905802744468126, 41.48827110272019780, -70.61906944529594909 ) ) ;
#7415=( GEOMETRIC_REPRESENTATION_CONTEXT ( 3 ) GLOBAL_UNCERTAINTY_ASSIGNED_CONTEXT ( ( #19026 ) ) GLOBAL_UNIT_ASSIGNED_CONTEXT ( ( #30713, #31761, #87865 ) ) REPRESENTATION_CONTEXT ( 'NONE', 'WORKASPACE' ) );
#7437=CARTESIAN_POINT ( 'NONE',  ( 0.000000000000000000, -3.000000000000000000, 8.000000000000000000 ) ) ;
#7439=PRESENTATION_STYLE_ASSIGNMENT (( #63052 ) ) ;
#7441=CARTESIAN_POINT ( 'NONE',  ( -17.49999999999997513, 49.05239384892048093, 64.04602356109414529 ) ) ;
#7494=CARTESIAN_POINT ( 'NONE',  ( 1.301042606982605321E-15, -5.000000000000000000, -10.00000000000000000 ) ) ;
#7515=CARTESIAN_POINT ( 'NONE',  ( 6.249703441989621133, 41.65323758485251915, -58.70056750649388277 ) ) ;
#7533=CARTESIAN_POINT ( 'NONE',  ( 18.00050007014547759, 45.00000000000000000, 62.56698010746755756 ) ) ;
#7539=CARTESIAN_POINT ( 'NONE',  ( -6.440906041033002793, -5.000000000000000000, -15.34892902906475420 ) ) ;
#7550=ADVANCED_FACE ( 'NONE', ( #59089 ), #45180, .T. ) ;
#7551=CARTESIAN_POINT ( 'NONE',  ( 65.20309930813584742, 48.00000000000002132, 0.3961530819213638921 ) ) ;
#7571=CARTESIAN_POINT ( 'NONE',  ( -65.26738680892601963, 40.83906611473079806, 0.8120011907944293394 ) ) ;
#7575=CARTESIAN_POINT ( 'NONE',  ( -17.50000000000202860, 49.80818831227223598, 62.14041309008910474 ) ) ;
#7589=CARTESIAN_POINT ( 'NONE',  ( -19.79304829293588952, 41.85759246273495648, -79.99079158153486446 ) ) ;
#7593=CARTESIAN_POINT ( 'NONE',  ( -13.36289530936645953, 41.70153063405961547, -78.00930164889606999 ) ) ;
#7596=CARTESIAN_POINT ( 'NONE',  ( 8.737863884122765157, -5.000000000000000888, -79.96381019769943066 ) ) ;
#7610=CARTESIAN_POINT ( 'NONE',  ( 2.370139314397876618, -5.000000000000000000, -97.83572313320559033 ) ) ;
#7611=DIRECTION ( 'NONE',  ( 0.000000000000000000, 0.000000000000000000, 1.000000000000000000 ) ) ;
#7617=CARTESIAN_POINT ( 'NONE',  ( 20.10874767230411209, 38.95312827010130974, 60.47886685784197169 ) ) ;
#7626=FILL_AREA_STYLE ('',( #99295 ) ) ;
#7667=ORIENTED_EDGE ( 'NONE', *, *, #93922, .T. ) ;
#7674=CARTESIAN_POINT ( 'NONE',  ( 6.763062899848484300, 41.48827110285979813, -70.48955655334555104 ) ) ;
#7678=B_SPLINE_CURVE_WITH_KNOTS ( 'NONE', 3,
 ( #28389, #87136, #93628, #12156 ),
 .UNSPECIFIED., .F., .F.,
 ( 4, 4 ),
 ( 0.000000000000000000, 1.000000000000000000 ),
 .UNSPECIFIED. ) ;
#7685=CARTESIAN_POINT ( 'NONE',  ( -56.90650429242394637, 38.95383793067070854, -28.99688671941349583 ) ) ;
#7701=CARTESIAN_POINT ( 'NONE',  ( 37.29474511894786559, 18.64284798592629500, -9.274907802241656896 ) ) ;
#7730=CARTESIAN_POINT ( 'NONE',  ( 60.62677696759038781, 40.83906611471993386, 24.18439664994441074 ) ) ;
#7776=CARTESIAN_POINT ( 'NONE',  ( -7.125691916582566954, 41.67430808341742932, -69.26730091582949456 ) ) ;
#7807=CARTESIAN_POINT ( 'NONE',  ( 12.50000000000000711, 27.24691889344157403, -44.79063170920220927 ) ) ;
#7813=CARTESIAN_POINT ( 'NONE',  ( -39.08667504521157809, 48.00000000000000000, -56.76470588235294912 ) ) ;
#7821=CARTESIAN_POINT ( 'NONE',  ( 17.50000000000003197, 48.99424772499676806, 64.05279666586571352 ) ) ;
#7832=CARTESIAN_POINT ( 'NONE',  ( 8.922269033012840467, -5.000000000000000000, 5.219866590718108768 ) ) ;
#7850=CARTESIAN_POINT ( 'NONE',  ( 6.542885630808934927, 41.77241054322398384, -59.03854290128418825 ) ) ;
#7861=CARTESIAN_POINT ( 'NONE',  ( 17.49999999999238298, 50.03761058181454047, 61.36442103422039196 ) ) ;
#7869=CARTESIAN_POINT ( 'NONE',  ( 5.175365594622103771, 41.93912328290134184, -69.86374199123662265 ) ) ;
#7870=CARTESIAN_POINT ( 'NONE',  ( -7.092880029132369479, -4.030086327916265532, -17.38322132480382720 ) ) ;
#7896=CARTESIAN_POINT ( 'NONE',  ( 51.78317192861597107, 50.00000000002003731, 39.73656039222791492 ) ) ;
#7924=CARTESIAN_POINT ( 'NONE',  ( 23.79146510329413644, 41.63428640024510230, -74.58727699534063049 ) ) ;
#7937=FILL_AREA_STYLE_COLOUR ( '', #15023 ) ;
#7971=CARTESIAN_POINT ( 'NONE',  ( 52.56491209535275999, 39.42572890907100458, -38.23519342730396176 ) ) ;
#7977=CARTESIAN_POINT ( 'NONE',  ( 0.000000000000000000, -3.000000000000000000, 8.000000000000000000 ) ) ;
#7981=EDGE_CURVE ( 'NONE', #25938, #57232, #15789, .T. ) ;
#7990=CIRCLE ( 'NONE', #45895, 15.00000000000000178 ) ;
#7996=CARTESIAN_POINT ( 'NONE',  ( 7.500000000000003553, 18.65452285268503729, -40.72535638072048414 ) ) ;
#8057=CARTESIAN_POINT ( 'NONE',  ( 6.568714581474836223, 41.61374591157808567, -58.74117443926016335 ) ) ;
#8102=CARTESIAN_POINT ( 'NONE',  ( -46.86302342948793864, 41.03834671688476732, -46.07399435196477100 ) ) ;
#8112=CARTESIAN_POINT ( 'NONE',  ( 6.516354785991091835E-11, 40.83842593836580903, 65.00000000086684793 ) ) ;
#8117=CARTESIAN_POINT ( 'NONE',  ( -17.50000000000100897, 49.16280683614362346, 62.52714020843506404 ) ) ;
#8132=CARTESIAN_POINT ( 'NONE',  ( -30.67017305325112275, 40.99855314031348286, -65.37930749121261442 ) ) ;
#8142=CARTESIAN_POINT ( 'NONE',  ( -6.145467200813103936, -5.000000000008177459, -92.99666842290147883 ) ) ;
#8143=CARTESIAN_POINT ( 'NONE',  ( -6.464976092152494580, 41.32132943617850174, -58.37832475197549797 ) ) ;
#8159=CARTESIAN_POINT ( 'NONE',  ( 4.692671595817627939, -5.000000000000000000, -97.18017958146204194 ) ) ;
#8160=DIRECTION ( 'NONE',  ( -1.000000000000000000, -0.000000000000000000, -0.000000000000000000 ) ) ;
#8197=CARTESIAN_POINT ( 'NONE',  ( 4.852941176470592310, -3.000000000000002665, -70.80672828634229177 ) ) ;
#8200=CARTESIAN_POINT ( 'NONE',  ( -7.190574406385736417, 41.61619605049727255, -59.53992226565166135 ) ) ;
#8223=CARTESIAN_POINT ( 'NONE',  ( 6.930184121914609641, 41.27136526567599617, -70.62329949176377397 ) ) ;
#8259=SURFACE_STYLE_USAGE ( .BOTH. , #41172 ) ;
#8268=EDGE_CURVE ( 'NONE', #60267, #86235, #49205, .T. ) ;
#8307=SURFACE_STYLE_USAGE ( .BOTH. , #82190 ) ;
#8312=CARTESIAN_POINT ( 'NONE',  ( -7.044111875035700798, 41.04202977231933147, -70.72791807316478696 ) ) ;
#8326=LINE ( 'NONE', #41760, #72760 ) ;
#8346=CARTESIAN_POINT ( 'NONE',  ( 12.50000000000000355, 41.59226156894002457, -76.70843802411151557 ) ) ;
#8360=STYLED_ITEM ( 'NONE', ( #136 ), #68626 ) ;
#8401=CARTESIAN_POINT ( 'NONE',  ( 18.95009564030317506, 49.33583170005577045, 62.02326760999128652 ) ) ;
#8408=CARTESIAN_POINT ( 'NONE',  ( 4.966176485634622217, 41.64999999999998437, -70.47555195150158625 ) ) ;
#8410=CARTESIAN_POINT ( 'NONE',  ( -5.318172249955896547, -5.000000000000039968, -15.46996282977505999 ) ) ;
#8427=UNCERTAINTY_MEASURE_WITH_UNIT (LENGTH_MEASURE( 1.000000000000000082E-05 ), #25031, 'distance_accuracy_value', 'NONE');
#8435=CARTESIAN_POINT ( 'NONE',  ( 64.91565662647984425, 48.00000000000000000, 6.815324757469506167 ) ) ;
#8448=VERTEX_POINT ( 'NONE', #105123 ) ;
#8470=CARTESIAN_POINT ( 'NONE',  ( -6.478079992187136149, 41.41225026867109449, -70.77206710307365256 ) ) ;
#8494=UNCERTAINTY_MEASURE_WITH_UNIT (LENGTH_MEASURE( 1.000000000000000082E-05 ), #12194, 'distance_accuracy_value', 'NONE');
#8499=B_SPLINE_CURVE_WITH_KNOTS ( 'NONE', 3,
 ( #14773, #5113, #78989, #6686, #5632, #62301, #29938, #22909, #38044, #40124, #88155, #96779, #95193, #80566, #87627, #54695, #29425, #70905, #103795, #14238, #105392, #21326, #62822, #63889, #22387, #87104 ),
 .UNSPECIFIED., .F., .F.,
 ( 4, 2, 2, 2, 2, 2, 1, 1, 2, 2, 2, 2, 2, 4 ),
 ( 0.000000000000000000, 0.06250000000001112999, 0.1250000000000222600, 0.2500000000000450751, 0.3750000000000678901, 0.4375000000000812683, 0.4687500000000897060, 0.4843750000000930922, 0.4921875000000922040, 0.5000000000000912603, 0.6250000000000683897, 0.7500000000000456302, 0.8750000000000227596, 1.000000000000000000 ),
 .UNSPECIFIED. ) ;
#8518=CARTESIAN_POINT ( 'NONE',  ( -12.50000000000000000, -3.000000000000000000, -8.595933841506989026 ) ) ;
#8524=EDGE_LOOP ( 'NONE', ( #62623, #49928, #10563, #77833 ) ) ;
#8532=STYLED_ITEM ( 'NONE', ( #97380 ), #6345 ) ;
#8551=ORIENTED_EDGE ( 'NONE', *, *, #16169, .T. ) ;
#8582=CARTESIAN_POINT ( 'NONE',  ( -90.56128410203886858, 42.00000000000000000, -11.85444436786843703 ) ) ;
#8591=CARTESIAN_POINT ( 'NONE',  ( 5.896197027862030815, 41.78011521630541125, -58.83937651719745787 ) ) ;
#8608=CARTESIAN_POINT ( 'NONE',  ( 18.28997961183965160, 45.00000000000000711, 62.41113724044252109 ) ) ;
#8615=CARTESIAN_POINT ( 'NONE',  ( -9.308639103300027529, -5.000000000000000888, -18.31521250230575149 ) ) ;
#8636=CARTESIAN_POINT ( 'NONE',  ( 5.499265899526156076, -3.000000000000002665, -99.22427370006747083 ) ) ;
#8651=CARTESIAN_POINT ( 'NONE',  ( -19.49736279435545327, 49.99988902982538974, 59.96655211255967544 ) ) ;
#8667=CARTESIAN_POINT ( 'NONE',  ( -33.10434277953672222, 40.69601545704099266, -62.12919646516525063 ) ) ;
#8674=CARTESIAN_POINT ( 'NONE',  ( 6.043427762771891310, -5.000000000000002665, -74.51456333905348117 ) ) ;
#8678=CARTESIAN_POINT ( 'NONE',  ( 7.500000000000005329, -5.250000000000005329, -71.71180648257555390 ) ) ;
#8684=EDGE_LOOP ( 'NONE', ( #14507, #15686, #51905, #106627 ) ) ;
#8688=CARTESIAN_POINT ( 'NONE',  ( -18.91791044776116237, 45.00000000000000711, 62.18611311450884926 ) ) ;
#8690=CARTESIAN_POINT ( 'NONE',  ( 12.98455676797003022, -5.000000000000000000, -86.33387663731812722 ) ) ;
#8696=CARTESIAN_POINT ( 'NONE',  ( -42.76627839262699382, 38.95206895324334795, 47.52996633003031235 ) ) ;
#8733=CARTESIAN_POINT ( 'NONE',  ( 7.004291983109769859, 40.56179000455576045, -71.01843131752761451 ) ) ;
#8736=( GEOMETRIC_REPRESENTATION_CONTEXT ( 3 ) GLOBAL_UNCERTAINTY_ASSIGNED_CONTEXT ( ( #19244 ) ) GLOBAL_UNIT_ASSIGNED_CONTEXT ( ( #68826, #2462, #92541 ) ) REPRESENTATION_CONTEXT ( 'NONE', 'WORKASPACE' ) );
#8752=CARTESIAN_POINT ( 'NONE',  ( 6.890281281981907924, 41.03680257675737408, -70.85895802599645776 ) ) ;
#8767=EDGE_CURVE ( 'NONE', #66436, #24664, #24593, .T. ) ;
#8768=CARTESIAN_POINT ( 'NONE',  ( -9.500000000000000000, -5.000000000000000000, -20.99851272547259384 ) ) ;
#8774=CARTESIAN_POINT ( 'NONE',  ( 7.386518197476049430, 41.27037547458987632, -59.50133886764230340 ) ) ;
#8788=FACE_OUTER_BOUND ( 'NONE', #9821, .T. ) ;
#8829=CARTESIAN_POINT ( 'NONE',  ( -17.49999999999997513, 50.00000000000000000, 100.0000000000000000 ) ) ;
#8842=CARTESIAN_POINT ( 'NONE',  ( -7.078150683205035598, 41.46400356776579343, -70.18186705553098648 ) ) ;
#8898=CARTESIAN_POINT ( 'NONE',  ( 7.500000000000000888, -3.000671055698259870, -20.99923901233272971 ) ) ;
#8903=CARTESIAN_POINT ( 'NONE',  ( -7.320805857562880270, 41.41776710089564517, -59.82972164228972645 ) ) ;
#8909=SURFACE_SIDE_STYLE ('',( #75779 ) ) ;
#8910=( BOUNDED_CURVE ( )  B_SPLINE_CURVE ( 2, ( #25173, #75274, #24116 ),
 .UNSPECIFIED., .F., .F. ) 
 B_SPLINE_CURVE_WITH_KNOTS ( ( 3, 3 ),
 ( 0.000000000000000000, 1.000000000000000000 ),
 .UNSPECIFIED. ) 
 CURVE ( )  GEOMETRIC_REPRESENTATION_ITEM ( )  RATIONAL_B_SPLINE_CURVE ( ( 1.000000000000000000, 1.857142857142858317, 1.000000000000000000 ) ) 
 REPRESENTATION_ITEM ( '' )  );
#8930=CARTESIAN_POINT ( 'NONE',  ( -5.908324243937765452, 41.91795894114439136, -59.12627178481003654 ) ) ;
#8947=VERTEX_POINT ( 'NONE', #97448 ) ;
#8986=CARTESIAN_POINT ( 'NONE',  ( 19.43279966247120072, 41.87228345916210515, -80.47899240423528511 ) ) ;
#8992=ORIENTED_EDGE ( 'NONE', *, *, #19213, .T. ) ;
#8997=CARTESIAN_POINT ( 'NONE',  ( -6.701893397842001221, 41.44328394191487774, -70.59544911652842814 ) ) ;
#9002=VERTEX_POINT ( 'NONE', #32762 ) ;
#9039=CARTESIAN_POINT ( 'NONE',  ( -6.701893397842001221, 41.44328394191487774, -70.59544911652842814 ) ) ;
#9045=CARTESIAN_POINT ( 'NONE',  ( -12.50000000000000711, -4.999999999999999112, -80.60844091781802945 ) ) ;
#9051=EDGE_LOOP ( 'NONE', ( #26158, #69384, #51202, #99964 ) ) ;
#9089=CARTESIAN_POINT ( 'NONE',  ( -6.784953749642196996, 41.67963440881483450, -59.00226708758491156 ) ) ;
#9106=CARTESIAN_POINT ( 'NONE',  ( -45.60838156032659896, 42.00000000000000000, 79.13121736029036413 ) ) ;
#9116=CARTESIAN_POINT ( 'NONE',  ( 6.492511067189948193, 41.78432740739263096, -59.03547063838887965 ) ) ;
#9131=CARTESIAN_POINT ( 'NONE',  ( 17.51085981868257591, 45.00000000000000000, 63.60668009671144318 ) ) ;
#9144=CARTESIAN_POINT ( 'NONE',  ( -18.91791044776116237, 45.90000000000000568, 62.18611311450883505 ) ) ;
#9146=CARTESIAN_POINT ( 'NONE',  ( 41.61668529618731327, 47.99999999999999289, 50.19614130198702640 ) ) ;
#9152=ORIENTED_EDGE ( 'NONE', *, *, #25446, .F. ) ;
#9169=CARTESIAN_POINT ( 'NONE',  ( -17.50000000000507683, 48.51938947813042091, 62.60970113051429564 ) ) ;
#9185=CARTESIAN_POINT ( 'NONE',  ( 52.56483885390523625, 48.00000000000000000, -38.23529411764706509 ) ) ;
#9186=CARTESIAN_POINT ( 'NONE',  ( -19.44323342421834866, 41.87186953726217098, -80.46484636551333836 ) ) ;
#9261=B_SPLINE_CURVE_WITH_KNOTS ( 'NONE', 3,
 ( #83279, #42823, #18578, #41755, #76246, #91907, #59555, #34770 ),
 .UNSPECIFIED., .F., .F.,
 ( 4, 2, 2, 4 ),
 ( 0.000000000000000000, 0.2500000000000000000, 0.5000000000000000000, 1.000000000000000000 ),
 .UNSPECIFIED. ) ;
#9281=CARTESIAN_POINT ( 'NONE',  ( -50.91589357081878120, 38.95383793066859113, 39.12903940707597883 ) ) ;
#9311=EDGE_CURVE ( 'NONE', #53673, #7244, #79963, .T. ) ;
#9333=CARTESIAN_POINT ( 'NONE',  ( 45.60838156035057978, 42.00000000000004263, -79.13121736032620390 ) ) ;
#9341=SURFACE_STYLE_FILL_AREA ( #24525 ) ;
#9360=CARTESIAN_POINT ( 'NONE',  ( -7.398496323958707599, 40.00000000002496137, -70.41867143398266649 ) ) ;
#9391=CARTESIAN_POINT ( 'NONE',  ( 12.50000000000000533, 24.98774108567306840, -42.39486677989071950 ) ) ;
#9402=CARTESIAN_POINT ( 'NONE',  ( 63.67138272020815037, 38.95383793066860534, -8.334564508068659450 ) ) ;
#9403=EDGE_CURVE ( 'NONE', #105843, #72225, #88944, .T. ) ;
#9406=EDGE_CURVE ( 'NONE', #37873, #93842, #74802, .T. ) ;
#9462=CARTESIAN_POINT ( 'NONE',  ( -5.314078508931081579, -5.000000000000359712, -15.45392136113532366 ) ) ;
#9485=CARTESIAN_POINT ( 'NONE',  ( 23.38163988262877879, 50.00000000002003731, 60.94087333794557537 ) ) ;
#9516=PRESENTATION_STYLE_ASSIGNMENT (( #1418 ) ) ;
#9528=CARTESIAN_POINT ( 'NONE',  ( 3.140974613990258568, 50.00000000000000000, -96.68767211932436112 ) ) ;
#9542=( BOUNDED_CURVE ( )  B_SPLINE_CURVE ( 3, ( #34268, #74677, #100026, #759, #9402, #41263, #73616, #105983, #33726, #56898, #33198, #17005, #90348, #82787 ),
 .UNSPECIFIED., .F., .F. ) 
 B_SPLINE_CURVE_WITH_KNOTS ( ( 4, 2, 2, 2, 2, 2, 4 ),
 ( 0.000000000000000000, 0.05368345394220581934, 0.1429467631537782168, 0.2322100723653506005, 0.3214733815769227343, 0.4107366907884949514, 0.5000000000031382674 ),
 .UNSPECIFIED. ) 
 CURVE ( )  GEOMETRIC_REPRESENTATION_ITEM ( )  RATIONAL_B_SPLINE_CURVE ( ( 1.420262811277154924, 1.420262811277154924, 1.420262811277154924, 1.420262811277154924, 1.420262811277154924, 1.420262811277154924, 1.420262811277154924, 1.420262811277154924, 1.420262811277154924, 1.420262811277154924, 1.420262811277154924, 1.420262811277154924, 1.420262811277154924, 1.420262811277154924 ) ) 
 REPRESENTATION_ITEM ( '' )  );
#9561=CARTESIAN_POINT ( 'NONE',  ( -5.075741750048029743, -4.332638003024074536, -17.09621982684887698 ) ) ;
#9569=SURFACE_SIDE_STYLE ('',( #30712 ) ) ;
#9573=CARTESIAN_POINT ( 'NONE',  ( -19.44294908207561434, 50.00000000000000000, 59.98229726226637126 ) ) ;
#9580=LINE ( 'NONE', #66234, #78919 ) ;
#9611=CARTESIAN_POINT ( 'NONE',  ( -18.91791044776116237, 46.00000000000000000, 62.18611311450884926 ) ) ;
#9616=CARTESIAN_POINT ( 'NONE',  ( -6.563169324595991228, 41.73030616478934007, -58.95245868007680201 ) ) ;
#9623=B_SPLINE_CURVE_WITH_KNOTS ( 'NONE', 3,
 ( #51793, #87240, #79130, #5255 ),
 .UNSPECIFIED., .F., .F.,
 ( 4, 4 ),
 ( 0.000000000000000000, 1.000000000000000000 ),
 .UNSPECIFIED. ) ;
#9635=( NAMED_UNIT ( * ) SI_UNIT ( $, .STERADIAN. ) SOLID_ANGLE_UNIT ( ) );
#9643=CARTESIAN_POINT ( 'NONE',  ( 6.390966725705288454, 41.59892189792125095, -58.65495604877497726 ) ) ;
#9644=CARTESIAN_POINT ( 'NONE',  ( -5.500000000000006217, 42.00000000000000000, -62.89165061483231511 ) ) ;
#9647=EDGE_LOOP ( 'NONE', ( #53158, #84044, #103854, #20826 ) ) ;
#9653=CARTESIAN_POINT ( 'NONE',  ( -2.617478843592807358, -3.000000000000003109, -75.26027323331685182 ) ) ;
#9658=CARTESIAN_POINT ( 'NONE',  ( 17.53980351349540356, 45.00000000000001421, 63.37883192130072985 ) ) ;
#9664=CARTESIAN_POINT ( 'NONE',  ( -8.786332869125764944, -4.999999999999999112, -16.86266621361376750 ) ) ;
#9687=CARTESIAN_POINT ( 'NONE',  ( -11.78124729767428924, -3.000000000000002665, -94.38183245065363280 ) ) ;
#9702=ORIENTED_EDGE ( 'NONE', *, *, #9406, .F. ) ;
#9705=CARTESIAN_POINT ( 'NONE',  ( -18.92590207683343806, 49.07586612980275476, 62.10725160223359609 ) ) ;
#9716=CARTESIAN_POINT ( 'NONE',  ( -16.11469797371095325, 41.97267161074977793, -84.98552174202809795 ) ) ;
#9732=VERTEX_POINT ( 'NONE', #16571 ) ;
#9779=ORIENTED_EDGE ( 'NONE', *, *, #10884, .T. ) ;
#9784=CARTESIAN_POINT ( 'NONE',  ( -7.040774328009895555, 41.35742559143615438, -58.68913211047704692 ) ) ;
#9802=PRESENTATION_STYLE_ASSIGNMENT (( #11936 ) ) ;
#9819=CARTESIAN_POINT ( 'NONE',  ( -7.499999902153906106, -3.000145757760796617, -20.99858933621342061 ) ) ;
#9821=EDGE_LOOP ( 'NONE', ( #2000, #92540, #24125 ) ) ;
#9845=CARTESIAN_POINT ( 'NONE',  ( -7.500000000000004441, 42.83333333333329307, -71.71180648257555390 ) ) ;
#9863=EDGE_CURVE ( 'NONE', #78368, #105843, #50149, .T. ) ;
#9870=CARTESIAN_POINT ( 'NONE',  ( 11.85444436799972934, 42.00000000000000000, 90.56128410203886858 ) ) ;
#9881=CARTESIAN_POINT ( 'NONE',  ( -2.958006552684906865, 40.83778438954344381, 65.00031278382145672 ) ) ;
#9884=CARTESIAN_POINT ( 'NONE',  ( 12.50000000000000355, 41.59226156894002457, -76.70843802411151557 ) ) ;
#9887=ORIENTED_EDGE ( 'NONE', *, *, #36515, .F. ) ;
#9901=CARTESIAN_POINT ( 'NONE',  ( -12.13034742782427955, 48.00000000000000000, -93.82352941176471006 ) ) ;
#9903=CARTESIAN_POINT ( 'NONE',  ( -7.319239792064268890, 40.56016599439953296, -70.61402026096378393 ) ) ;
#9918=CARTESIAN_POINT ( 'NONE',  ( -5.500000000000007994, 42.00000000000000000, -68.91429205818155879 ) ) ;
#9925=( NAMED_UNIT ( * ) SI_UNIT ( $, .STERADIAN. ) SOLID_ANGLE_UNIT ( ) );
#9940=CARTESIAN_POINT ( 'NONE',  ( 12.50000000000000000, 29.87326214413186776, -47.66873073394299354 ) ) ;
#9953=CARTESIAN_POINT ( 'NONE',  ( 17.50000000000002842, 49.00315172309048961, 64.05179859717361524 ) ) ;
#9987=COLOUR_RGB ( '', 0.40784314, 0.44705882, 0.49803922) ;
#9996=FACE_OUTER_BOUND ( 'NONE', #97474, .T. ) ;
#10008=CARTESIAN_POINT ( 'NONE',  ( -8.056626385452181793, -4.999999999999978684, -15.81257860883812327 ) ) ;
#10010=CARTESIAN_POINT ( 'NONE',  ( 17.51469545665185024, 50.00000000000001421, 63.29293518440665167 ) ) ;
#10014=PRESENTATION_STYLE_ASSIGNMENT (( #817 ) ) ;
#10034=CARTESIAN_POINT ( 'NONE',  ( -5.388845162059435978, 41.63012960719941447, -58.67906650638375510 ) ) ;
#10046=CARTESIAN_POINT ( 'NONE',  ( -30.95568101992225252, 18.64284798593066483, 22.77427805267372563 ) ) ;
#10076=CARTESIAN_POINT ( 'NONE',  ( -2.617478844990396514, 50.00000000000001421, -94.73972676610910071 ) ) ;
#10135=ORIENTED_EDGE ( 'NONE', *, *, #39007, .F. ) ;
#10160=CARTESIAN_POINT ( 'NONE',  ( -6.943035977205679110, 41.50417750172036335, -58.81491712266881677 ) ) ;
#10167=CARTESIAN_POINT ( 'NONE',  ( 12.50000000000000000, 14.91295971516869301, -32.73279170529961846 ) ) ;
#10175=CARTESIAN_POINT ( 'NONE',  ( -79.13121736037271603, 42.00000000000000000, 45.60838156032633606 ) ) ;
#10187=CARTESIAN_POINT ( 'NONE',  ( -7.500000000000007105, 42.00000000000000711, -58.69229087761262065 ) ) ;
#10197=CARTESIAN_POINT ( 'NONE',  ( -9.739726766683153514, -3.000000000000002665, -82.38252115640719353 ) ) ;
#10207=B_SPLINE_CURVE_WITH_KNOTS ( 'NONE', 3,
 ( #22776, #66383, #76064, #84175, #25985, #99814, #34059, #17857, #3258, #26508 ),
 .UNSPECIFIED., .F., .F.,
 ( 4, 2, 2, 2, 4 ),
 ( 0.000000000000000000, 0.5000000000000000000, 0.7500000000000000000, 0.8750000000000000000, 1.000000000000000000 ),
 .UNSPECIFIED. ) ;
#10232=( GEOMETRIC_REPRESENTATION_CONTEXT ( 3 ) GLOBAL_UNCERTAINTY_ASSIGNED_CONTEXT ( ( #3831 ) ) GLOBAL_UNIT_ASSIGNED_CONTEXT ( ( #29524, #6243, #22487 ) ) REPRESENTATION_CONTEXT ( 'NONE', 'WORKASPACE' ) );
#10259=CARTESIAN_POINT ( 'NONE',  ( -6.542885568110277106, 41.77240995323538897, -59.03854211387476880 ) ) ;
#10266=CARTESIAN_POINT ( 'NONE',  ( -8.737863884121843228, -3.000000000000002665, -79.96381019768948306 ) ) ;
#10295=( NAMED_UNIT ( * ) SI_UNIT ( $, .STERADIAN. ) SOLID_ANGLE_UNIT ( ) );
#10297=CARTESIAN_POINT ( 'NONE',  ( 7.225703553013920200, -4.999999999999999112, -73.19314196553180807 ) ) ;
#10307=SURFACE_STYLE_USAGE ( .BOTH. , #51830 ) ;
#10322=CARTESIAN_POINT ( 'NONE',  ( -7.237253929247286166, 41.05631633789147372, -58.62830998736340149 ) ) ;
#10324=CARTESIAN_POINT ( 'NONE',  ( -12.50000000000000000, -3.000000000000003109, -14.34180675897363599 ) ) ;
#10341=FACE_OUTER_BOUND ( 'NONE', #83340, .T. ) ;
#10375=MECHANICAL_DESIGN_GEOMETRIC_PRESENTATION_REPRESENTATION('',(#56877),#6991);
#10406=SURFACE_STYLE_USAGE ( .BOTH. , #43844 ) ;
#10415=CARTESIAN_POINT ( 'NONE',  ( 51.81797853811001886, 40.83872170108235622, 39.69809105071564659 ) ) ;
#10418=CARTESIAN_POINT ( 'NONE',  ( 14.91270732344407257, 41.98564553269472555, -86.62216337287246404 ) ) ;
#10425=CARTESIAN_POINT ( 'NONE',  ( 1.735558044533036748, 41.99999999999999289, -69.74083754112251654 ) ) ;
#10431=CARTESIAN_POINT ( 'NONE',  ( -1.570796324980112679, 50.00000000000000000, -97.00000000000000000 ) ) ;
#10432=CARTESIAN_POINT ( 'NONE',  ( -12.44829945131329474, -3.980163019925683443, -13.20820160251541431 ) ) ;
#10446=CARTESIAN_POINT ( 'NONE',  ( -6.145999768515837403, -5.000000000000000000, 7.996316163935361487 ) ) ;
#10457=( GEOMETRIC_REPRESENTATION_CONTEXT ( 3 ) GLOBAL_UNCERTAINTY_ASSIGNED_CONTEXT ( ( #66742 ) ) GLOBAL_UNIT_ASSIGNED_CONTEXT ( ( #64712, #2079, #11767 ) ) REPRESENTATION_CONTEXT ( 'NONE', 'WORKASPACE' ) );
#10469=CARTESIAN_POINT ( 'NONE',  ( -18.26456092131584796, 45.00000000000001421, 62.42260643610311632 ) ) ;
#10475=CARTESIAN_POINT ( 'NONE',  ( 5.420470438621123321, 41.88321586334136981, -59.04137885805280916 ) ) ;
#10483=( BOUNDED_SURFACE ( )  B_SPLINE_SURFACE ( 2, 3, ( 
 ( #6132, #71943, #6668, #46085, #70883, #30448, #55212, #22890 ),
 ( #96236, #103255, #78966, #29401, #104846, #13156, #61756, #96758 ),
 ( #62283, #4558, #71399, #69824, #87610, #88137, #55729, #95173 ) ),
 .UNSPECIFIED., .F., .F., .F. ) 
 B_SPLINE_SURFACE_WITH_KNOTS ( ( 3, 3 ),
 ( 4, 2, 2, 4 ),
 ( 0.000000000000000000, 1.000000000000000000 ),
 ( -0.05863181436295197141, -0.05487404235502676975, -0.04584008019048942117, -0.04405802166693190830 ),
 .UNSPECIFIED. ) 
 GEOMETRIC_REPRESENTATION_ITEM ( )  RATIONAL_B_SPLINE_SURFACE ( (
 ( 1.000000000000000000, 1.000000000000000000, 1.000000000000000000, 1.000000000000000000, 1.000000000000000000, 1.000000000000000000, 1.000000000000000000, 1.000000000000000000),
 ( 1.857142857142858317, 1.857142857142858317, 1.857142857142858317, 1.857142857142858317, 1.857142857142858317, 1.857142857142858317, 1.857142857142858317, 1.857142857142858317),
 ( 1.000000000000000000, 1.000000000000000000, 1.000000000000000000, 1.000000000000000000, 1.000000000000000000, 1.000000000000000000, 1.000000000000000000, 1.000000000000000000) ) ) 
 REPRESENTATION_ITEM ( '' )  SURFACE ( )  );
#10506=ORIENTED_EDGE ( 'NONE', *, *, #52543, .T. ) ;
#10522=CARTESIAN_POINT ( 'NONE',  ( -51.78317192862404994, 48.00000000000000000, 39.73656039225668479 ) ) ;
#10537=CARTESIAN_POINT ( 'NONE',  ( 17.78133731104211535, 50.00000000000002132, 62.21716898123242601 ) ) ;
#10547=CARTESIAN_POINT ( 'NONE',  ( -6.106896958092910666, -4.373166921188805567, -16.80698729315730944 ) ) ;
#10557=CARTESIAN_POINT ( 'NONE',  ( 6.403347876734715172, 41.95607664916837365, -69.22843809692237471 ) ) ;
#10558=CARTESIAN_POINT ( 'NONE',  ( -60.66923414622394262, 50.00000000000000000, 17.93278245653412384 ) ) ;
#10563=ORIENTED_EDGE ( 'NONE', *, *, #26243, .T. ) ;
#10571=CARTESIAN_POINT ( 'NONE',  ( -35.39685905337628213, 18.64284798593103787, 14.96610495029052323 ) ) ;
#10584=CARTESIAN_POINT ( 'NONE',  ( 31.91296609491446645, 40.84410790408901448, -63.71736666452449072 ) ) ;
#10588=EDGE_LOOP ( 'NONE', ( #20571, #101809, #97698, #46960, #13358, #103817 ) ) ;
#10599=CARTESIAN_POINT ( 'NONE',  ( 6.043427762771891310, 50.00000000000000000, -95.48543666094653304 ) ) ;
#10639=CARTESIAN_POINT ( 'NONE',  ( 14.91270732344407257, 41.98564553269472555, -86.62216337287246404 ) ) ;
#10662=CARTESIAN_POINT ( 'NONE',  ( 0.000000000000000000, 50.00000000000000000, -97.00000000000000000 ) ) ;
#10666=ORIENTED_EDGE ( 'NONE', *, *, #24537, .T. ) ;
#10685=VERTEX_POINT ( 'NONE', #88613 ) ;
#10691=EDGE_CURVE ( 'NONE', #69383, #14419, #4526, .T. ) ;
#10700=CARTESIAN_POINT ( 'NONE',  ( 55.65414010180120385, 42.00000000000000000, -72.41885610122511707 ) ) ;
#10707=CARTESIAN_POINT ( 'NONE',  ( 6.970005868343639222, 41.38563980255786845, -58.64823803489037601 ) ) ;
#10709=CARTESIAN_POINT ( 'NONE',  ( -7.500000000000007105, 40.00000000000000000, -58.09827136975972905 ) ) ;
#10718=CARTESIAN_POINT ( 'NONE',  ( -4.651132217449170270, -5.000000000000000000, -15.66661053588738106 ) ) ;
#10728=AXIS2_PLACEMENT_3D ( 'NONE', #14983, #57033, #47878 ) ;
#10733=CARTESIAN_POINT ( 'NONE',  ( -12.11400133237649968, -4.683782139512427278, -76.82602898264141800 ) ) ;
#10740=ORIENTED_EDGE ( 'NONE', *, *, #96302, .T. ) ;
#10765=CARTESIAN_POINT ( 'NONE',  ( -17.49999999999998579, 51.30660076971290096, 62.83706383106828497 ) ) ;
#10776=CARTESIAN_POINT ( 'NONE',  ( -6.338673264423879239, 41.81695718870634693, -59.02782128990620691 ) ) ;
#10783=CARTESIAN_POINT ( 'NONE',  ( 1.308996937480704670, -3.000000000000002665, -95.00000000000000000 ) ) ;
#10791=CARTESIAN_POINT ( 'NONE',  ( 7.255520619061520016, -4.332661967062336750, 16.69105336089074854 ) ) ;
#10796=STYLED_ITEM ( 'NONE', ( #37067 ), #75546 ) ;
#10813=CARTESIAN_POINT ( 'NONE',  ( 14.81716630709848737, 41.99561238121396656, -87.50450243860541377 ) ) ;
#10822=CARTESIAN_POINT ( 'NONE',  ( -11.16469478931291448, -4.978653580250081312, -12.57749972225050072 ) ) ;
#10827=CARTESIAN_POINT ( 'NONE',  ( 13.88435755492751511, 42.00000000000000000, -90.88030988993200765 ) ) ;
#10831=EDGE_CURVE ( 'NONE', #71976, #83228, #94128, .T. ) ;
#10840=CARTESIAN_POINT ( 'NONE',  ( -7.341136682164572491, 41.28570584283517064, -59.23704219074569721 ) ) ;
#10841=CARTESIAN_POINT ( 'NONE',  ( 6.731385056190076099, 41.26098032358547840, -70.78618130126719166 ) ) ;
#10857=CARTESIAN_POINT ( 'NONE',  ( -1.715570313355245569, -4.332661967060489339, -17.83376356531591256 ) ) ;
#10859=CARTESIAN_POINT ( 'NONE',  ( 6.907083959255991168, 41.55068448857264229, -58.85924345847777062 ) ) ;
#10862=CARTESIAN_POINT ( 'NONE',  ( -10.48543666094732352, -5.000000000000002665, -78.95657223722187723 ) ) ;
#10884=EDGE_CURVE ( 'NONE', #58075, #71976, #50363, .T. ) ;
#10885=CARTESIAN_POINT ( 'NONE',  ( 23.07257312861869281, 18.64284798592816017, 30.73399254005308734 ) ) ;
#10906=CARTESIAN_POINT ( 'NONE',  ( 19.50000000000171596, 49.99999999999931788, 59.64162155654628350 ) ) ;
#10907=MECHANICAL_DESIGN_GEOMETRIC_PRESENTATION_REPRESENTATION('',(#57422),#76369);
#10924=CARTESIAN_POINT ( 'NONE',  ( 90.56128410203886858, 42.00000000000000000, 11.85444436786826472 ) ) ;
#10931=CARTESIAN_POINT ( 'NONE',  ( -64.56213072485851967, 40.83885790042619846, -8.095562774589749822 ) ) ;
#10940=CARTESIAN_POINT ( 'NONE',  ( -1.966965783804975887, 41.99999999999999289, -67.70628254661242806 ) ) ;
#10949=CARTESIAN_POINT ( 'NONE',  ( 11.99999999999999467, 50.00000000000000000, -83.42920367501479006 ) ) ;
#10953=UNCERTAINTY_MEASURE_WITH_UNIT (LENGTH_MEASURE( 1.000000000000000082E-05 ), #79380, 'distance_accuracy_value', 'NONE');
#10964=CARTESIAN_POINT ( 'NONE',  ( -9.739726766683149961, 47.99999999999999289, -87.61747884359279226 ) ) ;
#10981=CARTESIAN_POINT ( 'NONE',  ( -6.855072974175857148, 40.29457745454482875, -71.16068772830431044 ) ) ;
#11013=CARTESIAN_POINT ( 'NONE',  ( -34.46463798447544491, 42.67666558786937969, -63.11895629106728478 ) ) ;
#11022=SURFACE_STYLE_USAGE ( .BOTH. , #51492 ) ;
#11028=CARTESIAN_POINT ( 'NONE',  ( -5.420469775605654128, 41.88321586335170821, -59.04137891894603030 ) ) ;
#11029=CARTESIAN_POINT ( 'NONE',  ( 11.82318485997968160, -4.853296004839451783, -12.56016920883609167 ) ) ;
#11036=CARTESIAN_POINT ( 'NONE',  ( -11.39884040742384919, -4.333298119783878910, 13.82668420665306819 ) ) ;
#11044=CARTESIAN_POINT ( 'NONE',  ( 56.06936961865346802, 48.00000000000000000, -33.41736086621895652 ) ) ;
#11064=CARTESIAN_POINT ( 'NONE',  ( -1.841875822471433519E-14, -3.000000000000002665, -70.00227127314062159 ) ) ;
#11078=CARTESIAN_POINT ( 'NONE',  ( 5.041270396327364622, 41.82074884801023984, -70.25592674792672199 ) ) ;
#11080=CARTESIAN_POINT ( 'NONE',  ( -56.06936961859863544, 49.99999999999999289, -33.41736086620520751 ) ) ;
#11083=ORIENTED_EDGE ( 'NONE', *, *, #22608, .T. ) ;
#11091=EDGE_LOOP ( 'NONE', ( #53599, #100785, #14060, #30145, #103936 ) ) ;
#11121=CARTESIAN_POINT ( 'NONE',  ( 9.739726766105679445, 49.99999999999999289, -82.38252115500968387 ) ) ;
#11158=ADVANCED_FACE ( 'NONE', ( #45778 ), #37729, .T. ) ;
#11182=CARTESIAN_POINT ( 'NONE',  ( -4.045830998955862512, 50.00000000000000711, -97.52795967580351544 ) ) ;
#11187=CARTESIAN_POINT ( 'NONE',  ( 9.610124387788696154, 50.00000000000001421, -92.36062461489224518 ) ) ;
#11202=CARTESIAN_POINT ( 'NONE',  ( -6.965116046117188375, 41.61856606226407962, -70.00485699691061825 ) ) ;
#11207=CARTESIAN_POINT ( 'NONE',  ( -5.658903634044489372, 41.71506109579434707, -58.75004022056472053 ) ) ;
#11232=CARTESIAN_POINT ( 'NONE',  ( 33.52312678243841759, 18.64316884716171785, -19.32152200345659665 ) ) ;
#11239=CARTESIAN_POINT ( 'NONE',  ( 6.870855349944958057, 41.24230146623948912, -58.43742520720547162 ) ) ;
#11240=CARTESIAN_POINT ( 'NONE',  ( -7.500000000000008882, 42.00000000000000711, -71.41947339646975479 ) ) ;
#11256=CARTESIAN_POINT ( 'NONE',  ( 7.414909996474294829, 40.55825027170075003, -70.34917702029655118 ) ) ;
#11266=CARTESIAN_POINT ( 'NONE',  ( 23.85217781305834350, 47.99999999999999289, 60.68504519422547361 ) ) ;
#11271=ORIENTED_EDGE ( 'NONE', *, *, #4403, .T. ) ;
#11274=CARTESIAN_POINT ( 'NONE',  ( 11.90609530896518464, -5.000000000000002665, -79.26133957282229403 ) ) ;
#11275=CARTESIAN_POINT ( 'NONE',  ( 14.67571981732077191, -3.000000000000002665, -81.61772031543902983 ) ) ;
#11313=CARTESIAN_POINT ( 'NONE',  ( 7.149999999999997691, 41.65000000000000568, -59.82695526683420439 ) ) ;
#11315=CARTESIAN_POINT ( 'NONE',  ( 2.617478844990903664, -3.000000000000002665, -94.73972676610405586 ) ) ;
#11325=CARTESIAN_POINT ( 'NONE',  ( 3.510455435514055811, -4.999999999999999112, 17.23741894013592102 ) ) ;
#11343=( LENGTH_UNIT ( ) NAMED_UNIT ( * ) SI_UNIT ( .MILLI., .METRE. ) );
#11345=CARTESIAN_POINT ( 'NONE',  ( 19.49348534677603340, 49.99933769095211744, 60.04655563041394117 ) ) ;
#11360=CARTESIAN_POINT ( 'NONE',  ( -5.367391215540106231, 43.24496486319789312, -60.11082976391323029 ) ) ;
#11363=UNCERTAINTY_MEASURE_WITH_UNIT (LENGTH_MEASURE( 1.000000000000000082E-05 ), #41082, 'distance_accuracy_value', 'NONE');
#11373=CARTESIAN_POINT ( 'NONE',  ( -19.21241590914347341, 49.78725338447024740, 61.53583624396806329 ) ) ;
#11374=CARTESIAN_POINT ( 'NONE',  ( -7.384656406523468775, 41.09429650711703630, -59.07190356531275910 ) ) ;
#11377=CARTESIAN_POINT ( 'NONE',  ( 6.812289211616648466, 40.56151012360425767, -71.12586855819816378 ) ) ;
#11395=CARTESIAN_POINT ( 'NONE',  ( 10.48543666094595217, -5.000000000000002665, -91.04342776276725147 ) ) ;
#11416=CARTESIAN_POINT ( 'NONE',  ( 38.38499389482827695, 18.64284798592676395, 1.874612472324977519 ) ) ;
#11435=( NAMED_UNIT ( * ) SI_UNIT ( $, .STERADIAN. ) SOLID_ANGLE_UNIT ( ) );
#11461=FILL_AREA_STYLE ('',( #31544 ) ) ;
#11477=CARTESIAN_POINT ( 'NONE',  ( 6.821717117272701358, 41.99999999999999289, -69.36621149908677353 ) ) ;
#11486=CARTESIAN_POINT ( 'NONE',  ( 1.469576158976823356E-15, 50.00000000000000000, -73.00000000000001421 ) ) ;
#11488=CARTESIAN_POINT ( 'NONE',  ( -12.48795976855787870, -3.509606880211245006, -13.74293554157829078 ) ) ;
#11491=CARTESIAN_POINT ( 'NONE',  ( -7.500000000000006217, 40.00000000000064659, -68.91429205785792078 ) ) ;
#11498=B_SPLINE_CURVE_WITH_KNOTS ( 'NONE', 3,
 ( #9901, #42809, #82737, #98386, #187, #99979, #25610, #57384, #75703, #33152, #90297, #1801, #91376, #42269, #74630, #92413, #58469, #34759 ),
 .UNSPECIFIED., .F., .F.,
 ( 4, 2, 2, 2, 2, 2, 2, 2, 4 ),
 ( 0.000000000000000000, 0.1250000000000000555, 0.2500000000000001110, 0.3750000000000000555, 0.5000000000000000000, 0.6249999999999998890, 0.7499999999999998890, 0.8749999999999998890, 1.000000000000000000 ),
 .UNSPECIFIED. ) ;
#11503=CARTESIAN_POINT ( 'NONE',  ( -7.500000000000005329, -3.000000000000000000, -52.94236561372732552 ) ) ;
#11511=CARTESIAN_POINT ( 'NONE',  ( -6.731385053086962778, 41.26098029351368979, -70.78618130022729815 ) ) ;
#11513=ORIENTED_EDGE ( 'NONE', *, *, #40084, .T. ) ;
#11528=VERTEX_POINT ( 'NONE', #35877 ) ;
#11562=CARTESIAN_POINT ( 'NONE',  ( -7.500000000000005329, -3.000000000000000888, -52.94236561372726868 ) ) ;
#11574=CARTESIAN_POINT ( 'NONE',  ( 7.500000000000007105, -4.999999999999999112, -68.91429205785460965 ) ) ;
#11585=CARTESIAN_POINT ( 'NONE',  ( -5.484632972945890472, 41.99999999999999289, -59.73832710422585990 ) ) ;
#11609=ORIENTED_EDGE ( 'NONE', *, *, #861, .F. ) ;
#11617=CARTESIAN_POINT ( 'NONE',  ( 5.622685207874442703, 41.99823429251897977, -69.46126848786613550 ) ) ;
#11619=CARTESIAN_POINT ( 'NONE',  ( 53.52139369741866659, 50.00000000000000000, 33.73130704865685914 ) ) ;
#11643=CARTESIAN_POINT ( 'NONE',  ( 42.26632963665326770, 39.52651209077802008, -49.94030005733648636 ) ) ;
#11647=( NAMED_UNIT ( * ) SI_UNIT ( $, .STERADIAN. ) SOLID_ANGLE_UNIT ( ) );
#11653=CARTESIAN_POINT ( 'NONE',  ( 49.55398133112713310, 40.83861519483421176, -42.37453886910446244 ) ) ;
#11658=CARTESIAN_POINT ( 'NONE',  ( 39.08667504521157099, 48.00000000000000000, -56.76470588235297043 ) ) ;
#11661=CARTESIAN_POINT ( 'NONE',  ( 11.99999999999999467, 50.00000000000000000, -86.57079632498522415 ) ) ;
#11684=CARTESIAN_POINT ( 'NONE',  ( -5.293208566653007097, 18.42467780193287297, -37.80131242301784766 ) ) ;
#11713=EDGE_LOOP ( 'NONE', ( #69465, #76513, #12368, #32632 ) ) ;
#11743=CARTESIAN_POINT ( 'NONE',  ( -6.736688764309785249, 41.36687430129245513, -58.48851226247030155 ) ) ;
#11762=FACE_OUTER_BOUND ( 'NONE', #10588, .T. ) ;
#11765=CARTESIAN_POINT ( 'NONE',  ( 19.32152200345201010, 18.64316884708351552, 33.52312678236467747 ) ) ;
#11767=( NAMED_UNIT ( * ) SI_UNIT ( $, .STERADIAN. ) SOLID_ANGLE_UNIT ( ) );
#11770=B_SPLINE_CURVE_WITH_KNOTS ( 'NONE', 3,
 ( #17534, #18066, #50924, #90340, #81688, #25100, #75747, #82779, #82238, #1299 ),
 .UNSPECIFIED., .F., .F.,
 ( 4, 2, 2, 2, 4 ),
 ( 0.000000000000000000, 0.2500000000000000000, 0.5000000000000000000, 0.7500000000000000000, 1.000000000000000000 ),
 .UNSPECIFIED. ) ;
#11775=CARTESIAN_POINT ( 'NONE',  ( 5.945587289688900157, 41.44588091670027552, -58.45240130220552288 ) ) ;
#11776=CARTESIAN_POINT ( 'NONE',  ( -7.500000000000007105, 40.00000000000000000, -59.28631038546422616 ) ) ;
#11782=( NAMED_UNIT ( * ) PLANE_ANGLE_UNIT ( ) SI_UNIT ( $, .RADIAN. ) );
#11801=CARTESIAN_POINT ( 'NONE',  ( -12.13034742782337361, 42.00000149755588552, -93.82352941176404215 ) ) ;
#11807=ORIENTED_EDGE ( 'NONE', *, *, #92115, .T. ) ;
#11815=CARTESIAN_POINT ( 'NONE',  ( -9.891797161801505922, -5.000000000000002665, -73.72381496649795452 ) ) ;
#11816=CARTESIAN_POINT ( 'NONE',  ( 14.92666003044830703, -3.000000000000003109, -87.00284506552866048 ) ) ;
#11823=FILL_AREA_STYLE ('',( #86810 ) ) ;
#11835=CARTESIAN_POINT ( 'NONE',  ( -17.50000000000003553, 51.77766888148061497, 61.91533629926085780 ) ) ;
#11846=PLANE ( 'NONE',  #92726 ) ;
#11855=CARTESIAN_POINT ( 'NONE',  ( 0.000000000000000000, 47.00000000000000000, 60.00000000000000000 ) ) ;
#11868=CARTESIAN_POINT ( 'NONE',  ( -13.05035048250584495, -5.000000000000000000, -10.38464894538556749 ) ) ;
#11905=CARTESIAN_POINT ( 'NONE',  ( -7.500000000000007105, 41.91230289050422186, -61.59623549333881698 ) ) ;
#11916=CARTESIAN_POINT ( 'NONE',  ( -18.93287512597741795, 49.14208625572008060, 62.08427962429427538 ) ) ;
#11917=DIRECTION ( 'NONE',  ( -0.000000000000000000, 0.000000000000000000, -1.000000000000000000 ) ) ;
#11918=CARTESIAN_POINT ( 'NONE',  ( 5.225680565739399874, 40.98154495381307783, -70.87362144414954912 ) ) ;
#11936=SURFACE_STYLE_USAGE ( .BOTH. , #28173 ) ;
#11966=CARTESIAN_POINT ( 'NONE',  ( 7.360624614910192598, -5.000000000000000000, -94.61012438777778755 ) ) ;
#11973=CARTESIAN_POINT ( 'NONE',  ( -6.931554132363010545, -3.000000000000119904, -71.13906995426670221 ) ) ;
#11984=CARTESIAN_POINT ( 'NONE',  ( 17.50000000000093792, 49.99999999999815259, 59.71562975593438694 ) ) ;
#11990=CARTESIAN_POINT ( 'NONE',  ( 35.27776333575812373, 42.56632766162715598, -62.00109374954521257 ) ) ;
#12000=CARTESIAN_POINT ( 'NONE',  ( 29.83308852626540641, 42.00000000008230927, -51.76085035116526711 ) ) ;
#12008=CARTESIAN_POINT ( 'NONE',  ( -55.03804888984217314, 40.83927881983959907, 34.70779749804891168 ) ) ;
#12017=ORIENTED_EDGE ( 'NONE', *, *, #38944, .F. ) ;
#12026=CARTESIAN_POINT ( 'NONE',  ( 9.596002107491598210, 50.00000000000000000, -77.62543935901993564 ) ) ;
#12038=ORIENTED_EDGE ( 'NONE', *, *, #24958, .F. ) ;
#12054=CARTESIAN_POINT ( 'NONE',  ( -6.592078127955123712, 40.00000000008959944, -71.20206365128680659 ) ) ;
#12066=CARTESIAN_POINT ( 'NONE',  ( -17.52852338478520977, 45.00000000000000711, 63.46670662168261856 ) ) ;
#12099=CARTESIAN_POINT ( 'NONE',  ( 11.16922809658906424, -4.977367432874250319, -12.57708011016608296 ) ) ;
#12108=CARTESIAN_POINT ( 'NONE',  ( -12.71180608306794291, -4.333298119783883351, 12.63015221170769031 ) ) ;
#12110=CARTESIAN_POINT ( 'NONE',  ( 6.145467199749146125, 48.00000000000000711, -77.00333157601821199 ) ) ;
#12113=CARTESIAN_POINT ( 'NONE',  ( 9.500000000000000000, -5.000000000000000000, -20.99851272547260095 ) ) ;
#12114=CARTESIAN_POINT ( 'NONE',  ( 7.996668423981797780, -3.000000000000002665, -91.14546719974913458 ) ) ;
#12118=CARTESIAN_POINT ( 'NONE',  ( 55.22048556080756043, 48.00000000000000000, 34.80214219304977519 ) ) ;
#12123=CARTESIAN_POINT ( 'NONE',  ( -5.430162889308253860, 41.93410902331645929, -59.17461592276305993 ) ) ;
#12153=CARTESIAN_POINT ( 'NONE',  ( 6.458627575847655677, 41.53001914941116723, -70.63868815791025213 ) ) ;
#12156=CARTESIAN_POINT ( 'NONE',  ( 12.49986889690059222, -3.000000000000002665, -76.70852482682694529 ) ) ;
#12175=EDGE_CURVE ( 'NONE', #64826, #5970, #67119, .T. ) ;
#12183=CARTESIAN_POINT ( 'NONE',  ( -7.500000000000000888, -4.999999999999997335, -14.04024970282782547 ) ) ;
#12189=CARTESIAN_POINT ( 'NONE',  ( 46.55033305608798599, 41.07609238384448247, -46.50387254352151700 ) ) ;
#12194=( LENGTH_UNIT ( ) NAMED_UNIT ( * ) SI_UNIT ( .MILLI., .METRE. ) );
#12195=VERTEX_POINT ( 'NONE', #47189 ) ;
#12196=CARTESIAN_POINT ( 'NONE',  ( -9.999999999999992895, 48.00000000000000000, -86.30899693747680601 ) ) ;
#12207=ORIENTED_EDGE ( 'NONE', *, *, #41966, .T. ) ;
#12221=CARTESIAN_POINT ( 'NONE',  ( -5.197438949454540769, 4.242550593911340151, -24.96153357884654866 ) ) ;
#12226=CARTESIAN_POINT ( 'NONE',  ( -6.806778129255477872, 41.25019534346876782, -70.74215739106598733 ) ) ;
#12238=CARTESIAN_POINT ( 'NONE',  ( -17.88715956647400773, 50.00000000000001421, 62.04331920601425310 ) ) ;
#12265=CARTESIAN_POINT ( 'NONE',  ( 3.122376895888458570, 50.00000000000000711, -73.30448186995486992 ) ) ;
#12284=CARTESIAN_POINT ( 'NONE',  ( -5.402794924240495789, 41.73472301521996997, -58.79867575249376443 ) ) ;
#12303=CARTESIAN_POINT ( 'NONE',  ( 36.40416150955762475, 42.00000000000001421, -47.37019975555940476 ) ) ;
#12315=ORIENTED_EDGE ( 'NONE', *, *, #103971, .F. ) ;
#12327=COLOUR_RGB ( '', 0.66274510, 0.83137255, 0.94901961) ;
#12336=CARTESIAN_POINT ( 'NONE',  ( -10.50000000000000711, -5.000000000000000000, -77.33514508527181874 ) ) ;
#12351=CARTESIAN_POINT ( 'NONE',  ( 13.75294187950173175, -4.333298119783698610, -11.48770422858942375 ) ) ;
#12368=ORIENTED_EDGE ( 'NONE', *, *, #24742, .F. ) ;
#12372=( BOUNDED_SURFACE ( )  B_SPLINE_SURFACE ( 2, 3, ( 
 ( #43330, #76211, #36866, #18542, #18004, #19633, #10931, #59524, #34741, #35262, #75685, #50865, #52466, #44395, #20163, #92394, #12008, #60070, #77291, #101565, #3403, #51407, #69216, #83770, #36345, #69734, #58989, #67612, #9881, #84318, #102082, #60596, #53013, #43852, #84848, #28244, #61114, #76742, #44941, #10415, #68130, #1784, #101026, #94001, #2852, #92933, #85937, #19095, #42792, #35806, #68684, #27722, #77825, #91877 ),
 ( #71833, #86475, #22793, #13058, #63238, #29307, #103162, #53544, #79403, #70789, #37927, #38442, #54045, #62706, #62197, #104201, #63770, #47023, #79925, #14646, #47555, #80451, #95083, #20706, #22263, #46507, #6562, #86990, #96658, #6034, #104739, #78869, #39495, #30889, #103685, #29829, #102625, #38957, #55628, #88565, #61665, #95597, #5519, #21215, #88042, #94554, #28783, #12531, #21735, #45466, #45989, #78339, #4457, #55112 ),
 ( #37400, #70261, #30345, #14122, #4996, #54574, #87513, #13593, #71308, #96130, #105276, #41072, #106312, #15727, #33009, #72885, #105796, #16799, #57233, #8696, #33530, #15191, #40013, #16256, #91239, #56704, #66402, #49685, #41604, #48612, #17346, #74487, #73415, #7617, #83122, #82591, #562, #99283, #31422, #32476, #82042, #31935, #57763, #64297, #25462, #58314, #65347, #97169, #81497, #72370, #50221, #24909, #90689, #23316 ) ),
 .UNSPECIFIED., .F., .F., .F. ) 
 B_SPLINE_SURFACE_WITH_KNOTS ( ( 3, 3 ),
 ( 4, 2, 2, 2, 2, 2, 2, 2, 2, 2, 2, 2, 2, 2, 2, 2, 2, 2, 2, 2, 2, 2, 2, 2, 2, 2, 4 ),
 ( 0.000000000000000000, 1.000000000000000000 ),
 ( 0.000000000000000000, 0.01724146208191289220, 0.02586219312286933830, 0.03448292416382578440, 0.04310365520478223050, 0.05172438624573867660, 0.06034511728669512270, 0.06896584832765156881, 0.07758657936860802184, 0.08620731040956446101, 0.1034487724914773532, 0.1120695035324338062, 0.1206902345733902454, 0.1293109656143466846, 0.1379316966553031376, 0.1465524276962595907, 0.1551731587372160437, 0.1637938897781724967, 0.1724146208191289220, 0.1896560829010418003, 0.2068975449829547064, 0.2155182760239111595, 0.2241390070648676125, 0.2413804691467804908, 0.2500012001877369161, 0.2586219312286933691, 0.2758633933106062752 ),
 .UNSPECIFIED. ) 
 GEOMETRIC_REPRESENTATION_ITEM ( )  RATIONAL_B_SPLINE_SURFACE ( (
 ( 1.000000000000000000, 1.000000000000000000, 1.000000000000000000, 1.000000000000000000, 1.000000000000000000, 1.000000000000000000, 1.000000000000000000, 1.000000000000000000, 1.000000000000000000, 1.000000000000000000, 1.000000000000000000, 1.000000000000000000, 1.000000000000000000, 1.000000000000000000, 1.000000000000000000, 1.000000000000000000, 1.000000000000000000, 1.000000000000000000, 1.000000000000000000, 1.000000000000000000, 1.000000000000000000, 1.000000000000000000, 1.000000000000000000, 1.000000000000000000, 1.000000000000000000, 1.000000000000000000, 1.000000000000000000, 1.000000000000000000, 1.000000000000000000, 1.000000000000000000, 1.000000000000000000, 1.000000000000000000, 1.000000000000000000, 1.000000000000000000, 1.000000000000000000, 1.000000000000000000, 1.000000000000000000, 1.000000000000000000, 1.000000000000000000, 1.000000000000000000, 1.000000000000000000, 1.000000000000000000, 1.000000000000000000, 1.000000000000000000, 1.000000000000000000, 1.000000000000000000, 1.000000000000000000, 1.000000000000000000, 1.000000000000000000, 1.000000000000000000, 1.000000000000000000, 1.000000000000000000, 1.000000000000000000, 1.000000000000000000),
 ( 1.857142857142858317, 1.857142857142858317, 1.857142857142858317, 1.857142857142858317, 1.857142857142858317, 1.857142857142858317, 1.857142857142858317, 1.857142857142858317, 1.857142857142858317, 1.857142857142858317, 1.857142857142858317, 1.857142857142858317, 1.857142857142858317, 1.857142857142858317, 1.857142857142858317, 1.857142857142858317, 1.857142857142858317, 1.857142857142858317, 1.857142857142858317, 1.857142857142858317, 1.857142857142858317, 1.857142857142858317, 1.857142857142858317, 1.857142857142858317, 1.857142857142858317, 1.857142857142858317, 1.857142857142858317, 1.857142857142858317, 1.857142857142858317, 1.857142857142858317, 1.857142857142858317, 1.857142857142858317, 1.857142857142858317, 1.857142857142858317, 1.857142857142858317, 1.857142857142858317, 1.857142857142858317, 1.857142857142858317, 1.857142857142858317, 1.857142857142858317, 1.857142857142858317, 1.857142857142858317, 1.857142857142858317, 1.857142857142858317, 1.857142857142858317, 1.857142857142858317, 1.857142857142858317, 1.857142857142858317, 1.857142857142858317, 1.857142857142858317, 1.857142857142858317, 1.857142857142858317, 1.857142857142858317, 1.857142857142858317),
 ( 1.000000000000000000, 1.000000000000000000, 1.000000000000000000, 1.000000000000000000, 1.000000000000000000, 1.000000000000000000, 1.000000000000000000, 1.000000000000000000, 1.000000000000000000, 1.000000000000000000, 1.000000000000000000, 1.000000000000000000, 1.000000000000000000, 1.000000000000000000, 1.000000000000000000, 1.000000000000000000, 1.000000000000000000, 1.000000000000000000, 1.000000000000000000, 1.000000000000000000, 1.000000000000000000, 1.000000000000000000, 1.000000000000000000, 1.000000000000000000, 1.000000000000000000, 1.000000000000000000, 1.000000000000000000, 1.000000000000000000, 1.000000000000000000, 1.000000000000000000, 1.000000000000000000, 1.000000000000000000, 1.000000000000000000, 1.000000000000000000, 1.000000000000000000, 1.000000000000000000, 1.000000000000000000, 1.000000000000000000, 1.000000000000000000, 1.000000000000000000, 1.000000000000000000, 1.000000000000000000, 1.000000000000000000, 1.000000000000000000, 1.000000000000000000, 1.000000000000000000, 1.000000000000000000, 1.000000000000000000, 1.000000000000000000, 1.000000000000000000, 1.000000000000000000, 1.000000000000000000, 1.000000000000000000, 1.000000000000000000) ) ) 
 REPRESENTATION_ITEM ( '' )  SURFACE ( )  );
#12392=ORIENTED_EDGE ( 'NONE', *, *, #7126, .T. ) ;
#12393=CARTESIAN_POINT ( 'NONE',  ( 9.999008799016117166, -4.999999999999999112, -14.11099437790398348 ) ) ;
#12417=CARTESIAN_POINT ( 'NONE',  ( 7.421727596596154441, -4.999999999999994671, -70.37058874442523404 ) ) ;
#12429=CARTESIAN_POINT ( 'NONE',  ( -5.327003236163648126, 25.27808877631457207, -43.98407828350998727 ) ) ;
#12442=CARTESIAN_POINT ( 'NONE',  ( -18.91820967797469777, 48.57556059539511750, 62.17047390035803289 ) ) ;
#12444=CARTESIAN_POINT ( 'NONE',  ( 6.499946456771120040, 41.29102236647165114, -70.87268750739401924 ) ) ;
#12457=CARTESIAN_POINT ( 'NONE',  ( 5.293416525178801457, 18.46906883814961375, -37.84133857137602064 ) ) ;
#12459=CARTESIAN_POINT ( 'NONE',  ( -4.916373759799319565, -2.999999999999999556, -6.397334739185442487 ) ) ;
#12462=CARTESIAN_POINT ( 'NONE',  ( -6.145467200813103936, -5.000000000008177459, -92.99666842290147883 ) ) ;
#12483=EDGE_CURVE ( 'NONE', #72225, #106540, #78235, .T. ) ;
#12501=CARTESIAN_POINT ( 'NONE',  ( -7.717304146825799016, 50.00000000000000000, -95.65871486499432308 ) ) ;
#12512=ADVANCED_FACE ( 'NONE', ( #61149 ), #67841, .T. ) ;
#12513=SURFACE_STYLE_FILL_AREA ( #69713 ) ;
#12515=CARTESIAN_POINT ( 'NONE',  ( 43.55653793352204417, 41.43733932821601229, -50.61966037282592623 ) ) ;
#12524=CARTESIAN_POINT ( 'NONE',  ( -23.57730434126679597, 18.64316884711713485, 30.67950393662591324 ) ) ;
#12531=CARTESIAN_POINT ( 'NONE',  ( 64.56043141426960119, 39.42554324411963762, -8.108556725190846137 ) ) ;
#12564=CARTESIAN_POINT ( 'NONE',  ( -6.145467199749146125, 48.00000000000000000, -77.00333157601821199 ) ) ;
#12580=CARTESIAN_POINT ( 'NONE',  ( -6.806778129255477872, 41.25019534346876782, -70.74215739106598733 ) ) ;
#12591=CARTESIAN_POINT ( 'NONE',  ( -17.50415200142436234, 45.00000000000000711, 63.77658534312520544 ) ) ;
#12608=DIRECTION ( 'NONE',  ( 0.000000000000000000, 0.000000000000000000, 1.000000000000000000 ) ) ;
#12621=CARTESIAN_POINT ( 'NONE',  ( 11.04680601421287278, -4.985848638097940544, -12.57695916701952576 ) ) ;
#12641=CARTESIAN_POINT ( 'NONE',  ( -11.91432047182436094, 49.99999999999999289, 64.17585289259305625 ) ) ;
#12647=CARTESIAN_POINT ( 'NONE',  ( -6.986467899046544971, 41.76526127512707376, -59.56845298218130580 ) ) ;
#12658=CARTESIAN_POINT ( 'NONE',  ( 18.22111540436264221, 50.00000000000000711, 61.60966662904773017 ) ) ;
#12667=CARTESIAN_POINT ( 'NONE',  ( 6.738100180926640093, 41.71798714554645215, -59.05424661244425266 ) ) ;
#12669=CARTESIAN_POINT ( 'NONE',  ( 56.15646638878826735, 50.00000000000000711, 28.58272340641810771 ) ) ;
#12680=CARTESIAN_POINT ( 'NONE',  ( 5.175365594622103771, 41.93912328290134184, -69.86374199123662265 ) ) ;
#12714=B_SPLINE_CURVE_WITH_KNOTS ( 'NONE', 3,
 ( #70814, #87535, #29853, #13618 ),
 .UNSPECIFIED., .F., .F.,
 ( 4, 4 ),
 ( 0.000000000000000000, 0.4999999999999996114 ),
 .UNSPECIFIED. ) ;
#12718=DIRECTION ( 'NONE',  ( 8.160201061530222974E-17, 0.7456561006171790185, -0.6663309835302448914 ) ) ;
#12725=CARTESIAN_POINT ( 'NONE',  ( 8.737863884121436442, 48.00000000000000000, -79.96381019768851672 ) ) ;
#12735=CARTESIAN_POINT ( 'NONE',  ( -2.617478843592799365, -3.000000000000003109, -94.73972676668314818 ) ) ;
#12751=CARTESIAN_POINT ( 'NONE',  ( -5.221552941240854118, 7.001034474524052698, -27.46988742860714794 ) ) ;
#12764=CARTESIAN_POINT ( 'NONE',  ( -19.16958797051855612, 50.00000000000000000, 60.35583957385809128 ) ) ;
#12782=CARTESIAN_POINT ( 'NONE',  ( -13.43739347944073792, 42.84543662633798533, -92.02663817126700962 ) ) ;
#12810=CARTESIAN_POINT ( 'NONE',  ( 11.93415444004271464, -5.000000000000000000, 11.28339104396314774 ) ) ;
#12811=CARTESIAN_POINT ( 'NONE',  ( -6.798790223523980103, 41.26122158754633062, -58.42041485083363028 ) ) ;
#12825=CARTESIAN_POINT ( 'NONE',  ( 6.914390625618707986, 41.80417612998946453, -59.57688307474369793 ) ) ;
#12826=CARTESIAN_POINT ( 'NONE',  ( 59.23741894013591036, 42.00000000000000711, -7.754160006507188285 ) ) ;
#12828=ADVANCED_FACE ( 'NONE', ( #18452 ), #23936, .T. ) ;
#12862=CARTESIAN_POINT ( 'NONE',  ( -10.85300161404138031, -4.996537049337243630, -77.21885189817174933 ) ) ;
#12885=FILL_AREA_STYLE ('',( #94905 ) ) ;
#12909=CARTESIAN_POINT ( 'NONE',  ( -1.816153886384274108, 42.00000000000000711, -59.31995585001073579 ) ) ;
#12918=ORIENTED_EDGE ( 'NONE', *, *, #73366, .T. ) ;
#12924=CARTESIAN_POINT ( 'NONE',  ( -7.255520619063071663, -4.332661967060333907, 16.69105336089183211 ) ) ;
#12945=CARTESIAN_POINT ( 'NONE',  ( 18.91882778223193284, 48.67756978012194935, 62.16217564495511283 ) ) ;
#12968=CARTESIAN_POINT ( 'NONE',  ( -18.93152581076188312, 49.12231756752685641, 62.08966917159322207 ) ) ;
#12970=CARTESIAN_POINT ( 'NONE',  ( 6.035341166382893974, 41.06696360509113219, -71.06135895768771604 ) ) ;
#12973=CARTESIAN_POINT ( 'NONE',  ( 12.50000000000000178, -3.000000000000000000, -34.12705337366765690 ) ) ;
#12983=CARTESIAN_POINT ( 'NONE',  ( 5.293277849528764456, 18.43946955771025031, -37.81464980344904347 ) ) ;
#12984=CARTESIAN_POINT ( 'NONE',  ( 12.50000000000000000, -2.999999999999996891, -14.34180675897363955 ) ) ;
#12989=CARTESIAN_POINT ( 'NONE',  ( -1.308996937483428491, -5.000000000000002665, -75.00000000000001421 ) ) ;
#13015=CARTESIAN_POINT ( 'NONE',  ( 1.308679155693521556, -5.000000000000001776, 10.00000000000000533 ) ) ;
#13032=CARTESIAN_POINT ( 'NONE',  ( -42.39103542892770804, 39.51255807744743009, -49.77354649102187523 ) ) ;
#13051=CARTESIAN_POINT ( 'NONE',  ( 19.32152200345201010, 18.64316884708351552, 33.52312678236467747 ) ) ;
#13058=CARTESIAN_POINT ( 'NONE',  ( -61.99922069412622960, 39.42506226776489342, -19.74808858303288872 ) ) ;
#13079=CARTESIAN_POINT ( 'NONE',  ( 9.739726766105679445, 49.99999999999999289, -82.38252115500968387 ) ) ;
#13106=CARTESIAN_POINT ( 'NONE',  ( -5.255459963615564334, 41.40616545433940132, -70.76123437048775600 ) ) ;
#13156=CARTESIAN_POINT ( 'NONE',  ( 7.500000000000007105, 42.00000000000000711, -59.28631038546475907 ) ) ;
#13171=CARTESIAN_POINT ( 'NONE',  ( -37.84772257691307829, 50.00000000000000000, 50.69408796163851605 ) ) ;
#13179=CARTESIAN_POINT ( 'NONE',  ( -6.245851558170836704, 41.90677382336576073, -59.22337183934418903 ) ) ;
#13185=CARTESIAN_POINT ( 'NONE',  ( 18.01960457320383213, 50.00000000000000000, 61.86176977369216701 ) ) ;
#13195=CARTESIAN_POINT ( 'NONE',  ( 54.98690275242383052, 50.00000000000000000, 30.77418336387238540 ) ) ;
#13208=CARTESIAN_POINT ( 'NONE',  ( 6.503418564380250899, 41.93912275385427080, -68.91429206611401526 ) ) ;
#13252=CARTESIAN_POINT ( 'NONE',  ( -7.996668422904766871, 48.00000000000000000, -91.14546720082618947 ) ) ;
#13274=CARTESIAN_POINT ( 'NONE',  ( -5.221363059330018430, 6.978633969780313251, -27.44954744754475229 ) ) ;
#13289=SURFACE_SIDE_STYLE ('',( #6257 ) ) ;
#13304=( BOUNDED_SURFACE ( )  B_SPLINE_SURFACE ( 2, 3, ( 
 ( #66343, #51206, #84127, #43142, #35612, #42065, #35075, #76023, #2122, #8636, #100825, #74952, #67944, #43662, #26993, #41536, #59871, #84663, #76550, #2662, #57700, #3752 ),
 ( #45276, #53356, #54380, #101897, #36683, #69547, #4274, #19972, #28579, #69024, #70069, #29646, #78154, #37202, #77632, #28057, #85744, #95405, #60929, #21545, #52818, #11815 ),
 ( #93816, #44747, #85189, #11274, #102437, #53873, #94895, #102971, #44208, #61467, #46328, #21039, #29135, #70604, #62005, #93287, #94359, #86804, #86278, #87326, #62521, #37744 ) ),
 .UNSPECIFIED., .F., .F., .F. ) 
 B_SPLINE_SURFACE_WITH_KNOTS ( ( 3, 3 ),
 ( 4, 2, 2, 2, 2, 2, 2, 2, 2, 2, 4 ),
 ( 0.000000000000000000, 1.000000000000000000 ),
 ( 0.7200910805559007644, 0.9402275871953454933, 1.490568853793957427, 2.040910120392569471, 2.591251386991181072, 3.141592653589793116, 3.691933920188405160, 4.242275186787017205, 4.792616453385628361, 5.342957719984240406, 5.563094226623684690 ),
 .UNSPECIFIED. ) 
 GEOMETRIC_REPRESENTATION_ITEM ( )  RATIONAL_B_SPLINE_SURFACE ( (
 ( 1.000000000000000000, 1.000000000000000000, 1.000000000000000000, 1.000000000000000000, 1.000000000000000000, 1.000000000000000000, 1.000000000000000000, 1.000000000000000000, 1.000000000000000000, 1.000000000000000000, 1.000000000000000000, 1.000000000000000000, 1.000000000000000000, 1.000000000000000000, 1.000000000000000000, 1.000000000000000000, 1.000000000000000000, 1.000000000000000000, 1.000000000000000000, 1.000000000000000000, 1.000000000000000000, 1.000000000000000000),
 ( 1.857142857142858317, 1.857142857142858317, 1.857142857142858317, 1.857142857142858317, 1.857142857142858317, 1.857142857142858317, 1.857142857142858317, 1.857142857142858317, 1.857142857142858317, 1.857142857142858317, 1.857142857142858317, 1.857142857142858317, 1.857142857142858317, 1.857142857142858317, 1.857142857142858317, 1.857142857142858317, 1.857142857142858317, 1.857142857142858317, 1.857142857142858317, 1.857142857142858317, 1.857142857142858317, 1.857142857142858317),
 ( 1.000000000000000000, 1.000000000000000000, 1.000000000000000000, 1.000000000000000000, 1.000000000000000000, 1.000000000000000000, 1.000000000000000000, 1.000000000000000000, 1.000000000000000000, 1.000000000000000000, 1.000000000000000000, 1.000000000000000000, 1.000000000000000000, 1.000000000000000000, 1.000000000000000000, 1.000000000000000000, 1.000000000000000000, 1.000000000000000000, 1.000000000000000000, 1.000000000000000000, 1.000000000000000000, 1.000000000000000000) ) ) 
 REPRESENTATION_ITEM ( '' )  SURFACE ( )  );
#13311=CARTESIAN_POINT ( 'NONE',  ( -13.42788529234582029, 42.83958909155323624, -92.03970976739232412 ) ) ;
#13330=CARTESIAN_POINT ( 'NONE',  ( -6.101170145166853409, 41.83126053482132534, -70.32427505980624005 ) ) ;
#13335=CARTESIAN_POINT ( 'NONE',  ( -6.661867480585052625, 41.56276523291556657, -58.70509806605610237 ) ) ;
#13353=CARTESIAN_POINT ( 'NONE',  ( 7.049753237835907349, 41.74264190701163102, -59.69459104953257622 ) ) ;
#13354=CARTESIAN_POINT ( 'NONE',  ( -10.04205104288555184, 18.64316884714294886, -37.36680950593608230 ) ) ;
#13358=ORIENTED_EDGE ( 'NONE', *, *, #648, .T. ) ;
#13383=ORIENTED_EDGE ( 'NONE', *, *, #38825, .F. ) ;
#13406=CARTESIAN_POINT ( 'NONE',  ( 14.93248505798278103, -4.333298119783776770, 9.906141972414001629 ) ) ;
#13441=CARTESIAN_POINT ( 'NONE',  ( -1.843592604519083133, 42.00000000000000000, -60.21617040574370350 ) ) ;
#13499=CARTESIAN_POINT ( 'NONE',  ( -19.47277721183689891, 49.99121553149272756, 60.38168132464637239 ) ) ;
#13505=CARTESIAN_POINT ( 'NONE',  ( 12.50000000000000000, -3.000000000000000000, -9.904958390907863119 ) ) ;
#13517=CARTESIAN_POINT ( 'NONE',  ( 5.346341838538793745, 32.51490075182633177, -50.48043416745477430 ) ) ;
#13519=CARTESIAN_POINT ( 'NONE',  ( -1.047197551196599630, -2.999999999999999556, 8.000000000000000000 ) ) ;
#13523=CARTESIAN_POINT ( 'NONE',  ( -8.737863884121431113, -3.000000000000002665, -90.03618980231151170 ) ) ;
#13558=FACE_OUTER_BOUND ( 'NONE', #87252, .T. ) ;
#13575=PRESENTATION_STYLE_ASSIGNMENT (( #37379 ) ) ;
#13577=CARTESIAN_POINT ( 'NONE',  ( 19.68171092263090216, 43.94894922844405016, -83.44212096724145056 ) ) ;
#13586=CARTESIAN_POINT ( 'NONE',  ( 30.67950393662592745, 18.64316884711713485, 23.57730434126678887 ) ) ;
#13593=CARTESIAN_POINT ( 'NONE',  ( -63.69848661309710991, 38.95268708794027646, -2.134519030202793655 ) ) ;
#13611=CARTESIAN_POINT ( 'NONE',  ( 6.145467200820246667, 48.00000000000000000, -77.00333157708931253 ) ) ;
#13618=CARTESIAN_POINT ( 'NONE',  ( 6.201636426617084574E-15, 39.99999999999999289, -70.00365511371767013 ) ) ;
#13631=DIRECTION ( 'NONE',  ( 0.000000000000000000, 1.000000000000000000, 0.000000000000000000 ) ) ;
#13646=CIRCLE ( 'NONE', #29259, 56.99999999999999289 ) ;
#13675=CARTESIAN_POINT ( 'NONE',  ( 6.931965211968624807, 41.62851022707389603, -59.01894829855800140 ) ) ;
#13681=CARTESIAN_POINT ( 'NONE',  ( 5.347321875081102682, 33.30354557871893917, -51.19160682728892908 ) ) ;
#13702=CARTESIAN_POINT ( 'NONE',  ( 1.308996938995746318, -3.000000000000003553, -75.00000000000002842 ) ) ;
#13707=CARTESIAN_POINT ( 'NONE',  ( -62.59524157945776324, 49.99999999999999289, 18.50207713769457030 ) ) ;
#13720=CARTESIAN_POINT ( 'NONE',  ( 18.88506184278858058, 49.99999999999999289, 60.74108293188928798 ) ) ;
#13731=CARTESIAN_POINT ( 'NONE',  ( 53.87696817191028487, 49.99999999999999289, -33.03141454126155452 ) ) ;
#13742=CARTESIAN_POINT ( 'NONE',  ( 7.099152780515114891, 41.70084721948487072, -59.82719249545999674 ) ) ;
#13753=UNCERTAINTY_MEASURE_WITH_UNIT (LENGTH_MEASURE( 1.000000000000000082E-05 ), #69387, 'distance_accuracy_value', 'NONE');
#13781=CARTESIAN_POINT ( 'NONE',  ( 2.617478844989858722, 48.00000000000000000, -94.73972676610448218 ) ) ;
#13805=CARTESIAN_POINT ( 'NONE',  ( 8.000000000000000000, -4.999999999999998224, 2.094395098902538166 ) ) ;
#13807=CARTESIAN_POINT ( 'NONE',  ( -5.202336047186821411, 4.778347419875773383, -25.44939864730328338 ) ) ;
#13826=CARTESIAN_POINT ( 'NONE',  ( -18.17171551426997667, 50.00000000000001421, 61.67088195560315711 ) ) ;
#13834=CARTESIAN_POINT ( 'NONE',  ( 17.49999999999741007, 49.48689581941909665, 62.41113125630858605 ) ) ;
#13842=FACE_OUTER_BOUND ( 'NONE', #6854, .T. ) ;
#13869=CARTESIAN_POINT ( 'NONE',  ( 13.98998652022258682, -5.000000000000000000, 8.603073681314127086 ) ) ;
#13888=ORIENTED_EDGE ( 'NONE', *, *, #104526, .T. ) ;
#13899=EDGE_CURVE ( 'NONE', #24875, #55315, #48599, .T. ) ;
#13940=B_SPLINE_CURVE_WITH_KNOTS ( 'NONE', 3,
 ( #73174, #73719, #34378, #65644, #66165, #858, #50500, #48903, #66708, #99048, #65107, #49980, #100129, #26296, #8986, #32228, #41890, #59156, #92039, #106079, #16023, #24157, #98529, #7924, #106622, #32772, #24675, #57528, #45109, #69901, #34906, #85567, #67771, #20873, #42967, #51576, #26819, #69379, #53707, #10584, #60763, #37033, #19282, #59692, #102260, #84491, #28409, #27896, #3031, #86639, #93108, #86107, #101728, #3574, #92571, #77988, #43500, #52635, #61831, #76377, #100658, #11643, #2488, #4105, #93651, #68309, #75859, #35981, #19799, #44573 ),
 .UNSPECIFIED., .F., .F.,
 ( 4, 2, 2, 2, 1, 1, 1, 1, 1, 2, 2, 2, 2, 2, 1, 1, 1, 1, 1, 1, 2, 2, 2, 2, 2, 2, 1, 1, 1, 1, 1, 1, 2, 2, 2, 2, 2, 1, 1, 1, 1, 1, 2, 2, 2, 4 ),
 ( 0.000000000000000000, 0.06249999999979889698, 0.09374999999969835240, 0.1093749999996480732, 0.1171874999996228711, 0.1210937499996100064, 0.1230468749996035255, 0.1240234374996002781, 0.1245117187495986960, 0.1247558593745979189, 0.1249999999995971278, 0.1874999999994058364, 0.2187499999993102739, 0.2343749999992621735, 0.2421874999992381372, 0.2460937499992256472, 0.2480468749992193744, 0.2490234374992167377, 0.2495117187492148225, 0.2497558593742143507, 0.2498779296867145727, 0.2499999999992147948, 0.3124999999992655875, 0.3749999999993163802, 0.4374999999993672284, 0.4687499999993925970, 0.4843749999994054756, 0.4921874999994120814, 0.4960937499994153010, 0.4980468749994169664, 0.4990234374994177990, 0.4995117187494180211, 0.4997558593744183542, 0.4999999999994186872, 0.6249999999995474731, 0.6874999999996117550, 0.7187499999996438405, 0.7343749999996600497, 0.7421874999996682654, 0.7460937499996723732, 0.7480468749996741495, 0.7490234374996752598, 0.7495117187496758149, 0.7499999999996762590, 0.8749999999998381295, 1.000000000000000000 ),
 .UNSPECIFIED. ) ;
#13944=CARTESIAN_POINT ( 'NONE',  ( 10.00000000000000000, -5.000000000000000000, -2.617993873628171375 ) ) ;
#13950=FACE_BOUND ( 'NONE', #52472, .T. ) ;
#13977=ORIENTED_EDGE ( 'NONE', *, *, #18780, .T. ) ;
#13981=CARTESIAN_POINT ( 'NONE',  ( 16.64670748672000755, -5.000000000000000000, -1.019662339603576440 ) ) ;
#14002=CARTESIAN_POINT ( 'NONE',  ( 18.91772294158841206, 48.18298762545486369, 62.18609455207796088 ) ) ;
#14028=CARTESIAN_POINT ( 'NONE',  ( -7.150000000000001243, 41.64999999999999147, -68.91429205801802027 ) ) ;
#14030=SURFACE_STYLE_FILL_AREA ( #46935 ) ;
#14052=CARTESIAN_POINT ( 'NONE',  ( -9.739726766104286781, -3.000000000000002665, -87.61747884499033034 ) ) ;
#14060=ORIENTED_EDGE ( 'NONE', *, *, #103875, .F. ) ;
#14062=CARTESIAN_POINT ( 'NONE',  ( 7.498343863766716133, -2.970317092009080895, -20.23009517155373871 ) ) ;
#14075=CARTESIAN_POINT ( 'NONE',  ( -11.91432047156633622, 40.83906611472538373, 64.17585289266233417 ) ) ;
#14076=CARTESIAN_POINT ( 'NONE',  ( -7.126148247341459019, 41.12758119229484066, -58.55282700859728351 ) ) ;
#14079=( NAMED_UNIT ( * ) SI_UNIT ( $, .STERADIAN. ) SOLID_ANGLE_UNIT ( ) );
#14084=SURFACE_SIDE_STYLE ('',( #69700 ) ) ;
#14102=ORIENTED_EDGE ( 'NONE', *, *, #64833, .T. ) ;
#14103=CARTESIAN_POINT ( 'NONE',  ( 34.55488935567512243, 42.66466471040279629, -62.99488116903847867 ) ) ;
#14112=AXIS2_PLACEMENT_3D ( 'NONE', #67889, #66831, #27479 ) ;
#14115=CARTESIAN_POINT ( 'NONE',  ( 19.32152200343512760, 18.64316884711617561, -33.52312678240317467 ) ) ;
#14122=CARTESIAN_POINT ( 'NONE',  ( -60.72861731925209483, 38.95313093343226996, -19.34325272470447388 ) ) ;
#14128=EDGE_LOOP ( 'NONE', ( #19079, #10666, #75311, #94340 ) ) ;
#14140=CARTESIAN_POINT ( 'NONE',  ( 9.999999999999994671, 48.00000000000000000, -86.30899693747679180 ) ) ;
#14153=CARTESIAN_POINT ( 'NONE',  ( 9.364662338062446523, -5.000000000000000000, -18.68129556872268893 ) ) ;
#14171=CARTESIAN_POINT ( 'NONE',  ( 1.401122807519727897E-15, -4.999999999999988454, -95.00000000000000000 ) ) ;
#14180=ORIENTED_EDGE ( 'NONE', *, *, #57664, .F. ) ;
#14200=CARTESIAN_POINT ( 'NONE',  ( 7.303354934956394651, 41.37531465094661343, -59.25981217162325265 ) ) ;
#14209=CARTESIAN_POINT ( 'NONE',  ( 7.500000000000004441, 23.94542680926433320, -45.46585527945179450 ) ) ;
#14210=B_SPLINE_CURVE_WITH_KNOTS ( 'NONE', 3,
 ( #45912, #44861, #28168, #61581, #37320, #29238, #19555, #94472, #77749, #95009, #60520, #36269, #2778, #4380, #12984 ),
 .UNSPECIFIED., .F., .F.,
 ( 4, 2, 1, 2, 2, 1, 1, 2, 4 ),
 ( 0.000000000000000000, 0.4999999999999985567, 0.5624999999999986677, 0.5703124999999995559, 0.5781250000000004441, 0.5937500000000016653, 0.6250000000000032196, 0.7500000000000021094, 1.000000000000000000 ),
 .UNSPECIFIED. ) ;
#14232=CARTESIAN_POINT ( 'NONE',  ( 11.91432047181420195, 49.99999999997997691, 64.17585289263315929 ) ) ;
#14238=CARTESIAN_POINT ( 'NONE',  ( 11.72777639070659639, -4.888764692996097061, -76.94183081656832712 ) ) ;
#14246=CARTESIAN_POINT ( 'NONE',  ( 19.16286804424708023, 49.99999999999998579, 60.36494180815562771 ) ) ;
#14257=CARTESIAN_POINT ( 'NONE',  ( 46.29078044294533356, 50.00000000000000711, 42.75143139671600068 ) ) ;
#14270=MECHANICAL_DESIGN_GEOMETRIC_PRESENTATION_REPRESENTATION('',(#88364),#7415);
#14273=CARTESIAN_POINT ( 'NONE',  ( -17.49999999999997513, 50.00000000000000000, -500000.0000000000582 ) ) ;
#14286=CARTESIAN_POINT ( 'NONE',  ( 7.150000000000005684, 41.64999999999999147, -68.91429206202190016 ) ) ;
#14300=DIRECTION ( 'NONE',  ( -1.160749806054361473E-16, 0.000000000000000000, -1.000000000000000000 ) ) ;
#14308=ORIENTED_EDGE ( 'NONE', *, *, #41762, .F. ) ;
#14309=CARTESIAN_POINT ( 'NONE',  ( 1.308996937480704670, 48.00000000000000000, -75.00000000000001421 ) ) ;
#14330=CARTESIAN_POINT ( 'NONE',  ( 0.000000000000000000, -4.999999999999998224, 8.000000000000000000 ) ) ;
#14343=COLOUR_RGB ( '', 0.31764706, 0.68627451, 0.89019608) ;
#14349=CARTESIAN_POINT ( 'NONE',  ( -17.53286307268036737, 50.00000000000001421, 63.07570132845683020 ) ) ;
#14411=CARTESIAN_POINT ( 'NONE',  ( 6.700948648136186847, 41.88761797260490738, -59.59787299616537837 ) ) ;
#14419=VERTEX_POINT ( 'NONE', #57858 ) ;
#14453=MECHANICAL_DESIGN_GEOMETRIC_PRESENTATION_REPRESENTATION('',(#52346),#47188);
#14461=CARTESIAN_POINT ( 'NONE',  ( 11.39884040753850947, -4.333298119783793645, 13.82668420656116837 ) ) ;
#14464=CARTESIAN_POINT ( 'NONE',  ( 2.617993873628172263, -5.000000000000000000, -10.00000000000000000 ) ) ;
#14469=DIRECTION ( 'NONE',  ( 0.000000000000000000, -0.000000000000000000, 1.000000000000000000 ) ) ;
#14473=CYLINDRICAL_SURFACE ( 'NONE', #85554, 15.00000000000000000 ) ;
#14492=CARTESIAN_POINT ( 'NONE',  ( 6.298933871243065141, 41.33266196706044582, -58.30935828777717234 ) ) ;
#14507=ORIENTED_EDGE ( 'NONE', *, *, #4946, .F. ) ;
#14529=CARTESIAN_POINT ( 'NONE',  ( 19.19786010934679865, 49.77473709286820736, 61.56662838479388000 ) ) ;
#14578=CARTESIAN_POINT ( 'NONE',  ( -6.145467200819251019, -5.000000000000002665, -77.00333157709852117 ) ) ;
#14587=CARTESIAN_POINT ( 'NONE',  ( 7.084012698783952011, -4.012402067428147312, -17.39015006380907380 ) ) ;
#14589=CARTESIAN_POINT ( 'NONE',  ( -10.47796581436091579, 50.00000000000001421, -91.06180813479443259 ) ) ;
#14596=CARTESIAN_POINT ( 'NONE',  ( 7.150000000000005684, 41.64999999999999147, -68.91429206202190016 ) ) ;
#14607=PLANE ( 'NONE',  #66487 ) ;
#14625=CARTESIAN_POINT ( 'NONE',  ( -9.999999999999996447, -5.000000000000002665, -86.30899693747676338 ) ) ;
#14646=CARTESIAN_POINT ( 'NONE',  ( -43.66100747388606607, 39.42406093352394691, 48.52432126285668090 ) ) ;
#14664=CARTESIAN_POINT ( 'NONE',  ( -7.996668422906947349, 48.00000000000000000, -78.85453279917602742 ) ) ;
#14671=SURFACE_SIDE_STYLE ('',( #96157 ) ) ;
#14679=STYLED_ITEM ( 'NONE', ( #13575 ), #87845 ) ;
#14711=CARTESIAN_POINT ( 'NONE',  ( 6.819782173531151237, 41.52802923938777013, -70.37695045978405517 ) ) ;
#14719=CARTESIAN_POINT ( 'NONE',  ( -12.50000000000000711, 41.24423117302004727, -72.11661107032048790 ) ) ;
#14754=CARTESIAN_POINT ( 'NONE',  ( -4.205882352941162416, -5.000000000000000000, -72.69916451482997388 ) ) ;
#14764=CARTESIAN_POINT ( 'NONE',  ( 63.25915952246698026, 50.00000000000000000, 0.7870165385177050332 ) ) ;
#14773=CARTESIAN_POINT ( 'NONE',  ( 12.49986889690059222, -3.000000000000002665, -76.70852482682694529 ) ) ;
#14780=ORIENTED_EDGE ( 'NONE', *, *, #46849, .T. ) ;
#14781=CARTESIAN_POINT ( 'NONE',  ( 19.16335059359749593, 50.00000000000000000, 60.36429063721810451 ) ) ;
#14799=LINE ( 'NONE', #66013, #1424 ) ;
#14805=CARTESIAN_POINT ( 'NONE',  ( 6.849721346867525540, 41.84384207023756375, -59.83401400531045056 ) ) ;
#14847=CARTESIAN_POINT ( 'NONE',  ( -37.46929538836621276, 50.00000000000000000, -55.58823529426164356 ) ) ;
#14850=COLOUR_RGB ( '', 0.72549020, 0.75294118, 0.79215686) ;
#14867=( NAMED_UNIT ( * ) SI_UNIT ( $, .STERADIAN. ) SOLID_ANGLE_UNIT ( ) );
#14870=SURFACE_STYLE_USAGE ( .BOTH. , #21948 ) ;
#14882=CARTESIAN_POINT ( 'NONE',  ( -19.53695861423244651, 43.95068861312910258, -83.64112249031806812 ) ) ;
#14891=CARTESIAN_POINT ( 'NONE',  ( 17.50000000000007461, 48.00000000000153477, 62.61753806507840636 ) ) ;
#14894=( BOUNDED_SURFACE ( )  B_SPLINE_SURFACE ( 2, 3, ( 
 ( #55294, #11653, #12189, #36522, #45119, #77998, #102270, #61295, #102811, #37043 ),
 ( #28972, #64478, #82228, #23500, #81679, #56345, #98929, #15907, #105967, #97347 ),
 ( #90329, #31076, #41244, #66052, #64992, #89808, #22970, #16437, #40709, #96841 ) ),
 .UNSPECIFIED., .F., .F., .F. ) 
 B_SPLINE_SURFACE_WITH_KNOTS ( ( 3, 3 ),
 ( 4, 2, 2, 2, 4 ),
 ( 0.000000000000000000, 1.000000000000000000 ),
 ( 0.000000000000000000, 0.01533609919089652315, 0.03067219838179304631, 0.04600829757268956599, 0.06134439676358609261 ),
 .UNSPECIFIED. ) 
 GEOMETRIC_REPRESENTATION_ITEM ( )  RATIONAL_B_SPLINE_SURFACE ( (
 ( 1.000000000000000000, 1.000000000000000000, 1.000000000000000000, 1.000000000000000000, 1.000000000000000000, 1.000000000000000000, 1.000000000000000000, 1.000000000000000000, 1.000000000000000000, 1.000000000000000000),
 ( 1.857142857142858317, 1.857142857142858317, 1.857142857142858317, 1.857142857142858317, 1.857142857142858317, 1.857142857142858317, 1.857142857142858317, 1.857142857142858317, 1.857142857142858317, 1.857142857142858317),
 ( 1.000000000000000000, 1.000000000000000000, 1.000000000000000000, 1.000000000000000000, 1.000000000000000000, 1.000000000000000000, 1.000000000000000000, 1.000000000000000000, 1.000000000000000000, 1.000000000000000000) ) ) 
 REPRESENTATION_ITEM ( '' )  SURFACE ( )  );
#14900=CARTESIAN_POINT ( 'NONE',  ( -9.085304181916990629, -4.999999999999727329, -17.32925045961839317 ) ) ;
#14901=CARTESIAN_POINT ( 'NONE',  ( -12.13034742782427777, 41.99999999999999289, -93.82352941176471006 ) ) ;
#14950=CARTESIAN_POINT ( 'NONE',  ( 5.916007316295453400, 41.94280310092248243, -59.21688529221268738 ) ) ;
#14983=CARTESIAN_POINT ( 'NONE',  ( 0.000000000000000000, 0.000000000000000000, 0.000000000000000000 ) ) ;
#15007=CARTESIAN_POINT ( 'NONE',  ( 8.922269033010996608, -5.000000000000000000, -5.219866590717683330 ) ) ;
#15014=CARTESIAN_POINT ( 'NONE',  ( -12.49999999999999822, -4.999999999999999112, -8.595933841506989026 ) ) ;
#15015=CARTESIAN_POINT ( 'NONE',  ( 9.609938133566929608, -5.000000000000000000, -92.36043836069937640 ) ) ;
#15023=COLOUR_RGB ( '', 0.08235294, 0.09019608, 0.10196078) ;
#15037=CARTESIAN_POINT ( 'NONE',  ( -7.232205791931226813, 41.33266196707086237, -58.20097105120220249 ) ) ;
#15076=CARTESIAN_POINT ( 'NONE',  ( 19.40536060365760207, 49.94405995648938301, 60.94144269849599738 ) ) ;
#15098=CARTESIAN_POINT ( 'NONE',  ( -6.645598051714149967, 41.91296950070219651, -68.91429205809731684 ) ) ;
#15105=CARTESIAN_POINT ( 'NONE',  ( 10.50000000000000711, -5.000000000000000000, -80.60844091781802945 ) ) ;
#15123=CARTESIAN_POINT ( 'NONE',  ( -17.49999999999996803, 44.85000000000000853, 64.09953197957064219 ) ) ;
#15136=CARTESIAN_POINT ( 'NONE',  ( 7.499994653025345848, -2.925861026135234244, -20.99866594783414797 ) ) ;
#15173=CARTESIAN_POINT ( 'NONE',  ( 9.739726766102963396, -5.000000000000000888, -82.38252115499879835 ) ) ;
#15181=B_SPLINE_CURVE_WITH_KNOTS ( 'NONE', 3,
 ( #85669, #77567, #36614, #102364 ),
 .UNSPECIFIED., .F., .F.,
 ( 4, 4 ),
 ( 0.000000000000000000, 1.000000000000000000 ),
 .UNSPECIFIED. ) ;
#15184=CARTESIAN_POINT ( 'NONE',  ( -12.60465631124217900, -5.000000000000000000, -81.60874940243330400 ) ) ;
#15191=CARTESIAN_POINT ( 'NONE',  ( -30.78465349003366214, 38.95360288174918395, 55.80746841105920453 ) ) ;
#15200=MECHANICAL_DESIGN_GEOMETRIC_PRESENTATION_REPRESENTATION('',(#103078),#56533);
#15219=COLOUR_RGB ( '', 0.09019608, 0.27058824, 0.51372549) ;
#15229=CARTESIAN_POINT ( 'NONE',  ( 7.409209413120518839, -5.000000000000000888, -15.54546483169703563 ) ) ;
#15241=CARTESIAN_POINT ( 'NONE',  ( 5.096247963225427391, -4.999999999999998224, -73.00359695309825270 ) ) ;
#15255=CARTESIAN_POINT ( 'NONE',  ( 7.200568560992048006, 40.92548620364146927, -70.61799382922531265 ) ) ;
#15266=CARTESIAN_POINT ( 'NONE',  ( -62.27995536352283779, 50.00000000000000000, 9.818553861624332413 ) ) ;
#15272=B_SPLINE_SURFACE_WITH_KNOTS ( 'NONE', 3, 3, ( 
 ( #39913, #16152, #98658, #73858, #9116, #42025, #106752, #33971, #89527, #65244 ),
 ( #74908, #40970, #41494, #992, #24808, #99734, #58760, #57660, #98135, #56604 ),
 ( #48510, #81404, #16692, #91655, #31833, #47978, #90047, #8591, #80884, #6995 ),
 ( #97587, #49040, #81937, #49582, #8057, #82491, #7515, #72787, #105692, #64716 ),
 ( #40433, #43623, #36641, #19936, #60367, #9643, #67381, #93242, #69508, #83542 ),
 ( #28544, #10707, #51165, #35038, #68984, #102394, #3714, #52240, #17772, #60889 ),
 ( #52778, #19406, #42552, #67901, #85147, #35571, #61424, #11775, #93777, #76515 ),
 ( #50625, #85698, #68445, #11239, #44707, #27492, #2623, #101859, #84084, #34513 ) ),
 .UNSPECIFIED., .F., .F., .F.,
 ( 4, 2, 2, 4 ),
 ( 4, 2, 2, 2, 4 ),
 ( 0.000000000000000000, 0.2500000000000000000, 0.5000000000000000000, 1.000000000000000000 ),
 ( 0.000000000000000000, 0.1250000000000000000, 0.2500000000000000000, 0.5000000000000000000, 1.000000000000000000 ),
 .UNSPECIFIED. ) ;
#15302=CARTESIAN_POINT ( 'NONE',  ( 62.59524157938817268, 40.83906611471955728, 18.50207713792757147 ) ) ;
#15323=MECHANICAL_DESIGN_GEOMETRIC_PRESENTATION_REPRESENTATION('',(#56657),#44614);
#15364=B_SPLINE_CURVE_WITH_KNOTS ( 'NONE', 3,
 ( #41706, #66507, #1755, #82151, #49788, #57334 ),
 .UNSPECIFIED., .F., .F.,
 ( 4, 2, 4 ),
 ( 0.000000000000000000, 0.5000000000000000000, 1.000000000000000000 ),
 .UNSPECIFIED. ) ;
#15404=CARTESIAN_POINT ( 'NONE',  ( 7.137815226408910974, -4.999999999999998224, 4.175893272575850190 ) ) ;
#15413=CARTESIAN_POINT ( 'NONE',  ( -4.852941176470598528, -3.000000000000002665, -70.80672828634229177 ) ) ;
#15427=AXIS2_PLACEMENT_3D ( 'NONE', #46823, #102947, #29618 ) ;
#15431=CARTESIAN_POINT ( 'NONE',  ( 17.50000000000004619, 50.67917894245540822, 63.46126552127685727 ) ) ;
#15439=CARTESIAN_POINT ( 'NONE',  ( -7.022229286278467875, -4.221542269106504541, -17.11103215587112913 ) ) ;
#15455=ORIENTED_EDGE ( 'NONE', *, *, #44345, .F. ) ;
#15461=CARTESIAN_POINT ( 'NONE',  ( 63.03617022297318329, 49.99999999997997691, -16.93907820452584545 ) ) ;
#15494=CARTESIAN_POINT ( 'NONE',  ( 6.031322594622289479, 41.99459408341585487, -59.73016589819391697 ) ) ;
#15504=CARTESIAN_POINT ( 'NONE',  ( -6.392921701574284299, 41.54610357429506706, -70.64273452805430509 ) ) ;
#15506=VERTEX_POINT ( 'NONE', #51913 ) ;
#15507=( NAMED_UNIT ( * ) SI_UNIT ( $, .STERADIAN. ) SOLID_ANGLE_UNIT ( ) );
#15542=CARTESIAN_POINT ( 'NONE',  ( 7.137815226409024660, -5.000000000001136868, -4.175893272573466319 ) ) ;
#15550=FILL_AREA_STYLE_COLOUR ( '', #41836 ) ;
#15551=CARTESIAN_POINT ( 'NONE',  ( -10.50000000000000711, -5.000000000000000000, -78.42624373368740009 ) ) ;
#15555=B_SPLINE_CURVE_WITH_KNOTS ( 'NONE', 3,
 ( #82900, #64724, #88477, #22165, #15098, #29739, #80354, #14028 ),
 .UNSPECIFIED., .F., .F.,
 ( 4, 2, 2, 4 ),
 ( 0.000000000000000000, 0.5000000000000000000, 0.7500000000000000000, 1.000000000000000000 ),
 .UNSPECIFIED. ) ;
#15583=CARTESIAN_POINT ( 'NONE',  ( -8.786988139152953468E-15, 18.64300841652315910, 38.36521369532682257 ) ) ;
#15608=EDGE_CURVE ( 'NONE', #12195, #83228, #5778, .T. ) ;
#15661=CARTESIAN_POINT ( 'NONE',  ( 7.417322861520009525, -4.999999999978371079, -16.62528780688618824 ) ) ;
#15680=CARTESIAN_POINT ( 'NONE',  ( -17.50000000000013500, 50.00117660290769805, 59.93398959461790554 ) ) ;
#15686=ORIENTED_EDGE ( 'NONE', *, *, #100790, .T. ) ;
#15702=CARTESIAN_POINT ( 'NONE',  ( 6.145467200820721843, -5.000000000000002665, -77.00333157708637088 ) ) ;
#15706=FILL_AREA_STYLE_COLOUR ( '', #53894 ) ;
#15719=CARTESIAN_POINT ( 'NONE',  ( -10.50000000000000711, -5.000000000000000000, -77.33514508527181874 ) ) ;
#15727=CARTESIAN_POINT ( 'NONE',  ( -59.20842685209844092, 38.95251792617707309, 23.59073220948269878 ) ) ;
#15729=B_SPLINE_CURVE_WITH_KNOTS ( 'NONE', 3,
 ( #83474, #68914, #43558, #10639 ),
 .UNSPECIFIED., .F., .F.,
 ( 4, 4 ),
 ( 0.000000000000000000, 0.1960348326659903384 ),
 .UNSPECIFIED. ) ;
#15745=CARTESIAN_POINT ( 'NONE',  ( -10.96784672161025753, -4.990140223832483457, -12.57412324632270284 ) ) ;
#15751=( GEOMETRIC_REPRESENTATION_CONTEXT ( 3 ) GLOBAL_UNCERTAINTY_ASSIGNED_CONTEXT ( ( #106555 ) ) GLOBAL_UNIT_ASSIGNED_CONTEXT ( ( #76735, #27713, #60588 ) ) REPRESENTATION_CONTEXT ( 'NONE', 'WORKASPACE' ) );
#15764=CARTESIAN_POINT ( 'NONE',  ( -7.150000055923752207, 41.64999994407625650, -59.82695526654634222 ) ) ;
#15773=CARTESIAN_POINT ( 'NONE',  ( 4.205882352941182845, -5.000000000000000000, -72.69916451482998809 ) ) ;
#15785=CARTESIAN_POINT ( 'NONE',  ( 7.204798266847586952, 41.05104862198670190, -70.50691143559862439 ) ) ;
#15789=B_SPLINE_CURVE_WITH_KNOTS ( 'NONE', 3,
 ( #91207, #48583, #80955, #9185 ),
 .UNSPECIFIED., .F., .F.,
 ( 4, 4 ),
 ( 0.000000000000000000, 1.000000000000000000 ),
 .UNSPECIFIED. ) ;
#15796=CARTESIAN_POINT ( 'NONE',  ( -50.32426797222468196, 50.00000000000001421, 38.04620492663661935 ) ) ;
#15806=CARTESIAN_POINT ( 'NONE',  ( 7.149999999999998579, 41.65000000000000568, -59.82695526683419729 ) ) ;
#15820=EDGE_LOOP ( 'NONE', ( #54504, #68732, #40707, #19834, #50586, #87715 ) ) ;
#15825=SURFACE_STYLE_USAGE ( .BOTH. , #31514 ) ;
#15845=CARTESIAN_POINT ( 'NONE',  ( -6.642722259512091831, 41.46658730094534917, -70.60825968550385312 ) ) ;
#15878=FILL_AREA_STYLE_COLOUR ( '', #76081 ) ;
#15882=CARTESIAN_POINT ( 'NONE',  ( -7.493258478124158906, 40.28998945925845021, -69.65507826025705640 ) ) ;
#15888=ORIENTED_EDGE ( 'NONE', *, *, #43425, .F. ) ;
#15907=CARTESIAN_POINT ( 'NONE',  ( 22.51022058473584053, 41.90417167145406552, -79.55356307799623039 ) ) ;
#15914=CARTESIAN_POINT ( 'NONE',  ( 12.50000000000000355, 39.75445632001817842, -65.02425370658717441 ) ) ;
#15937=CARTESIAN_POINT ( 'NONE',  ( 2.094395098902661179, -4.999999999999998224, 8.000000000000000000 ) ) ;
#15944=( GEOMETRIC_REPRESENTATION_CONTEXT ( 3 ) GLOBAL_UNCERTAINTY_ASSIGNED_CONTEXT ( ( #85550 ) ) GLOBAL_UNIT_ASSIGNED_CONTEXT ( ( #100301, #59329, #58249 ) ) REPRESENTATION_CONTEXT ( 'NONE', 'WORKASPACE' ) );
#15967=CARTESIAN_POINT ( 'NONE',  ( 17.50000000000000355, 51.12013589171683492, 63.06608111885196877 ) ) ;
#15976=CARTESIAN_POINT ( 'NONE',  ( -7.500141383061431632, -5.000000000000005329, -20.99866593659555036 ) ) ;
#16003=SURFACE_SIDE_STYLE ('',( #72637 ) ) ;
#16012=CARTESIAN_POINT ( 'NONE',  ( -11.09043181265275813, 18.64284798592964165, 36.79570967431529738 ) ) ;
#16023=CARTESIAN_POINT ( 'NONE',  ( 23.39223446984816590, 41.66174788536504536, -75.12607633062728496 ) ) ;
#16055=CARTESIAN_POINT ( 'NONE',  ( 5.420470438621123321, 41.88321586334136981, -59.04137885805280916 ) ) ;
#16056=UNCERTAINTY_MEASURE_WITH_UNIT (LENGTH_MEASURE( 1.000000000000000082E-05 ), #76106, 'distance_accuracy_value', 'NONE');
#16077=CARTESIAN_POINT ( 'NONE',  ( 0.000000000000000000, -4.999999999999998224, 8.000000000000000000 ) ) ;
#16144=UNCERTAINTY_MEASURE_WITH_UNIT (LENGTH_MEASURE( 1.000000000000000082E-05 ), #22431, 'distance_accuracy_value', 'NONE');
#16152=CARTESIAN_POINT ( 'NONE',  ( 6.690415142086857614, 41.73276191905608812, -59.04972836783017698 ) ) ;
#16156=EDGE_CURVE ( 'NONE', #21912, #52979, #101485, .T. ) ;
#16164=SURFACE_STYLE_USAGE ( .BOTH. , #64214 ) ;
#16169=EDGE_CURVE ( 'NONE', #12195, #81281, #31754, .T. ) ;
#16171=CARTESIAN_POINT ( 'NONE',  ( 17.54774805024657880, 45.00000000000000711, 63.32653931362602862 ) ) ;
#16178=CARTESIAN_POINT ( 'NONE',  ( -9.366249310892840185, -5.000000000000000888, -18.69166165298246085 ) ) ;
#16187=ORIENTED_EDGE ( 'NONE', *, *, #19931, .T. ) ;
#16194=CARTESIAN_POINT ( 'NONE',  ( 7.499143977329139510, -3.006661276311841213, -20.23006715386459220 ) ) ;
#16212=CARTESIAN_POINT ( 'NONE',  ( -19.31075363035708037, 49.87050359945074263, 61.31541196678981009 ) ) ;
#16232=CARTESIAN_POINT ( 'NONE',  ( -1.570796324980114456, -5.000000000000002665, -73.00000000000001421 ) ) ;
#16237=PRESENTATION_STYLE_ASSIGNMENT (( #31919 ) ) ;
#16248=CARTESIAN_POINT ( 'NONE',  ( -10.36961810765524206, -5.000000000000000000, -92.92744404105623346 ) ) ;
#16256=CARTESIAN_POINT ( 'NONE',  ( -22.83134759184064677, 38.95245226452999532, 59.50471635465192577 ) ) ;
#16265=SURFACE_STYLE_FILL_AREA ( #7626 ) ;
#16292=CARTESIAN_POINT ( 'NONE',  ( -6.933421966067523812, 41.67527023642382034, -59.13217477274009326 ) ) ;
#16310=CARTESIAN_POINT ( 'NONE',  ( 7.150000000000015454, 41.65000000000000568, -68.91429206202192859 ) ) ;
#16316=CARTESIAN_POINT ( 'NONE',  ( -7.126148247341459019, 41.12758119229484066, -58.55282700859728351 ) ) ;
#16336=CARTESIAN_POINT ( 'NONE',  ( 7.500000000000007105, 40.28750351091937176, -59.87155384411956760 ) ) ;
#16353=CARTESIAN_POINT ( 'NONE',  ( -19.42937650476450173, 49.96296734528215211, 60.82359239913852633 ) ) ;
#16355=CARTESIAN_POINT ( 'NONE',  ( -7.500000000000004441, 24.91666666666666430, -71.71180648257555390 ) ) ;
#16360=CARTESIAN_POINT ( 'NONE',  ( 55.22048556069530889, 40.83906611472065862, 34.80214219327351799 ) ) ;
#16410=CARTESIAN_POINT ( 'NONE',  ( -6.819782170910313468, 41.52802923942638103, -70.37695045795369708 ) ) ;
#16429=CARTESIAN_POINT ( 'NONE',  ( -9.610124387782905231, -5.000000000000000000, -92.36062461491069087 ) ) ;
#16437=CARTESIAN_POINT ( 'NONE',  ( 20.94716680843786705, 41.83711872324442993, -78.41834032275426125 ) ) ;
#16442=CARTESIAN_POINT ( 'NONE',  ( 12.50000000000000711, 34.86365967266531385, -54.17194305995318615 ) ) ;
#16446=CARTESIAN_POINT ( 'NONE',  ( -7.500000000000007105, 39.99999999999998579, -68.91429205786793943 ) ) ;
#16481=DIRECTION ( 'NONE',  ( 0.000000000000000000, -0.000000000000000000, -1.000000000000000000 ) ) ;
#16505=CARTESIAN_POINT ( 'NONE',  ( -5.686850908485443057, -4.337623088834303253, -16.91150612931922836 ) ) ;
#16514=ORIENTED_EDGE ( 'NONE', *, *, #70657, .T. ) ;
#16534=ORIENTED_EDGE ( 'NONE', *, *, #35288, .F. ) ;
#16571=CARTESIAN_POINT ( 'NONE',  ( 0.000000000000000000, 50.00000000000000000, 60.00000000000000000 ) ) ;
#16593=CARTESIAN_POINT ( 'NONE',  ( -14.33580413397241315, 42.00000000000000000, -89.41414995581023106 ) ) ;
#16613=CARTESIAN_POINT ( 'NONE',  ( -6.921856738059538827, 41.59435685020019235, -70.13580383255586526 ) ) ;
#16649=ORIENTED_EDGE ( 'NONE', *, *, #59776, .F. ) ;
#16682=CARTESIAN_POINT ( 'NONE',  ( 72.41885610124130324, 42.00000000000000000, 55.65414010178505322 ) ) ;
#16687=PRESENTATION_STYLE_ASSIGNMENT (( #6990 ) ) ;
#16692=CARTESIAN_POINT ( 'NONE',  ( 6.706751688761142027, 41.66489572023301946, -58.91094412759547794 ) ) ;
#16704=( NAMED_UNIT ( * ) PLANE_ANGLE_UNIT ( ) SI_UNIT ( $, .RADIAN. ) );
#16711=CARTESIAN_POINT ( 'NONE',  ( 17.99657652128994201, 44.99999999999999289, 62.56960515030601755 ) ) ;
#16716=CARTESIAN_POINT ( 'NONE',  ( -6.686471517026126854, -4.999999999999999112, -15.36038768879105731 ) ) ;
#16723=SURFACE_STYLE_USAGE ( .BOTH. , #31866 ) ;
#16724=DIRECTION ( 'NONE',  ( -0.000000000000000000, 0.000000000000000000, 1.000000000000000000 ) ) ;
#16751=CARTESIAN_POINT ( 'NONE',  ( -19.07202809346026129, 49.63760697579748182, 61.78692401719171556 ) ) ;
#16773=CARTESIAN_POINT ( 'NONE',  ( -10.48543666094594862, -5.000000000000002665, -91.04342776276726568 ) ) ;
#16791=CARTESIAN_POINT ( 'NONE',  ( -12.86258593040350995, -5.000000000000000000, -82.77024182148061016 ) ) ;
#16799=CARTESIAN_POINT ( 'NONE',  ( -50.58582176620591753, 38.95379933617689971, 38.77008064533420395 ) ) ;
#16842=CARTESIAN_POINT ( 'NONE',  ( 6.619572829571047201, 41.38254192185750924, -70.73105035554675624 ) ) ;
#16845=COLOUR_RGB ( '', 0.66274510, 0.83137255, 0.94901961) ;
#16855=CARTESIAN_POINT ( 'NONE',  ( 5.363597346073513350, 41.33266196706048845, -58.39526881795627844 ) ) ;
#16864=CARTESIAN_POINT ( 'NONE',  ( 7.452250447672242650, 40.95020998762944942, -69.64366759659492345 ) ) ;
#16867=( GEOMETRIC_REPRESENTATION_CONTEXT ( 3 ) GLOBAL_UNCERTAINTY_ASSIGNED_CONTEXT ( ( #32264 ) ) GLOBAL_UNIT_ASSIGNED_CONTEXT ( ( #74122, #51976, #9925 ) ) REPRESENTATION_CONTEXT ( 'NONE', 'WORKASPACE' ) );
#16869=ORIENTED_EDGE ( 'NONE', *, *, #42087, .F. ) ;
#16884=ADVANCED_FACE ( 'NONE', ( #29632 ), #49883, .T. ) ;
#16885=CARTESIAN_POINT ( 'NONE',  ( 7.054522925320324767, 41.71556257522360767, -59.55896313260247865 ) ) ;
#16898=CARTESIAN_POINT ( 'NONE',  ( 13.44879422951056291, 42.85243152879387196, -92.01096473121475583 ) ) ;
#16957=CARTESIAN_POINT ( 'NONE',  ( -6.941422770587817759, 41.41225025357826439, -70.44081391737150000 ) ) ;
#16973=VERTEX_POINT ( 'NONE', #32804 ) ;
#16990=CARTESIAN_POINT ( 'NONE',  ( 12.50000000000000000, 28.57588390897651820, -46.22316309954614155 ) ) ;
#17003=MECHANICAL_DESIGN_GEOMETRIC_PRESENTATION_REPRESENTATION('',(#8360),#70433);
#17005=CARTESIAN_POINT ( 'NONE',  ( 16.66584972137510690, 38.95383793069935763, 62.01418705508215368 ) ) ;
#17019=CARTESIAN_POINT ( 'NONE',  ( -7.500000000000007105, 40.28750026290749275, -59.87155394325278479 ) ) ;
#17045=CARTESIAN_POINT ( 'NONE',  ( 18.91772294109960484, 48.25776538899425816, 62.18609455222646432 ) ) ;
#17053=CARTESIAN_POINT ( 'NONE',  ( -7.543027128863474040, -5.000000000008911982, -20.22853049137013315 ) ) ;
#17077=CARTESIAN_POINT ( 'NONE',  ( 43.69716417794892749, 48.00000000000000000, 48.48761666242516100 ) ) ;
#17092=ORIENTED_EDGE ( 'NONE', *, *, #67802, .T. ) ;
#17117=CARTESIAN_POINT ( 'NONE',  ( -19.46358522980415273, 49.98601987196752106, 60.49302799977217404 ) ) ;
#17203=CARTESIAN_POINT ( 'NONE',  ( 9.500000000000003553, -5.000000000000000000, -68.91429205785459544 ) ) ;
#17207=CARTESIAN_POINT ( 'NONE',  ( -7.150000000000003908, 41.64999999999997726, -68.91429205801804869 ) ) ;
#17240=PLANE ( 'NONE',  #113 ) ;
#17304=CARTESIAN_POINT ( 'NONE',  ( -17.49999999999077360, 50.03176226080658040, 60.82931034967823081 ) ) ;
#17316=CARTESIAN_POINT ( 'NONE',  ( -23.57474994864879037, 41.64982833201018053, -74.87904004496073185 ) ) ;
#17327=ORIENTED_EDGE ( 'NONE', *, *, #50569, .T. ) ;
#17346=CARTESIAN_POINT ( 'NONE',  ( 5.816656174490083764, 38.95337264755559659, 63.46943632529147550 ) ) ;
#17382=CYLINDRICAL_SURFACE ( 'NONE', #21737, 9.999999999999994671 ) ;
#17409=CARTESIAN_POINT ( 'NONE',  ( -63.05056382741410204, 50.00000000000000711, -0.01919565705159020919 ) ) ;
#17468=CARTESIAN_POINT ( 'NONE',  ( 72.41885610124130324, 42.00000000000000000, 55.65414010178505322 ) ) ;
#17496=CARTESIAN_POINT ( 'NONE',  ( -7.354129747669107431, 40.93126392605007879, -70.29718773507885032 ) ) ;
#17527=CARTESIAN_POINT ( 'NONE',  ( 12.50000000000000000, 35.04556876861937553, -54.45246410008698490 ) ) ;
#17534=CARTESIAN_POINT ( 'NONE',  ( -4.852941176470598528, -3.000000000000002665, -70.80672828634229177 ) ) ;
#17584=CARTESIAN_POINT ( 'NONE',  ( -6.831363903021533623, 41.73171925724633979, -59.17722475679354233 ) ) ;
#17606=ORIENTED_EDGE ( 'NONE', *, *, #5276, .F. ) ;
#17613=( NAMED_UNIT ( * ) SI_UNIT ( $, .STERADIAN. ) SOLID_ANGLE_UNIT ( ) );
#17684=COLOUR_RGB ( '', 0.66274510, 0.83137255, 0.94901961) ;
#17694=CARTESIAN_POINT ( 'NONE',  ( -17.49999999999997868, 49.03511921915654170, 64.04809060635940909 ) ) ;
#17711=CARTESIAN_POINT ( 'NONE',  ( -14.91271302809441401, 41.98564543112699710, -86.62215342991694911 ) ) ;
#17728=EDGE_LOOP ( 'NONE', ( #62051, #91091, #53396, #7396 ) ) ;
#17741=CARTESIAN_POINT ( 'NONE',  ( -6.690415133250795954, 41.73276121203647904, -59.04972748448755482 ) ) ;
#17750=CARTESIAN_POINT ( 'NONE',  ( 12.50000000000000355, 16.77477425093740848, -34.50590399936646691 ) ) ;
#17772=CARTESIAN_POINT ( 'NONE',  ( 5.663715349034363022, 41.53602215441348022, -58.55436094691613391 ) ) ;
#17794=CARTESIAN_POINT ( 'NONE',  ( -7.462369933651546106, -5.000000000000000000, -15.56882655052671005 ) ) ;
#17800=CARTESIAN_POINT ( 'NONE',  ( 57.77058984079067017, 47.99999999999999289, 30.23507972700048541 ) ) ;
#17802=VERTEX_POINT ( 'NONE', #88514 ) ;
#17811=SURFACE_SIDE_STYLE ('',( #25943 ) ) ;
#17812=CARTESIAN_POINT ( 'NONE',  ( -2.695484166377266178, -3.000000000000003109, -99.81725120020260533 ) ) ;
#17824=EDGE_CURVE ( 'NONE', #37165, #21469, #102419, .T. ) ;
#17832=CARTESIAN_POINT ( 'NONE',  ( -19.21238756580856588, 49.78778941994462315, 61.53710458953445084 ) ) ;
#17847=CARTESIAN_POINT ( 'NONE',  ( -19.47123783567355915, 41.87075544860245913, -80.42687978217861655 ) ) ;
#17857=CARTESIAN_POINT ( 'NONE',  ( 6.581905806972325301, 41.48827110309209587, -70.61906944721928880 ) ) ;
#17896=CARTESIAN_POINT ( 'NONE',  ( -11.82790241188288149, -4.854504338693105048, -12.55817724909448785 ) ) ;
#17905=ORIENTED_EDGE ( 'NONE', *, *, #18520, .T. ) ;
#17913=CARTESIAN_POINT ( 'NONE',  ( -7.262243269759384390, 41.41224259789315454, -59.17677581639546247 ) ) ;
#17969=EDGE_CURVE ( 'NONE', #84701, #84646, #104906, .T. ) ;
#17971=CARTESIAN_POINT ( 'NONE',  ( -7.500000000000005329, 42.83333333333328596, -68.91429205785459544 ) ) ;
#17995=CARTESIAN_POINT ( 'NONE',  ( -88.20421627925436781, 42.00000000000000000, 23.70422451878991765 ) ) ;
#18004=CARTESIAN_POINT ( 'NONE',  ( -62.84963380242372466, 40.83902055873923587, -16.84608294976931120 ) ) ;
#18007=CARTESIAN_POINT ( 'NONE',  ( 13.36289610070329381, 41.70153073425857571, -78.00930284188133612 ) ) ;
#18022=CARTESIAN_POINT ( 'NONE',  ( -7.224854285009186583, 41.52722297675348528, -69.60668029987157013 ) ) ;
#18034=CARTESIAN_POINT ( 'NONE',  ( -5.500000000000007994, 42.00000000000000000, -68.91429205818155879 ) ) ;
#18042=EDGE_CURVE ( 'NONE', #21685, #21200, #44550, .T. ) ;
#18061=CARTESIAN_POINT ( 'NONE',  ( 12.50000000000000533, 39.21611849718817666, -63.05155651949752382 ) ) ;
#18066=CARTESIAN_POINT ( 'NONE',  ( -5.693345022499886277, -3.000000000001474820, -71.09407784968050237 ) ) ;
#18092=PLANE ( 'NONE',  #92195 ) ;
#18107=PRESENTATION_STYLE_ASSIGNMENT (( #25144 ) ) ;
#18113=FILL_AREA_STYLE ('',( #36972 ) ) ;
#18128=CARTESIAN_POINT ( 'NONE',  ( 17.79338952166786569, 50.00000000000001421, 62.19549801434460790 ) ) ;
#18150=CARTESIAN_POINT ( 'NONE',  ( -5.378041831648492810, 41.50935559050609669, -58.55697846129572071 ) ) ;
#18169=ORIENTED_EDGE ( 'NONE', *, *, #648, .F. ) ;
#18171=STYLED_ITEM ( 'NONE', ( #84412 ), #64682 ) ;
#18175=DIRECTION ( 'NONE',  ( -0.000000000000000000, 1.000000000000000000, -0.000000000000000000 ) ) ;
#18192=CARTESIAN_POINT ( 'NONE',  ( -6.145467200823436116, 49.99999999999999289, -92.99666842290275781 ) ) ;
#18232=CARTESIAN_POINT ( 'NONE',  ( -6.733158593834142280, 41.46658730094299017, -70.54360490943875561 ) ) ;
#18239=B_SPLINE_CURVE_WITH_KNOTS ( 'NONE', 3,
 ( #99898, #26071, #48677, #74553, #40601, #81049, #33595, #66470, #25528, #49213, #23931, #17409, #58927, #15266, #89696, #48150, #7163, #41142, #73484, #72955, #105862, #32004, #15796, #32544, #64879, #81561, #24464, #106382, #65416, #57299, #98310 ),
 .UNSPECIFIED., .F., .F.,
 ( 4, 2, 2, 1, 1, 2, 2, 1, 2, 2, 2, 2, 1, 1, 2, 2, 2, 4 ),
 ( 0.000000000000000000, 0.05356300153016844284, 0.06695375191271055182, 0.08034450229525266773, 0.1071260030603368579, 0.1205167534428789461, 0.1339075038254210204, 0.1606890045905052244, 0.1874705053555893730, 0.2142520061206735493, 0.2410335068857577534, 0.2544242572682998693, 0.2678150076508419297, 0.2945965084159261060, 0.3079872587984681109, 0.3213780091810101158, 0.3749410107111783574, 0.4285040122413465991 ),
 .UNSPECIFIED. ) ;
#18303=( NAMED_UNIT ( * ) PLANE_ANGLE_UNIT ( ) SI_UNIT ( $, .RADIAN. ) );
#18308=B_SPLINE_CURVE_WITH_KNOTS ( 'NONE', 3,
 ( #88366, #62499, #21528, #46308 ),
 .UNSPECIFIED., .F., .F.,
 ( 4, 4 ),
 ( 0.000000000000000000, 1.000000000000000000 ),
 .UNSPECIFIED. ) ;
#18323=CARTESIAN_POINT ( 'NONE',  ( -7.996668423981801332, -3.000000000000002665, -78.85453280025087963 ) ) ;
#18343=COLOUR_RGB ( '', 0.72549020, 0.75294118, 0.79215686) ;
#18354=CARTESIAN_POINT ( 'NONE',  ( 9.920059540000885079, -3.000000000000002665, -96.33176891504291461 ) ) ;
#18372=CARTESIAN_POINT ( 'NONE',  ( -17.49999999999997513, 52.00000000000000711, 59.86364615470452577 ) ) ;
#18384=CARTESIAN_POINT ( 'NONE',  ( -5.668939695963768344, 41.88723863199725628, -59.02759498664629945 ) ) ;
#18391=CARTESIAN_POINT ( 'NONE',  ( -6.145467200824003662, -3.000000000000002665, -92.99666842290695001 ) ) ;
#18409=DIRECTION ( 'NONE',  ( 0.000000000000000000, 1.000000000000000000, 0.000000000000000000 ) ) ;
#18425=CARTESIAN_POINT ( 'NONE',  ( 6.931554132387847567, -4.999999999998125055, -71.13906995425121238 ) ) ;
#18438=CARTESIAN_POINT ( 'NONE',  ( -5.025684061874351016, -6.606954474312070502, -14.98089720656572688 ) ) ;
#18451=CARTESIAN_POINT ( 'NONE',  ( -7.130799806110275973, 41.48518899657568682, -59.01258712674732010 ) ) ;
#18452=FACE_OUTER_BOUND ( 'NONE', #96964, .T. ) ;
#18465=ORIENTED_EDGE ( 'NONE', *, *, #48848, .F. ) ;
#18468=CARTESIAN_POINT ( 'NONE',  ( 6.828042838857774299, 41.63841260098274688, -58.95291818684747653 ) ) ;
#18520=EDGE_CURVE ( 'NONE', #23955, #91293, #86764, .T. ) ;
#18542=CARTESIAN_POINT ( 'NONE',  ( -61.99911740321165610, 40.83832667049977516, -19.74839170142865541 ) ) ;
#18560=CARTESIAN_POINT ( 'NONE',  ( -9.739726766104316980, 49.99999999999999289, -87.61747884499031613 ) ) ;
#18578=CARTESIAN_POINT ( 'NONE',  ( 4.910934285265537547, 41.41789230214733664, -70.63711736860776114 ) ) ;
#18588=DIRECTION ( 'NONE',  ( 0.000000000000000000, 0.000000000000000000, 1.000000000000000000 ) ) ;
#18603=CARTESIAN_POINT ( 'NONE',  ( -17.68672840718395634, 45.00000000000000711, 62.88372900578075075 ) ) ;
#18638=( NAMED_UNIT ( * ) PLANE_ANGLE_UNIT ( ) SI_UNIT ( $, .RADIAN. ) );
#18647=STYLED_ITEM ( 'NONE', ( #10014 ), #40818 ) ;
#18651=CARTESIAN_POINT ( 'NONE',  ( 7.500000000000007105, -3.000000000000000000, -68.91429205785459544 ) ) ;
#18660=SURFACE_STYLE_FILL_AREA ( #18113 ) ;
#18671=COLOUR_RGB ( '', 0.40784314, 0.44705882, 0.49803922) ;
#18674=CARTESIAN_POINT ( 'NONE',  ( 17.51571489128689763, 50.00000000000000711, 63.27752882552535851 ) ) ;
#18693=CARTESIAN_POINT ( 'NONE',  ( -60.62677696746660416, 49.99999999999999289, 24.18439665019479179 ) ) ;
#18708=UNCERTAINTY_MEASURE_WITH_UNIT (LENGTH_MEASURE( 1.000000000000000082E-05 ), #90504, 'distance_accuracy_value', 'NONE');
#18729=EDGE_LOOP ( 'NONE', ( #71859, #89614, #95140, #45752 ) ) ;
#18732=VECTOR ( 'NONE', #38077, 1000.000000000000000 ) ;
#18743=CARTESIAN_POINT ( 'NONE',  ( -5.036189802309416486, 49.99999999999999289, -76.26213611588271135 ) ) ;
#18780=EDGE_CURVE ( 'NONE', #60267, #105843, #58470, .T. ) ;
#18823=VERTEX_POINT ( 'NONE', #34292 ) ;
#18834=CARTESIAN_POINT ( 'NONE',  ( -6.970005740671308736, 41.38563782891063880, -58.64823611141540027 ) ) ;
#18837=AXIS2_PLACEMENT_3D ( 'NONE', #37434, #13631, #95636 ) ;
#18849=CYLINDRICAL_SURFACE ( 'NONE', #14112, 9.999999999999994671 ) ;
#18851=CARTESIAN_POINT ( 'NONE',  ( -17.49999999999996803, 47.99999999999997868, 64.09949417230998847 ) ) ;
#18852=CARTESIAN_POINT ( 'NONE',  ( -90.56128410203886858, 42.00000000000000000, 11.85444436786840328 ) ) ;
#18863=CARTESIAN_POINT ( 'NONE',  ( -5.500000000000007994, 42.00000000000000000, -70.16688272716517361 ) ) ;
#18894=CARTESIAN_POINT ( 'NONE',  ( 49.01201108414410612, 48.00000000000000000, 43.00492839360018849 ) ) ;
#18919=DIRECTION ( 'NONE',  ( 0.000000000000000000, 1.000000000000000000, 0.000000000000000000 ) ) ;
#18943=CARTESIAN_POINT ( 'NONE',  ( 6.145467200819017428, -3.000000000000002665, -77.00333157708807619 ) ) ;
#18953=CARTESIAN_POINT ( 'NONE',  ( 7.811152745362717198, -4.332661967060489339, -16.03212449091516945 ) ) ;
#18973=CARTESIAN_POINT ( 'NONE',  ( 19.49977600865978289, 50.00000000000003553, 59.92175665475047452 ) ) ;
#19013=ADVANCED_FACE ( 'NONE', ( #78252 ), #103071, .T. ) ;
#19024=CARTESIAN_POINT ( 'NONE',  ( -11.68767211932356531, -5.000000000000002665, -81.85902538601600043 ) ) ;
#19026=UNCERTAINTY_MEASURE_WITH_UNIT (LENGTH_MEASURE( 1.000000000000000082E-05 ), #30713, 'distance_accuracy_value', 'NONE');
#19063=CARTESIAN_POINT ( 'NONE',  ( 4.707696486723893514, 49.99999999999999289, -99.43546650846349166 ) ) ;
#19079=ORIENTED_EDGE ( 'NONE', *, *, #79075, .F. ) ;
#19088=CARTESIAN_POINT ( 'NONE',  ( 23.70422451876635250, 42.00000000000004263, -88.20421627930062414 ) ) ;
#19095=CARTESIAN_POINT ( 'NONE',  ( 64.56046279400122501, 40.83886016323774726, -8.108302868572121014 ) ) ;
#19106=CARTESIAN_POINT ( 'NONE',  ( -8.087340429040079215, 41.99999999999999289, -69.98180430517560069 ) ) ;
#19114=CARTESIAN_POINT ( 'NONE',  ( 1.224646799147352073E-15, 49.99999999999999289, -75.00000000000001421 ) ) ;
#19139=CARTESIAN_POINT ( 'NONE',  ( -4.854898768586437541, 40.57568730855741990, -70.80100296729774811 ) ) ;
#19155=CARTESIAN_POINT ( 'NONE',  ( -17.54117848700256488, 45.00000000000000711, 63.36500943357729909 ) ) ;
#19176=CARTESIAN_POINT ( 'NONE',  ( -24.92095225878771458, 43.66054905306249623, -76.23935496511737142 ) ) ;
#19180=CARTESIAN_POINT ( 'NONE',  ( 0.000000000000000000, 0.000000000000000000, 0.000000000000000000 ) ) ;
#19207=CARTESIAN_POINT ( 'NONE',  ( 7.500000000000000000, -3.000000000000000000, -20.99851272547260095 ) ) ;
#19213=EDGE_CURVE ( 'NONE', #10685, #100984, #21260, .T. ) ;
#19219=FACE_OUTER_BOUND ( 'NONE', #40365, .T. ) ;
#19224=STYLED_ITEM ( 'NONE', ( #9516 ), #47680 ) ;
#19227=CARTESIAN_POINT ( 'NONE',  ( -9.574280356041013462, -5.000000000000002665, -20.99850713196553187 ) ) ;
#19237=CARTESIAN_POINT ( 'NONE',  ( -3.294249609603391082, -3.000000000000002665, -70.27378291343094929 ) ) ;
#19244=UNCERTAINTY_MEASURE_WITH_UNIT (LENGTH_MEASURE( 1.000000000000000082E-05 ), #68826, 'distance_accuracy_value', 'NONE');
#19250=DIRECTION ( 'NONE',  ( 0.000000000000000000, 1.000000000000000000, 0.000000000000000000 ) ) ;
#19253=FACE_OUTER_BOUND ( 'NONE', #89720, .T. ) ;
#19254=CARTESIAN_POINT ( 'NONE',  ( -28.89099332391479535, 50.00000000002003731, 58.53034795348396813 ) ) ;
#19274=CARTESIAN_POINT ( 'NONE',  ( 5.075566108724593128, -4.332661967060489339, -17.09624963492156269 ) ) ;
#19282=CARTESIAN_POINT ( 'NONE',  ( 32.85077815300981285, 40.72790403658980551, -62.46656677406199520 ) ) ;
#19287=VECTOR ( 'NONE', #8160, 1000.000000000000000 ) ;
#19296=FILL_AREA_STYLE ('',( #60256 ) ) ;
#19299=CARTESIAN_POINT ( 'NONE',  ( 6.043427762770655853, 50.00000000000000000, -74.51456333905269958 ) ) ;
#19345=ORIENTED_EDGE ( 'NONE', *, *, #27636, .F. ) ;
#19351=CARTESIAN_POINT ( 'NONE',  ( -14.75116209839011994, 43.55504285526384933, -90.22050492866908655 ) ) ;
#19379=CARTESIAN_POINT ( 'NONE',  ( -6.516859558828629773, 41.40454146154883830, -58.45803901209384179 ) ) ;
#19395=MECHANICAL_DESIGN_GEOMETRIC_PRESENTATION_REPRESENTATION('',(#102020),#15944);
#19397=CARTESIAN_POINT ( 'NONE',  ( 38.36535705883633796, 18.64316884711713840, 5.022013495247446890 ) ) ;
#19406=CARTESIAN_POINT ( 'NONE',  ( 7.026865755812575998, 41.28180827239863504, -58.57604196968413390 ) ) ;
#19423=( GEOMETRIC_REPRESENTATION_CONTEXT ( 3 ) GLOBAL_UNCERTAINTY_ASSIGNED_CONTEXT ( ( #60002 ) ) GLOBAL_UNIT_ASSIGNED_CONTEXT ( ( #2939, #43941, #27810 ) ) REPRESENTATION_CONTEXT ( 'NONE', 'WORKASPACE' ) );
#19488=CARTESIAN_POINT ( 'NONE',  ( -15.73927229776775150, -4.999999999999999112, -7.856667017201005798 ) ) ;
#19493=( GEOMETRIC_REPRESENTATION_CONTEXT ( 3 ) GLOBAL_UNCERTAINTY_ASSIGNED_CONTEXT ( ( #30564 ) ) GLOBAL_UNIT_ASSIGNED_CONTEXT ( ( #46710, #104407, #3611 ) ) REPRESENTATION_CONTEXT ( 'NONE', 'WORKASPACE' ) );
#19500=CARTESIAN_POINT ( 'NONE',  ( 52.56483885390523625, -79.93083296558610584, -38.23529411764706509 ) ) ;
#19514=SURFACE_STYLE_USAGE ( .BOTH. , #27601 ) ;
#19516=CARTESIAN_POINT ( 'NONE',  ( 4.205882352941162416, -4.999999999999998224, -72.69916451482997388 ) ) ;
#19526=CARTESIAN_POINT ( 'NONE',  ( -7.500000000000000000, -6.192646671729328922, -14.54134196042664229 ) ) ;
#19538=CARTESIAN_POINT ( 'NONE',  ( -7.425374667685089136, 41.07993512976541695, -59.67056295168852387 ) ) ;
#19539=CARTESIAN_POINT ( 'NONE',  ( 6.190137450539002550, 41.32597165365250191, -70.92513721826038875 ) ) ;
#19555=CARTESIAN_POINT ( 'NONE',  ( 12.48544000261163944, -3.553614324104685807, -13.69205050333947327 ) ) ;
#19556=CARTESIAN_POINT ( 'NONE',  ( -8.000000000000001776, -3.000000000000000444, 1.047197551196596077 ) ) ;
#19560=CARTESIAN_POINT ( 'NONE',  ( 11.99999999999999467, -5.000000000000002665, -86.57079632498522415 ) ) ;
#19584=CARTESIAN_POINT ( 'NONE',  ( 2.245730763532626462, 18.64284798592908032, 38.36507033181725035 ) ) ;
#19601=CARTESIAN_POINT ( 'NONE',  ( 8.904581707872910812, 48.00000000000000000, -97.29851715190937966 ) ) ;
#19626=CARTESIAN_POINT ( 'NONE',  ( -51.76085035121451483, 41.99999999999999289, -29.83308852628634966 ) ) ;
#19633=CARTESIAN_POINT ( 'NONE',  ( -64.12663816132096883, 40.83928107889916959, -11.02910957313798868 ) ) ;
#19635=VERTEX_POINT ( 'NONE', #75290 ) ;
#19650=CARTESIAN_POINT ( 'NONE',  ( -9.596002107488990518, 50.00000000000000000, -92.37456064098950037 ) ) ;
#19673=CARTESIAN_POINT ( 'NONE',  ( -5.548191825034886726, 40.55407105498441211, -71.04437881643139008 ) ) ;
#19687=CARTESIAN_POINT ( 'NONE',  ( -17.52413350827921690, 45.00000000000000000, 63.50693744801557017 ) ) ;
#19693=CARTESIAN_POINT ( 'NONE',  ( 17.50000000000002842, 46.00000000000000000, 64.09953197959339377 ) ) ;
#19708=DIRECTION ( 'NONE',  ( 0.000000000000000000, 1.000000000000000000, 0.000000000000000000 ) ) ;
#19729=CARTESIAN_POINT ( 'NONE',  ( 9.739726766683153514, 47.99999999999999289, -82.38252115640719353 ) ) ;
#19730=ADVANCED_FACE ( 'NONE', ( #19253 ), #39387, .T. ) ;
#19734=CARTESIAN_POINT ( 'NONE',  ( 9.739726766683153514, -3.000000000000002665, -87.61747884359279226 ) ) ;
#19736=CARTESIAN_POINT ( 'NONE',  ( -23.99113157947469332, 50.00000000000000000, -74.11764705882353610 ) ) ;
#19737=( NAMED_UNIT ( * ) PLANE_ANGLE_UNIT ( ) SI_UNIT ( $, .RADIAN. ) );
#19742=CARTESIAN_POINT ( 'NONE',  ( -6.434577627411612433, 41.95046723496767527, -59.72043439058787584 ) ) ;
#19756=EDGE_CURVE ( 'NONE', #78368, #71944, #93034, .T. ) ;
#19757=CARTESIAN_POINT ( 'NONE',  ( 10.50000000000000711, -5.000000000000000000, -77.33514508527181874 ) ) ;
#19779=CARTESIAN_POINT ( 'NONE',  ( 43.69716417795766006, 49.99999999997997691, 48.48761666245326296 ) ) ;
#19796=CARTESIAN_POINT ( 'NONE',  ( 17.50000000000002132, 45.90000000000000568, 64.09953197957062798 ) ) ;
#19799=CARTESIAN_POINT ( 'NONE',  ( 49.99533400023343432, 38.95362648028734043, -39.50304336076459322 ) ) ;
#19818=CARTESIAN_POINT ( 'NONE',  ( 9.596002107493083244, 50.00000000000000000, -92.37456064097861486 ) ) ;
#19833=CARTESIAN_POINT ( 'NONE',  ( -4.852941176470586093, 40.00000000000132871, -70.80672828634229177 ) ) ;
#19834=ORIENTED_EDGE ( 'NONE', *, *, #23013, .F. ) ;
#19862=CARTESIAN_POINT ( 'NONE',  ( -45.37589591933651434, 39.17805190087540979, -45.78237796162623141 ) ) ;
#19870=( LENGTH_UNIT ( ) NAMED_UNIT ( * ) SI_UNIT ( .MILLI., .METRE. ) );
#19877=PRODUCT_DEFINITION_FORMATION_WITH_SPECIFIED_SOURCE ( 'ANY', '', #84520, .NOT_KNOWN. ) ;
#19879=DIRECTION ( 'NONE',  ( -0.000000000000000000, 1.000000000000000000, -0.000000000000000000 ) ) ;
#19885=CARTESIAN_POINT ( 'NONE',  ( 11.69538631874992696, 50.00000000000001421, -88.12269504201513826 ) ) ;
#19899=CARTESIAN_POINT ( 'NONE',  ( -5.687763048235635388, 41.86978728324998400, -70.29636412762722841 ) ) ;
#19902=CARTESIAN_POINT ( 'NONE',  ( -14.78920111284466010, -5.000000000000000000, 7.149758979994854435 ) ) ;
#19903=CARTESIAN_POINT ( 'NONE',  ( -6.348225762706512398, 41.72645165896221897, -58.84140311374890331 ) ) ;
#19925=CARTESIAN_POINT ( 'NONE',  ( -52.56483885390523625, 48.00000000000000000, -38.23529411764706509 ) ) ;
#19926=CARTESIAN_POINT ( 'NONE',  ( 6.648506486173414665, 41.85229613648736091, -59.35075371410250256 ) ) ;
#19928=CARTESIAN_POINT ( 'NONE',  ( -57.69562748396144514, 41.99999999999999289, -15.50526908263377734 ) ) ;
#19931=EDGE_CURVE ( 'NONE', #72021, #93003, #40425, .T. ) ;
#19936=CARTESIAN_POINT ( 'NONE',  ( 6.661867388682258806, 41.56276662288188817, -58.70509931710797247 ) ) ;
#19950=ADVANCED_FACE ( 'NONE', ( #49287 ), #103753, .T. ) ;
#19972=CARTESIAN_POINT ( 'NONE',  ( 12.12626197893011515, -5.000000000000005329, -94.24800833403364209 ) ) ;
#20004=ORIENTED_EDGE ( 'NONE', *, *, #23013, .T. ) ;
#20020=B_SPLINE_CURVE_WITH_KNOTS ( 'NONE', 3,
 ( #50416, #17019, #49894, #83326, #1866, #8903, #41804, #34824 ),
 .UNSPECIFIED., .F., .F.,
 ( 4, 2, 2, 4 ),
 ( 0.000000000000000000, 0.5000000000000000000, 0.7500000000000000000, 1.000000000000000000 ),
 .UNSPECIFIED. ) ;
#20024=CARTESIAN_POINT ( 'NONE',  ( -7.157960986248002477, -5.000000000000000000, -14.69147069243657100 ) ) ;
#20045=CARTESIAN_POINT ( 'NONE',  ( 19.49193093582640302, 49.99898248078959284, 60.07857787404169159 ) ) ;
#20046=B_SPLINE_CURVE_WITH_KNOTS ( 'NONE', 3,
 ( #98832, #22874, #57841, #32556, #47629, #39576, #90768, #80531, #6648, #56784, #72450, #81062, #7701, #49765, #82669, #11416, #52413, #100973, #66480, #2805, #99357, #42741, #77236, #67562, #93431, #10885, #43799, #85331, #75633, #100444, #27132, #51883, #19584, #101512 ),
 .UNSPECIFIED., .F., .F.,
 ( 4, 2, 2, 2, 2, 2, 2, 2, 2, 2, 2, 2, 2, 2, 2, 2, 4 ),
 ( 0.000000000000000000, 0.03124999999999548625, 0.06249999999999097250, 0.09374999999998642752, 0.1249999999999818895, 0.1562499999999773237, 0.1874999999999727995, 0.2187499999999682476, 0.2499999999999637235, 0.2812499999999591993, 0.3124999999999546474, 0.3437499999999502065, 0.3749999999999456546, 0.4062499999999411582, 0.4374999999999366063, 0.4687499999999321654, 0.4999999999999275579 ),
 .UNSPECIFIED. ) ;
#20057=CARTESIAN_POINT ( 'NONE',  ( -5.369174336198356379, 44.20122194677738037, -60.96850753999265748 ) ) ;
#20064=DIRECTION ( 'NONE',  ( 0.000000000000000000, -1.000000000000000000, 0.000000000000000000 ) ) ;
#20070=CARTESIAN_POINT ( 'NONE',  ( -19.33400676013704000, 49.88855074631516828, 61.23237481859990794 ) ) ;
#20072=CARTESIAN_POINT ( 'NONE',  ( 6.280866958221838381, 40.29318264226383661, -71.19386870237659082 ) ) ;
#20087=CARTESIAN_POINT ( 'NONE',  ( 5.248477453467016218, 10.42489023671462611, -30.57443130249296459 ) ) ;
#20093=CARTESIAN_POINT ( 'NONE',  ( 3.140974613990258568, -5.000000000000002665, -73.31232788067565309 ) ) ;
#20095=( NAMED_UNIT ( * ) PLANE_ANGLE_UNIT ( ) SI_UNIT ( $, .RADIAN. ) );
#20138=VECTOR ( 'NONE', #84234, 1000.000000000000000 ) ;
#20163=CARTESIAN_POINT ( 'NONE',  ( -59.26346722528342781, 40.83785626851633310, 26.86426695247594409 ) ) ;
#20183=CARTESIAN_POINT ( 'NONE',  ( 10.48543666094731996, 50.00000000000000000, -91.04342776276723725 ) ) ;
#20207=CARTESIAN_POINT ( 'NONE',  ( -6.097206778545145589, 40.29241581810332207, -71.16079338543529786 ) ) ;
#20222=CARTESIAN_POINT ( 'NONE',  ( -17.51626200557882029, 45.00000000000000711, 63.59143666326379218 ) ) ;
#20258=CARTESIAN_POINT ( 'NONE',  ( 11.04679971567022712, -4.985848584336745937, -12.57695644737852092 ) ) ;
#20280=CARTESIAN_POINT ( 'NONE',  ( -5.947849941369417692, 41.98179909877737259, -59.44139789967899645 ) ) ;
#20285=CARTESIAN_POINT ( 'NONE',  ( 7.500000000000007105, 25.66666666666802854, -68.91429205785459544 ) ) ;
#20292=CARTESIAN_POINT ( 'NONE',  ( 17.50837830432311293, 50.00000000000002132, 63.40454194101801022 ) ) ;
#20317=SURFACE_STYLE_FILL_AREA ( #60214 ) ;
#20320=CARTESIAN_POINT ( 'NONE',  ( 6.101170550526181735, 41.83126063020969099, -70.32427471769284466 ) ) ;
#20321=CARTESIAN_POINT ( 'NONE',  ( -54.34415824576156950, 50.00000000000000000, -32.38913437803946493 ) ) ;
#20355=SURFACE_STYLE_FILL_AREA ( #95780 ) ;
#20360=( NAMED_UNIT ( * ) SI_UNIT ( $, .STERADIAN. ) SOLID_ANGLE_UNIT ( ) );
#20364=CARTESIAN_POINT ( 'NONE',  ( -1.570796324980112679, 50.00000000000000000, -97.00000000000000000 ) ) ;
#20403=FACE_OUTER_BOUND ( 'NONE', #27021, .T. ) ;
#20417=LINE ( 'NONE', #3108, #78379 ) ;
#20422=CARTESIAN_POINT ( 'NONE',  ( 10.51296777078104050, 50.00000000000000000, -92.64705882352942012 ) ) ;
#20428=CARTESIAN_POINT ( 'NONE',  ( 11.99986829839305535, 50.00000000000000711, -86.59063654372916119 ) ) ;
#20443=CARTESIAN_POINT ( 'NONE',  ( -6.159997634473088013, 41.93068719192066141, -70.02314903893139331 ) ) ;
#20445=CARTESIAN_POINT ( 'NONE',  ( 0.000000000000000000, 50.00000000000000000, 0.000000000000000000 ) ) ;
#20450=CARTESIAN_POINT ( 'NONE',  ( -6.373568580003205142, 41.63985673647684393, -58.70717887382906497 ) ) ;
#20467=CARTESIAN_POINT ( 'NONE',  ( 0.000000000000000000, 0.000000000000000000, 0.000000000000000000 ) ) ;
#20470=CARTESIAN_POINT ( 'NONE',  ( -1.233923992984923027E-14, 18.64316884711714195, -38.36535705883633085 ) ) ;
#20481=CARTESIAN_POINT ( 'NONE',  ( -5.500000000000006217, 42.00000000000000000, -59.28631038546422616 ) ) ;
#20498=CARTESIAN_POINT ( 'NONE',  ( -12.44963615905739474, -4.333246069852321192, -12.76855431059839141 ) ) ;
#20507=CARTESIAN_POINT ( 'NONE',  ( -12.13034742782246767, 42.00000000000000000, -93.82352941176338845 ) ) ;
#20552=SURFACE_SIDE_STYLE ('',( #94387 ) ) ;
#20571=ORIENTED_EDGE ( 'NONE', *, *, #99508, .T. ) ;
#20594=CARTESIAN_POINT ( 'NONE',  ( 19.48812817077294923, 49.99803169766527589, 60.15118601806505438 ) ) ;
#20605=CARTESIAN_POINT ( 'NONE',  ( -7.500000000000007105, 44.29449649216757479, -60.86453129175313137 ) ) ;
#20611=EDGE_CURVE ( 'NONE', #8947, #25938, #69430, .T. ) ;
#20615=CARTESIAN_POINT ( 'NONE',  ( -18.92793431205891608, 49.05858063650561007, 62.10525169381176624 ) ) ;
#20616=CARTESIAN_POINT ( 'NONE',  ( 6.654387246717901050, 41.27136532114669620, -70.82047233385743823 ) ) ;
#20632=CARTESIAN_POINT ( 'NONE',  ( -4.028951842967198438, -3.000000000000000444, 6.990291106834060741 ) ) ;
#20636=STYLED_ITEM ( 'NONE', ( #90594 ), #33641 ) ;
#20650=( BOUNDED_SURFACE ( )  B_SPLINE_SURFACE ( 2, 3, ( 
 ( #918, #98063, #24214, #57585, #57064, #55984, #82950, #8518 ),
 ( #9045, #73781, #74315, #89457, #74837, #33358, #88921, #15014 ),
 ( #6926, #39848, #15551, #72720, #105622, #31762, #64643, #97515 ) ),
 .UNSPECIFIED., .F., .F., .F. ) 
 B_SPLINE_SURFACE_WITH_KNOTS ( ( 3, 3 ),
 ( 4, 2, 2, 4 ),
 ( 0.000000000000000000, 1.000000000000000000 ),
 ( -0.06656819121499020497, -0.06329489543879425473, 0.001517242213116292218, 0.005444315861320835753 ),
 .UNSPECIFIED. ) 
 GEOMETRIC_REPRESENTATION_ITEM ( )  RATIONAL_B_SPLINE_SURFACE ( (
 ( 1.000000000000000000, 1.000000000000000000, 1.000000000000000000, 1.000000000000000000, 1.000000000000000000, 1.000000000000000000, 1.000000000000000000, 1.000000000000000000),
 ( 1.857142857142858317, 1.857142857142858317, 1.857142857142858317, 1.857142857142858317, 1.857142857142858317, 1.857142857142858317, 1.857142857142858317, 1.857142857142858317),
 ( 1.000000000000000000, 1.000000000000000000, 1.000000000000000000, 1.000000000000000000, 1.000000000000000000, 1.000000000000000000, 1.000000000000000000, 1.000000000000000000) ) ) 
 REPRESENTATION_ITEM ( '' )  SURFACE ( )  );
#20657=CARTESIAN_POINT ( 'NONE',  ( -12.49955057333833253, -4.332870170146376765, -12.71907580221295220 ) ) ;
#20672=CARTESIAN_POINT ( 'NONE',  ( 10.51296777078104050, 50.00000000000000000, -92.64705882352942012 ) ) ;
#20675=EDGE_CURVE ( 'NONE', #89440, #96838, #8326, .T. ) ;
#20686=CARTESIAN_POINT ( 'NONE',  ( 43.91139751470105779, 41.39507865991506463, -50.13180910527601242 ) ) ;
#20695=DIRECTION ( 'NONE',  ( 0.000000000000000000, 0.000000000000000000, -1.000000000000000000 ) ) ;
#20698=CARTESIAN_POINT ( 'NONE',  ( -10.04205104288555184, 18.64316884714294886, -37.36680950593608230 ) ) ;
#20700=AXIS2_PLACEMENT_3D ( 'NONE', #91583, #34439, #41949 ) ;
#20706=CARTESIAN_POINT ( 'NONE',  ( -23.30905507870230053, 39.42442235840471909, 60.74964960281029391 ) ) ;
#20724=CARTESIAN_POINT ( 'NONE',  ( -11.68767211932355465, 50.00000000000000000, -88.14097461399492772 ) ) ;
#20738=CARTESIAN_POINT ( 'NONE',  ( 7.036764705882352366, 40.00000000373363207, -71.06385277390853616 ) ) ;
#20740=PRESENTATION_STYLE_ASSIGNMENT (( #78907 ) ) ;
#20748=CARTESIAN_POINT ( 'NONE',  ( -6.122245915141247607, 40.00000000007563727, -71.16543060730309378 ) ) ;
#20760=CARTESIAN_POINT ( 'NONE',  ( -17.59874102159060527, 44.99999999999999289, 63.10646976788801510 ) ) ;
#20780=CARTESIAN_POINT ( 'NONE',  ( 7.182275720338873626, 41.30104542284085767, -58.77094221306448674 ) ) ;
#20781=FACE_OUTER_BOUND ( 'NONE', #58274, .T. ) ;
#20786=CARTESIAN_POINT ( 'NONE',  ( 5.268008033849937100, 13.26688624804745587, -33.14867888032319598 ) ) ;
#20787=B_SPLINE_CURVE_WITH_KNOTS ( 'NONE', 3,
 ( #60506, #62100, #77734, #12442, #69641, #21129, #102534, #94992, #20615, #45892, #12968, #11916, #86376, #4364, #93391, #2761, #69120, #53958, #3305, #51845, #78770, #45369, #78251, #37835, #100929, #85285, #68590, #27090, #35712, #43758, #85842, #59976, #76650, #52374, #11373, #44300, #77194, #101993, #28151, #61027, #93914, #20070, #52918, #44845, #30795, #104643, #5938, #7003, #55014, #96039, #103590, #79833, #97080, #87946, #38354, #39923, #6469, #49993, #96568, #17117, #31842, #13499, #22703, #87425, #55540, #31328, #46422 ),
 .UNSPECIFIED., .F., .F.,
 ( 4, 2, 2, 2, 2, 1, 2, 2, 2, 2, 2, 2, 1, 1, 2, 2, 2, 2, 1, 2, 2, 2, 2, 1, 1, 2, 2, 2, 2, 1, 1, 1, 2, 2, 2, 2, 2, 4 ),
 ( 0.000000000000000000, 0.06249999999989476474, 0.1249999999997895295, 0.1874999999996843081, 0.2187499999996354583, 0.2343749999996066202, 0.2421874999995970723, 0.2499999999995875521, 0.3124999999995375921, 0.3437499999995161093, 0.3749999999994946265, 0.4374999999994517164, 0.4687499999994302335, 0.4843749999994252375, 0.4921874999994257927, 0.4999999999994263478, 0.5624999999994299005, 0.5937499999994316768, 0.6093749999994333422, 0.6171874999994354516, 0.6249999999994374500, 0.6874999999994867439, 0.7187499999995128341, 0.7343749999995256017, 0.7421874999995317079, 0.7460937499995344835, 0.7499999999995371480, 0.8124999999995893285, 0.8437499999996155298, 0.8593749999996311839, 0.8671874999996388445, 0.8710937499996425082, 0.8730468749996473932, 0.8749999999996523892, 0.9062499999997443156, 0.9218749999997882805, 0.9374999999998322453, 1.000000000000000000 ),
 .UNSPECIFIED. ) ;
#20794=CARTESIAN_POINT ( 'NONE',  ( 11.11385657980845032, -4.981498555758606450, -12.57747955902696546 ) ) ;
#20802=CARTESIAN_POINT ( 'NONE',  ( 3.490407211888509836E-12, -4.332980043422162808, 17.83347932686506354 ) ) ;
#20813=CARTESIAN_POINT ( 'NONE',  ( -43.69716417793774355, 49.99999999999999289, 48.48761666241306756 ) ) ;
#20818=CARTESIAN_POINT ( 'NONE',  ( -5.916007711650134837, 41.94280317611644193, -59.21688531701510527 ) ) ;
#20826=ORIENTED_EDGE ( 'NONE', *, *, #53764, .F. ) ;
#20828=CARTESIAN_POINT ( 'NONE',  ( 18.82063668069593376, 49.99999999999999289, 60.82877375281272236 ) ) ;
#20834=( GEOMETRIC_REPRESENTATION_CONTEXT ( 3 ) GLOBAL_UNCERTAINTY_ASSIGNED_CONTEXT ( ( #62844 ) ) GLOBAL_UNIT_ASSIGNED_CONTEXT ( ( #21511, #11782, #85154 ) ) REPRESENTATION_CONTEXT ( 'NONE', 'WORKASPACE' ) );
#20840=CARTESIAN_POINT ( 'NONE',  ( 41.05732475771431211, 50.00000000000000711, 48.04410276558757431 ) ) ;
#20849=CARTESIAN_POINT ( 'NONE',  ( 6.639655237817898126, 41.83126053442604331, -69.93930111382492498 ) ) ;
#20855=ORIENTED_EDGE ( 'NONE', *, *, #55828, .F. ) ;
#20863=ORIENTED_EDGE ( 'NONE', *, *, #25458, .T. ) ;
#20873=CARTESIAN_POINT ( 'NONE',  ( 25.89378858170335462, 41.47439130909162941, -71.76338141261258841 ) ) ;
#20892=CARTESIAN_POINT ( 'NONE',  ( -6.145467200826166376, 48.00000000000000000, -92.99666842290478996 ) ) ;
#20918=CARTESIAN_POINT ( 'NONE',  ( -5.363597346089342466, 41.33266196706077267, -58.39526881795508473 ) ) ;
#20931=CARTESIAN_POINT ( 'NONE',  ( -17.52435683634852737, 50.00000000000000000, 63.16488839464014404 ) ) ;
#20932=CARTESIAN_POINT ( 'NONE',  ( 7.500000000000000888, -3.000671055698259870, -20.99923901233272971 ) ) ;
#20938=SURFACE_STYLE_FILL_AREA ( #62942 ) ;
#20940=( BOUNDED_SURFACE ( )  B_SPLINE_SURFACE ( 2, 3, ( 
 ( #40036, #39521, #88591, #72396 ),
 ( #29331, #104226, #5022, #56181 ),
 ( #70815, #6588, #62732, #31445 ) ),
 .UNSPECIFIED., .F., .F., .F. ) 
 B_SPLINE_SURFACE_WITH_KNOTS ( ( 3, 3 ),
 ( 4, 4 ),
 ( 0.000000000000000000, 1.000000000000000000 ),
 ( 0.000000000000000000, 0.003049892549641993172 ),
 .UNSPECIFIED. ) 
 GEOMETRIC_REPRESENTATION_ITEM ( )  RATIONAL_B_SPLINE_SURFACE ( (
 ( 1.000000000000000000, 1.000000000000000000, 1.000000000000000000, 1.000000000000000000),
 ( 1.857142857142858317, 1.857142857142858317, 1.857142857142858317, 1.857142857142858317),
 ( 1.000000000000000000, 1.000000000000000000, 1.000000000000000000, 1.000000000000000000) ) ) 
 REPRESENTATION_ITEM ( '' )  SURFACE ( )  );
#20945=B_SPLINE_CURVE_WITH_KNOTS ( 'NONE', 3,
 ( #49825, #64439, #55771, #31556, #88706, #80593, #89241, #40144, #97313, #23465, #81640, #73558 ),
 .UNSPECIFIED., .F., .F.,
 ( 4, 2, 2, 2, 2, 4 ),
 ( 0.04761886307670518126, 0.05150820645496530931, 0.05539754983322543735, 0.06317623658974569345, 0.07095492334626596342, 0.07873361010278621952 ),
 .UNSPECIFIED. ) ;
#20947=SURFACE_STYLE_USAGE ( .BOTH. , #5244 ) ;
#20949=CARTESIAN_POINT ( 'NONE',  ( -12.84929146819454182, 42.47186473153507080, -92.83514476613449062 ) ) ;
#20966=FILL_AREA_STYLE_COLOUR ( '', #22097 ) ;
#20967=CARTESIAN_POINT ( 'NONE',  ( -5.041270137995550904, 41.82074860089117152, -70.25592743835888143 ) ) ;
#20972=CARTESIAN_POINT ( 'NONE',  ( -10.49999999997808331, -5.000000000000000000, -12.52300748972991506 ) ) ;
#20973=CARTESIAN_POINT ( 'NONE',  ( -6.228838570019490817, 41.78908843073880774, -58.91793930065269791 ) ) ;
#20991=CARTESIAN_POINT ( 'NONE',  ( -33.52312678239033517, 18.64316884709848665, 19.32152200342503079 ) ) ;
#20996=ORIENTED_EDGE ( 'NONE', *, *, #85794, .F. ) ;
#21011=STYLED_ITEM ( 'NONE', ( #80918 ), #51131 ) ;
#21023=( NAMED_UNIT ( * ) SI_UNIT ( $, .STERADIAN. ) SOLID_ANGLE_UNIT ( ) );
#21039=CARTESIAN_POINT ( 'NONE',  ( -2.384812152908770244, -5.000000000000002665, -98.00000000000000000 ) ) ;
#21061=FACE_OUTER_BOUND ( 'NONE', #38925, .T. ) ;
#21080=CARTESIAN_POINT ( 'NONE',  ( 12.10102349785733544, -5.000000000000000000, 11.47683805494732390 ) ) ;
#21082=VERTEX_POINT ( 'NONE', #68594 ) ;
#21105=CARTESIAN_POINT ( 'NONE',  ( 18.94735611194717606, 49.28911315852006680, 62.03557990934028510 ) ) ;
#21129=CARTESIAN_POINT ( 'NONE',  ( -18.92118552154158806, 48.85453644119221650, 62.14239264200793400 ) ) ;
#21130=CARTESIAN_POINT ( 'NONE',  ( 6.743821559472605642, 40.92373752580943602, -71.01439591878522606 ) ) ;
#21133=CARTESIAN_POINT ( 'NONE',  ( 12.50000000000000711, -3.000000000000000000, -78.42624373368740009 ) ) ;
#21143=CARTESIAN_POINT ( 'NONE',  ( 5.224631516565895417, 7.366007320495609356, -27.80123404716705693 ) ) ;
#21148=CARTESIAN_POINT ( 'NONE',  ( 6.145467200816499442, -5.000000000008177459, -92.99666842292330671 ) ) ;
#21172=LINE ( 'NONE', #70209, #44207 ) ;
#21196=CARTESIAN_POINT ( 'NONE',  ( -5.075741750048029743, -4.332638003024074536, -17.09621982684887698 ) ) ;
#21200=VERTEX_POINT ( 'NONE', #87953 ) ;
#21207=CARTESIAN_POINT ( 'NONE',  ( 57.69562748396959506, 41.99999999991776178, -15.50526908263404735 ) ) ;
#21210=ADVANCED_FACE ( 'NONE', ( #22172 ), #33514, .T. ) ;
#21213=ORIENTED_EDGE ( 'NONE', *, *, #60902, .F. ) ;
#21215=CARTESIAN_POINT ( 'NONE',  ( 62.40461286002861385, 39.42532709582792450, 18.42694020216206496 ) ) ;
#21244=CARTESIAN_POINT ( 'NONE',  ( -9.999999999999996447, 48.00000000000000711, -83.69100306100429520 ) ) ;
#21245=CARTESIAN_POINT ( 'NONE',  ( 6.831787912114839934, -4.999999999999999112, -15.36996511329311588 ) ) ;
#21248=CARTESIAN_POINT ( 'NONE',  ( -4.852941176470598528, -3.000000000000002665, -70.80672828634229177 ) ) ;
#21255=( BOUNDED_CURVE ( )  B_SPLINE_CURVE ( 2, ( #99394, #154, #40650 ),
 .UNSPECIFIED., .F., .F. ) 
 B_SPLINE_CURVE_WITH_KNOTS ( ( 3, 3 ),
 ( 0.000000000000000000, 1.000000000000000000 ),
 .UNSPECIFIED. ) 
 CURVE ( )  GEOMETRIC_REPRESENTATION_ITEM ( )  RATIONAL_B_SPLINE_CURVE ( ( 1.000000000000000000, 1.857142857142858317, 1.000000000000000000 ) ) 
 REPRESENTATION_ITEM ( '' )  );
#21257=CARTESIAN_POINT ( 'NONE',  ( -6.040019051097406333, 40.93519689175381870, -71.09856422274093291 ) ) ;
#21260=B_SPLINE_CURVE_WITH_KNOTS ( 'NONE', 3,
 ( #2053, #34999, #957, #17203 ),
 .UNSPECIFIED., .F., .F.,
 ( 4, 4 ),
 ( 0.000000000000000000, 1.000000000000000000 ),
 .UNSPECIFIED. ) ;
#21278=CARTESIAN_POINT ( 'NONE',  ( -12.50000000000000355, 27.06290442698209020, -44.59571028169377627 ) ) ;
#21286=CARTESIAN_POINT ( 'NONE',  ( 6.913779129928547817, 41.73441125232163529, -59.30275354417914713 ) ) ;
#21294=CARTESIAN_POINT ( 'NONE',  ( 7.500000000000003553, 11.93422428098184263, -34.62196993281244062 ) ) ;
#21313=CARTESIAN_POINT ( 'NONE',  ( 9.999999999999998224, -3.000000000000002665, -83.69100306100429520 ) ) ;
#21317=CARTESIAN_POINT ( 'NONE',  ( -11.54772599577038505, 50.00000000000000000, 62.20121126512094634 ) ) ;
#21323=CARTESIAN_POINT ( 'NONE',  ( -5.448357726063037809, 41.97585548067615235, -59.38396255182521344 ) ) ;
#21326=CARTESIAN_POINT ( 'NONE',  ( 11.33049201284865859, -4.963977770831442982, -77.06423821557504539 ) ) ;
#21333=CARTESIAN_POINT ( 'NONE',  ( 18.12552907611484443, 50.00000000000002132, 61.72817625373181016 ) ) ;
#21342=CARTESIAN_POINT ( 'NONE',  ( 37.18367258770028627, 50.00000000000001421, 51.09969904534472107 ) ) ;
#21348=CARTESIAN_POINT ( 'NONE',  ( 7.500000000000006217, 39.99999999999942446, -59.88032989331673406 ) ) ;
#21355=CARTESIAN_POINT ( 'NONE',  ( 7.149999999999997691, 41.65000000000000568, -59.82695526683420439 ) ) ;
#21356=LINE ( 'NONE', #14273, #18732 ) ;
#21365=UNCERTAINTY_MEASURE_WITH_UNIT (LENGTH_MEASURE( 1.000000000000000082E-05 ), #63511, 'distance_accuracy_value', 'NONE');
#21394=CARTESIAN_POINT ( 'NONE',  ( -1.308996937483426715, 48.00000000000000000, -95.00000000000000000 ) ) ;
#21431=CARTESIAN_POINT ( 'NONE',  ( -18.83603686460278936, 49.99999999999999289, 60.80789323821156955 ) ) ;
#21469=VERTEX_POINT ( 'NONE', #47347 ) ;
#21471=FACE_OUTER_BOUND ( 'NONE', #90200, .T. ) ;
#21472=CARTESIAN_POINT ( 'NONE',  ( -6.074379036182786962, 41.75280167827273203, -70.48890184034459594 ) ) ;
#21473=STYLED_ITEM ( 'NONE', ( #28045 ), #16884 ) ;
#21477=CARTESIAN_POINT ( 'NONE',  ( -14.68326754034733739, -5.000000000000000888, -7.357674878908997407 ) ) ;
#21478=CARTESIAN_POINT ( 'NONE',  ( -5.373715199254561981, 41.43915796864546053, -58.48990672293015081 ) ) ;
#21496=CARTESIAN_POINT ( 'NONE',  ( 6.731699451537835444, 41.74873278439808644, -59.11937199553665323 ) ) ;
#21497=CARTESIAN_POINT ( 'NONE',  ( 29.83308852632731245, 41.99999999995888089, 51.76085035125569789 ) ) ;
#21511=( LENGTH_UNIT ( ) NAMED_UNIT ( * ) SI_UNIT ( .MILLI., .METRE. ) );
#21528=CARTESIAN_POINT ( 'NONE',  ( 15.41108395495531269, 43.84921856205087209, -89.31326237052935824 ) ) ;
#21545=CARTESIAN_POINT ( 'NONE',  ( -11.46641754970919358, -5.000000000000002665, -75.26692388747306950 ) ) ;
#21619=CARTESIAN_POINT ( 'NONE',  ( 19.01543600231714493, 49.53930566124419244, 61.88648251802599987 ) ) ;
#21638=EDGE_LOOP ( 'NONE', ( #67416, #54472, #62585, #18465 ) ) ;
#21644=CARTESIAN_POINT ( 'NONE',  ( 5.255459937908828927, 41.40616594607992340, -70.76123423727798922 ) ) ;
#21664=CARTESIAN_POINT ( 'NONE',  ( -2.617478844992371823, -5.000000000000002665, -75.26027323389158141 ) ) ;
#21681=CARTESIAN_POINT ( 'NONE',  ( -34.53113281790295019, 42.66782721010052626, -63.02754100881575994 ) ) ;
#21685=VERTEX_POINT ( 'NONE', #27781 ) ;
#21694=CARTESIAN_POINT ( 'NONE',  ( 9.742892617412987732, -5.000000000000000000, -2.583889972060940288 ) ) ;
#21697=FILL_AREA_STYLE_COLOUR ( '', #26886 ) ;
#21700=CARTESIAN_POINT ( 'NONE',  ( -5.693345022499886277, -3.000000000001474820, -71.09407784968050237 ) ) ;
#21708=CARTESIAN_POINT ( 'NONE',  ( -42.31627492074115793, 39.52091083735819410, -49.87351597195841890 ) ) ;
#21717=CARTESIAN_POINT ( 'NONE',  ( 43.57271197750083758, 41.43538979188361537, -50.59742473857805578 ) ) ;
#21728=CARTESIAN_POINT ( 'NONE',  ( -19.32152200341433357, 18.64316884707570310, 33.52312678237270660 ) ) ;
#21735=CARTESIAN_POINT ( 'NONE',  ( 64.12441025417933815, 39.42592377905895518, -11.04313413768638164 ) ) ;
#21737=AXIS2_PLACEMENT_3D ( 'NONE', #50256, #100399, #75044 ) ;
#21756=CARTESIAN_POINT ( 'NONE',  ( 7.996668422908976837, 49.99999999999999289, -78.85453279918145597 ) ) ;
#21768=CARTESIAN_POINT ( 'NONE',  ( 9.310717075081306859, -4.999999999999999112, -18.36753075048013528 ) ) ;
#21804=CARTESIAN_POINT ( 'NONE',  ( -12.50000000000000355, 27.16932851130122728, -44.70834376557844791 ) ) ;
#21825=CARTESIAN_POINT ( 'NONE',  ( 7.500000000006690648, 42.38482959929934424, -59.14603436866633501 ) ) ;
#21847=CARTESIAN_POINT ( 'NONE',  ( 65.26738680894031575, 49.99999999999999289, 0.8120011905333047730 ) ) ;
#21860=CARTESIAN_POINT ( 'NONE',  ( 18.81234315776984900, 49.99999999999999289, 60.84005166012197208 ) ) ;
#21870=CARTESIAN_POINT ( 'NONE',  ( 3.733178250754431993, 42.00000000000000000, -68.31018313526459451 ) ) ;
#21872=CARTESIAN_POINT ( 'NONE',  ( 47.93998421967890522, 50.00000000000002132, 40.89468907122802221 ) ) ;
#21912=VERTEX_POINT ( 'NONE', #81788 ) ;
#21914=( NAMED_UNIT ( * ) PLANE_ANGLE_UNIT ( ) SI_UNIT ( $, .RADIAN. ) );
#21920=CARTESIAN_POINT ( 'NONE',  ( -7.996668422906947349, 48.00000000000000000, -78.85453279917602742 ) ) ;
#21936=SURFACE_STYLE_FILL_AREA ( #95807 ) ;
#21941=CARTESIAN_POINT ( 'NONE',  ( 0.000000000000000000, -5.000000000000000000, 10.00000000000000000 ) ) ;
#21948=SURFACE_SIDE_STYLE ('',( #46722 ) ) ;
#21960=CARTESIAN_POINT ( 'NONE',  ( -17.82614187044788778, 49.99999999999999289, 62.13962658379361415 ) ) ;
#21977=( NAMED_UNIT ( * ) PLANE_ANGLE_UNIT ( ) SI_UNIT ( $, .RADIAN. ) );
#21986=CARTESIAN_POINT ( 'NONE',  ( 7.125691916903466705, 41.67430808309654822, -69.26730091920677523 ) ) ;
#21991=ORIENTED_EDGE ( 'NONE', *, *, #81424, .F. ) ;
#21996=EDGE_CURVE ( 'NONE', #57839, #45703, #47967, .T. ) ;
#21999=CARTESIAN_POINT ( 'NONE',  ( -6.241999136123610015, 41.80321047224195041, -70.33316275629502456 ) ) ;
#22018=ORIENTED_EDGE ( 'NONE', *, *, #52450, .T. ) ;
#22021=CARTESIAN_POINT ( 'NONE',  ( 6.364221311682587867, 41.95991762558126936, -59.61869606621115736 ) ) ;
#22097=COLOUR_RGB ( '', 0.08235294, 0.09019608, 0.10196078) ;
#22116=CARTESIAN_POINT ( 'NONE',  ( 16.49565406582141947, -5.000000000000000000, 2.458857127971515233 ) ) ;
#22141=CARTESIAN_POINT ( 'NONE',  ( 18.92236309988041043, 48.94305489900515482, 62.13249689941736165 ) ) ;
#22165=CARTESIAN_POINT ( 'NONE',  ( -6.503415501679381983, 41.93912328290132052, -68.91429205811094505 ) ) ;
#22172=FACE_OUTER_BOUND ( 'NONE', #3653, .T. ) ;
#22190=CARTESIAN_POINT ( 'NONE',  ( 2.617478844992707110, -5.000000000000015099, -94.73972676610841859 ) ) ;
#22201=CARTESIAN_POINT ( 'NONE',  ( 7.261743840240279191, -3.634783834950141124, -18.04052776595507268 ) ) ;
#22203=CARTESIAN_POINT ( 'NONE',  ( -11.69514296590995706, 50.00000000000000000, -88.12259424196773239 ) ) ;
#22204=CARTESIAN_POINT ( 'NONE',  ( -25.50394049119971740, 43.61918368478458774, -75.43787865382840607 ) ) ;
#22224=( NAMED_UNIT ( * ) PLANE_ANGLE_UNIT ( ) SI_UNIT ( $, .RADIAN. ) );
#22235=CARTESIAN_POINT ( 'NONE',  ( -46.21205304293484062, 39.15065308173836200, -44.64295635327282241 ) ) ;
#22242=( NAMED_UNIT ( * ) SI_UNIT ( $, .STERADIAN. ) SOLID_ANGLE_UNIT ( ) );
#22246=CARTESIAN_POINT ( 'NONE',  ( 39.06570142950455704, 42.03544815418795366, -56.79353983682526774 ) ) ;
#22248=CARTESIAN_POINT ( 'NONE',  ( 5.500000036871884213, 42.00000000000000000, -68.91429207046176941 ) ) ;
#22256=CARTESIAN_POINT ( 'NONE',  ( 15.50526908265481296, 41.99999999991779731, -57.69562748401063601 ) ) ;
#22263=CARTESIAN_POINT ( 'NONE',  ( -20.51735722783412541, 39.42506220197849132, 61.74843859600010632 ) ) ;
#22282=CARTESIAN_POINT ( 'NONE',  ( 8.737863884120029567, 49.99999999999999289, -79.96381019768851672 ) ) ;
#22289=ORIENTED_EDGE ( 'NONE', *, *, #12483, .F. ) ;
#22323=CARTESIAN_POINT ( 'NONE',  ( -18.91791044776116237, 45.00000000000000711, 62.18611311450884926 ) ) ;
#22334=CARTESIAN_POINT ( 'NONE',  ( -12.50000000000000178, 40.62314097313324623, -68.19079107895046832 ) ) ;
#22346=CARTESIAN_POINT ( 'NONE',  ( 7.087005777346045754, 41.65067221237009676, -59.33604986165270390 ) ) ;
#22349=ORIENTED_EDGE ( 'NONE', *, *, #102055, .F. ) ;
#22376=CARTESIAN_POINT ( 'NONE',  ( 65.26738680892601963, 40.83906611471848436, 0.8120011907752979763 ) ) ;
#22381=CARTESIAN_POINT ( 'NONE',  ( 53.52139369741866659, 50.00000000000000000, 33.73130704865685914 ) ) ;
#22387=CARTESIAN_POINT ( 'NONE',  ( 10.67808697578073129, -5.000000000000001776, -77.27709671283406578 ) ) ;
#22403=CARTESIAN_POINT ( 'NONE',  ( 5.500000036871884213, 42.00000000000000000, -68.91429207046176941 ) ) ;
#22405=CARTESIAN_POINT ( 'NONE',  ( 59.16597917554048536, 50.00000000000000711, 21.79159307829888803 ) ) ;
#22416=CARTESIAN_POINT ( 'NONE',  ( 6.075720087193105634, 41.99394347255277182, -59.86320241472431292 ) ) ;
#22417=CARTESIAN_POINT ( 'NONE',  ( -5.420469775605654128, 41.88321586335170821, -59.04137891894603030 ) ) ;
#22431=( LENGTH_UNIT ( ) NAMED_UNIT ( * ) SI_UNIT ( .MILLI., .METRE. ) );
#22443=CARTESIAN_POINT ( 'NONE',  ( -10.47796581436744923, -5.000000000000000000, -78.93819186519100128 ) ) ;
#22458=CARTESIAN_POINT ( 'NONE',  ( 2.617478844992369158, 49.99999999999999289, -75.26027323389158141 ) ) ;
#22482=CARTESIAN_POINT ( 'NONE',  ( -8.922269033012433681, -5.000000000000000000, 5.219866590718518218 ) ) ;
#22485=CARTESIAN_POINT ( 'NONE',  ( -5.293082431914539754, 18.39773536900015216, -37.77701885971370643 ) ) ;
#22487=( NAMED_UNIT ( * ) SI_UNIT ( $, .STERADIAN. ) SOLID_ANGLE_UNIT ( ) );
#22501=CARTESIAN_POINT ( 'NONE',  ( -49.55398223496038668, 40.83861519502255533, -42.37453762653911582 ) ) ;
#22503=CARTESIAN_POINT ( 'NONE',  ( -17.59947254824060536, 50.00000000000000000, 62.68871018980012622 ) ) ;
#22510=CARTESIAN_POINT ( 'NONE',  ( 17.50000000000003197, 52.00000000000194689, 59.64162155654130260 ) ) ;
#22517=CARTESIAN_POINT ( 'NONE',  ( -13.41428277683274395, 42.83120269148118098, -92.05841013448643650 ) ) ;
#22518=CARTESIAN_POINT ( 'NONE',  ( 7.251694438969768619, 41.54830556103024719, -59.82648080958256287 ) ) ;
#22539=SURFACE_STYLE_USAGE ( .BOTH. , #71052 ) ;
#22550=CARTESIAN_POINT ( 'NONE',  ( 1.224646799147352665E-15, -79.93083296558610584, -95.00000000000000000 ) ) ;
#22554=CARTESIAN_POINT ( 'NONE',  ( -15.30771400658740689, 18.64284798592982639, 35.25047262264921244 ) ) ;
#22563=ORIENTED_EDGE ( 'NONE', *, *, #10884, .F. ) ;
#22568=CARTESIAN_POINT ( 'NONE',  ( 5.787518022136032947, 41.99999999999999289, -59.87256586542197567 ) ) ;
#22599=ORIENTED_EDGE ( 'NONE', *, *, #46210, .T. ) ;
#22608=EDGE_CURVE ( 'NONE', #89905, #67790, #9261, .T. ) ;
#22618=CARTESIAN_POINT ( 'NONE',  ( 17.82150094932208262, -4.333298119783735913, -1.872127852956306571 ) ) ;
#22626=CARTESIAN_POINT ( 'NONE',  ( -8.922269033012433681, -5.000000000000000000, 5.219866590718518218 ) ) ;
#22630=FACE_BOUND ( 'NONE', #43366, .T. ) ;
#22644=FACE_OUTER_BOUND ( 'NONE', #67610, .T. ) ;
#22663=CARTESIAN_POINT ( 'NONE',  ( -52.56483885390523625, 48.00000000000000000, -38.23529411764706509 ) ) ;
#22677=CARTESIAN_POINT ( 'NONE',  ( 19.27285195068759549, 49.83909218305972644, 61.40325362178533908 ) ) ;
#22703=CARTESIAN_POINT ( 'NONE',  ( -19.47693998750411026, 49.99334787011666492, 60.32562116054356949 ) ) ;
#22727=CARTESIAN_POINT ( 'NONE',  ( 9.739726766104318756, -5.000000000001365130, -87.61747884499031613 ) ) ;
#22735=CARTESIAN_POINT ( 'NONE',  ( 7.701342750608461962, -4.999999999995311306, -18.36411236461295360 ) ) ;
#22737=CARTESIAN_POINT ( 'NONE',  ( -9.610124387803624657, 50.00000000000001421, -77.63937538513252434 ) ) ;
#22776=CARTESIAN_POINT ( 'NONE',  ( 4.966176485634622217, 41.64999999999998437, -70.47555195150158625 ) ) ;
#22777=VERTEX_POINT ( 'NONE', #28275 ) ;
#22793=CARTESIAN_POINT ( 'NONE',  ( -58.89672143727629816, 39.42406680342908487, -28.13783362225636608 ) ) ;
#22800=EDGE_LOOP ( 'NONE', ( #93336, #106381, #35659, #103544 ) ) ;
#22809=( BOUNDED_CURVE ( )  B_SPLINE_CURVE ( 2, ( #101819, #37666, #102894 ),
 .UNSPECIFIED., .F., .F. ) 
 B_SPLINE_CURVE_WITH_KNOTS ( ( 3, 3 ),
 ( 0.000000000000000000, 1.000000000000000000 ),
 .UNSPECIFIED. ) 
 CURVE ( )  GEOMETRIC_REPRESENTATION_ITEM ( )  RATIONAL_B_SPLINE_CURVE ( ( 1.000000000000000000, 1.428571428571428825, 1.428571428571429269 ) ) 
 REPRESENTATION_ITEM ( '' )  );
#22812=CARTESIAN_POINT ( 'NONE',  ( -7.996668422904766871, 48.00000000000000000, -91.14546720082618947 ) ) ;
#22829=CARTESIAN_POINT ( 'NONE',  ( 7.372395903208937895, -5.000000000000000000, -15.53007256938181513 ) ) ;
#22843=CARTESIAN_POINT ( 'NONE',  ( 9.500000025475724641, -4.999999999999998224, -69.85526497429231085 ) ) ;
#22854=CARTESIAN_POINT ( 'NONE',  ( 7.439123282901347167, 41.00341550150766068, -68.91429205944716330 ) ) ;
#22856=CARTESIAN_POINT ( 'NONE',  ( -7.195947757872210637, 41.08281073708428721, -58.60024740043413516 ) ) ;
#22861=CARTESIAN_POINT ( 'NONE',  ( -12.50000000000000355, 27.15417587463127091, -44.69229109533035427 ) ) ;
#22871=STYLED_ITEM ( 'NONE', ( #70977 ), #94497 ) ;
#22874=CARTESIAN_POINT ( 'NONE',  ( 14.62309622339465243, 18.64284798592481351, -35.53993507406291030 ) ) ;
#22884=ORIENTED_EDGE ( 'NONE', *, *, #32925, .F. ) ;
#22890=CARTESIAN_POINT ( 'NONE',  ( 5.500000000000006217, 42.00000000000000000, -58.09827136975972905 ) ) ;
#22903=CARTESIAN_POINT ( 'NONE',  ( -64.91565662648044110, 48.00000000000000000, 6.815324757466639127 ) ) ;
#22909=CARTESIAN_POINT ( 'NONE',  ( 12.36633005457780854, -4.301166014003213078, -76.75180828602340455 ) ) ;
#22910=EDGE_CURVE ( 'NONE', #84646, #33315, #44056, .T. ) ;
#22917=CARTESIAN_POINT ( 'NONE',  ( 17.95740001248639928, 50.00000000000000711, 61.94476881109564914 ) ) ;
#22970=CARTESIAN_POINT ( 'NONE',  ( 27.00466673664397632, 41.40534887492042060, -70.25901564828242840 ) ) ;
#22978=CARTESIAN_POINT ( 'NONE',  ( 1.224646799147352665E-15, 48.00000000000000000, -75.00000000000001421 ) ) ;
#22981=CARTESIAN_POINT ( 'NONE',  ( -25.60851123679742258, 50.00000000031798919, -75.29411764726208389 ) ) ;
#22988=CARTESIAN_POINT ( 'NONE',  ( -7.320748600891240798, 41.41789230214724427, -68.91429205797308555 ) ) ;
#23001=CARTESIAN_POINT ( 'NONE',  ( -5.219866590715411370, -5.000000000000000000, -8.922269033013266792 ) ) ;
#23013=EDGE_CURVE ( 'NONE', #67117, #21469, #102491, .T. ) ;
#23019=CARTESIAN_POINT ( 'NONE',  ( 6.738100180926640093, 41.71798714554645215, -59.05424661244425266 ) ) ;
#23021=SURFACE_STYLE_USAGE ( .BOTH. , #13289 ) ;
#23029=CARTESIAN_POINT ( 'NONE',  ( 17.50000000000004619, 51.99872764530864799, 60.15967750825412708 ) ) ;
#23037=CARTESIAN_POINT ( 'NONE',  ( -9.536280427380496860, -4.999999999999837463, -20.18661038764972560 ) ) ;
#23047=CARTESIAN_POINT ( 'NONE',  ( -7.468836275494362020, -3.123212597911423138, -19.53079664951584959 ) ) ;
#23082=CARTESIAN_POINT ( 'NONE',  ( 5.430163322397451253, 41.93410894844108583, -59.17461580565397128 ) ) ;
#23084=CARTESIAN_POINT ( 'NONE',  ( -1.233923992984923027E-14, 18.64316884711714195, -38.36535705883633085 ) ) ;
#23128=EDGE_LOOP ( 'NONE', ( #64352, #76818, #89230, #27149 ) ) ;
#23139=( NAMED_UNIT ( * ) SI_UNIT ( $, .STERADIAN. ) SOLID_ANGLE_UNIT ( ) );
#23160=EDGE_LOOP ( 'NONE', ( #48641, #93737, #30222 ) ) ;
#23190=ADVANCED_FACE ( 'NONE', ( #67519 ), #17382, .F. ) ;
#23201=CARTESIAN_POINT ( 'NONE',  ( 19.00081985458449552, 49.50573636308028824, 61.91387040241579598 ) ) ;
#23242=CARTESIAN_POINT ( 'NONE',  ( 6.990291106834062518, -2.999999999999999556, 4.028951842967195773 ) ) ;
#23246=CARTESIAN_POINT ( 'NONE',  ( 7.996668422914432028, -4.999999999991826094, -91.14546720080765851 ) ) ;
#23255=CARTESIAN_POINT ( 'NONE',  ( 6.689814467814940713, -4.999999999994905409, -16.20004731218675786 ) ) ;
#23257=CARTESIAN_POINT ( 'NONE',  ( -6.061808134820600991, 49.99999999999999289, -74.52203418564695880 ) ) ;
#23258=CARTESIAN_POINT ( 'NONE',  ( -39.03259858841720131, 42.04011792294609506, -56.83904871932554670 ) ) ;
#23275=EDGE_CURVE ( 'NONE', #57839, #59054, #20787, .T. ) ;
#23278=FACE_BOUND ( 'NONE', #6975, .T. ) ;
#23289=CARTESIAN_POINT ( 'NONE',  ( 6.913779129928547817, 41.73441125232163529, -59.30275354417914713 ) ) ;
#23297=CARTESIAN_POINT ( 'NONE',  ( 11.99999999999999467, -5.000000000000002665, -83.42920367501479006 ) ) ;
#23302=CARTESIAN_POINT ( 'NONE',  ( 4.852941176470593199, 24.91666666666666430, -70.80672828634229177 ) ) ;
#23316=CARTESIAN_POINT ( 'NONE',  ( 51.48757442383971039, 38.95383793068617706, -37.45149417477087184 ) ) ;
#23334=CARTESIAN_POINT ( 'NONE',  ( 1.224646799147352665E-15, 48.00000000000000000, -75.00000000000001421 ) ) ;
#23351=CARTESIAN_POINT ( 'NONE',  ( 7.146471073273054309, -5.000000000000000000, -15.44879583875536788 ) ) ;
#23366=CARTESIAN_POINT ( 'NONE',  ( 7.225703553013920200, -4.999999999999999112, -73.19314196553180807 ) ) ;
#23367=ORIENTED_EDGE ( 'NONE', *, *, #55553, .T. ) ;
#23378=CARTESIAN_POINT ( 'NONE',  ( 7.425259286936451986, 41.08730335070794126, -69.63985817587276017 ) ) ;
#23380=EDGE_CURVE ( 'NONE', #72225, #81898, #15555, .T. ) ;
#23397=CARTESIAN_POINT ( 'NONE',  ( 7.302130867679851534, 41.45639825872783035, -59.68093889946540287 ) ) ;
#23440=( BOUNDED_SURFACE ( )  B_SPLINE_SURFACE ( 2, 3, ( 
 ( #56085, #9144, #42055, #49612 ),
 ( #90615, #99761, #34005, #89026 ),
 ( #15123, #7028, #39946, #105723 ) ),
 .UNSPECIFIED., .F., .F., .T. ) 
 B_SPLINE_SURFACE_WITH_KNOTS ( ( 3, 3 ),
 ( 4, 4 ),
 ( 0.000000000000000000, 1.000000000000000000 ),
 ( 0.04485000000000000792, 0.04800000000000000100 ),
 .UNSPECIFIED. ) 
 GEOMETRIC_REPRESENTATION_ITEM ( )  RATIONAL_B_SPLINE_SURFACE ( (
 ( 1.000000000000000000, 1.000000000000000000, 1.000000000000000000, 1.000000000000000000),
 ( 1.857142857142858317, 1.857142857142858317, 1.857142857142858317, 1.857142857142858317),
 ( 1.000000000000000000, 1.000000000000000000, 1.000000000000000000, 1.000000000000000000) ) ) 
 REPRESENTATION_ITEM ( '' )  SURFACE ( )  );
#23465=CARTESIAN_POINT ( 'NONE',  ( -12.49999999999999822, 14.91296021360665769, -32.73279218218806363 ) ) ;
#23476=CARTESIAN_POINT ( 'NONE',  ( -6.701893397842001221, 41.44328394191487774, -70.59544911652842814 ) ) ;
#23500=CARTESIAN_POINT ( 'NONE',  ( 40.47243798843062734, 40.24842200370380851, -54.85959680779491521 ) ) ;
#23513=CARTESIAN_POINT ( 'NONE',  ( -12.13034742782428133, 49.99999999999999289, -93.82352941176471006 ) ) ;
#23560=CARTESIAN_POINT ( 'NONE',  ( 17.50000000000003908, 51.99999999999984368, 59.82664205500665844 ) ) ;
#23568=CARTESIAN_POINT ( 'NONE',  ( -5.076160773006212601, -4.320849473519612793, -17.10810059244015946 ) ) ;
#23593=CARTESIAN_POINT ( 'NONE',  ( -65.26738680890619548, 48.00000000000000000, 0.8120011905346659065 ) ) ;
#23618=CARTESIAN_POINT ( 'NONE',  ( 6.359250229816447053, 41.88719966772354297, -59.22188798823055578 ) ) ;
#23624=ORIENTED_EDGE ( 'NONE', *, *, #24742, .T. ) ;
#23628=EDGE_LOOP ( 'NONE', ( #13888, #69538, #68031, #34109 ) ) ;
#23663=ORIENTED_EDGE ( 'NONE', *, *, #86406, .F. ) ;
#23672=CARTESIAN_POINT ( 'NONE',  ( 5.219866590719942856, -5.000000000000000000, -8.922269033013279227 ) ) ;
#23680=FACE_OUTER_BOUND ( 'NONE', #85633, .T. ) ;
#23728=EDGE_CURVE ( 'NONE', #45623, #101469, #70445, .T. ) ;
#23751=ADVANCED_FACE ( 'NONE', ( #69910 ), #14894, .T. ) ;
#23784=CARTESIAN_POINT ( 'NONE',  ( 1.047197551196597631, -3.000000000000000888, 8.000000000000001776 ) ) ;
#23797=CARTESIAN_POINT ( 'NONE',  ( 7.499944090891561999, -3.043005460614601532, -20.23003913617544569 ) ) ;
#23805=B_SPLINE_CURVE_WITH_KNOTS ( 'NONE', 3,
 ( #17711, #75398, #50571, #93723 ),
 .UNSPECIFIED., .F., .F.,
 ( 4, 4 ),
 ( 0.8039644300567937441, 1.000000000000000000 ),
 .UNSPECIFIED. ) ;
#23817=ADVANCED_FACE ( 'NONE', ( #63955 ), #6209, .F. ) ;
#23834=CARTESIAN_POINT ( 'NONE',  ( -24.03027799567535538, 41.61735029016796261, -74.26546206927031335 ) ) ;
#23840=CARTESIAN_POINT ( 'NONE',  ( -11.68767211932491179, -5.000000000000002665, -88.14097461399494193 ) ) ;
#23878=CARTESIAN_POINT ( 'NONE',  ( -10.49999999997808331, -5.000000000000000000, -12.52300748972991506 ) ) ;
#23885=( GEOMETRIC_REPRESENTATION_CONTEXT ( 3 ) GLOBAL_UNCERTAINTY_ASSIGNED_CONTEXT ( ( #21365 ) ) GLOBAL_UNIT_ASSIGNED_CONTEXT ( ( #63511, #30088, #79672 ) ) REPRESENTATION_CONTEXT ( 'NONE', 'WORKASPACE' ) );
#23919=CARTESIAN_POINT ( 'NONE',  ( 6.701893401236465486, 41.44328394225253476, -70.59544911815949320 ) ) ;
#23931=CARTESIAN_POINT ( 'NONE',  ( -62.90160406446442209, 50.00000000000000711, -3.733639982922376532 ) ) ;
#23936=B_SPLINE_SURFACE_WITH_KNOTS ( 'NONE', 3, 3, ( 
 ( #73994, #75048, #51306, #49724, #76124, #8733, #84759, #43239 ),
 ( #84229, #2220, #10841, #76, #65913, #98793, #24950, #57804 ),
 ( #90727, #16842, #20616, #4366, #21130, #11377, #94994, #3308 ),
 ( #93915, #62615, #12444, #103072, #2765, #35714, #69642, #52376 ),
 ( #53959, #78253, #77736, #61029, #28683, #44302, #93393, #102536 ),
 ( #61565, #37304, #19539, #70168, #86897, #101995, #20072, #62102 ),
 ( #77196, #85844, #29227, #12970, #94460, #45896, #78772, #4906 ),
 ( #53457, #37836, #70701, #86378, #103591, #52919, #29740, #45371 ),
 ( #95501, #85287, #21644, #54480, #11918, #87427, #43760, #76652 ),
 ( #68591, #101476, #27627, #44846, #3847, #60508, #36777, #36253 ) ),
 .UNSPECIFIED., .F., .F., .F.,
 ( 4, 2, 2, 2, 4 ),
 ( 4, 2, 2, 4 ),
 ( 0.000000000000000000, 0.1250000000000000000, 0.2500000000000000000, 0.5000000000000000000, 1.000000000000000000 ),
 ( 0.000000000000000000, 0.2500000000000000000, 0.5000000000000000000, 1.000000000000000000 ),
 .UNSPECIFIED. ) ;
#23943=CARTESIAN_POINT ( 'NONE',  ( 4.852941176470595863, 39.99999999999999289, -70.80672828634229177 ) ) ;
#23955=VERTEX_POINT ( 'NONE', #62758 ) ;
#23963=CARTESIAN_POINT ( 'NONE',  ( 14.90155531838479064, 42.58002643028073919, -90.01374843427898043 ) ) ;
#23986=CARTESIAN_POINT ( 'NONE',  ( 10.51296777078104050, 50.00000000000000000, -92.64705882352942012 ) ) ;
#24033=CARTESIAN_POINT ( 'NONE',  ( -6.061808134762952882, -5.000000000000000000, -95.47796581438812780 ) ) ;
#24052=CARTESIAN_POINT ( 'NONE',  ( -23.99113157954622366, 50.00000000000000000, -74.11764705887553362 ) ) ;
#24066=CARTESIAN_POINT ( 'NONE',  ( -4.175893272572330339, -5.000000000001136868, -7.137815226410158864 ) ) ;
#24075=CARTESIAN_POINT ( 'NONE',  ( -4.852941176470598528, -5.000000000000002665, -70.80672828634229177 ) ) ;
#24076=( BOUNDED_SURFACE ( )  B_SPLINE_SURFACE ( 2, 3, ( 
 ( #61553, #11905, #28668, #76638, #86364, #94447, #68575, #35701, #78239, #44832 ),
 ( #20605, #26547, #101461, #77183, #100912, #52907, #92282, #3830, #53442, #19526 ),
 ( #20057, #11360, #3294, #4353, #12429, #45359, #67504, #36236, #100386, #18438 ) ),
 .UNSPECIFIED., .F., .F., .F. ) 
 B_SPLINE_SURFACE_WITH_KNOTS ( ( 3, 3 ),
 ( 4, 2, 2, 2, 4 ),
 ( 0.000000000000000000, 1.000000000000000000 ),
 ( 0.2013554496957829509, 0.2052093776119387758, 0.2375733647630427492, 0.2537553583385947498, 0.2699373519141466948 ),
 .UNSPECIFIED. ) 
 GEOMETRIC_REPRESENTATION_ITEM ( )  RATIONAL_B_SPLINE_SURFACE ( (
 ( 1.000000000000000000, 1.000000000000000000, 1.000000000000000000, 1.000000000000000000, 1.000000000000000000, 1.000000000000000000, 1.000000000000000000, 1.000000000000000000, 1.000000000000000000, 1.000000000000000000),
 ( 1.857142857142858317, 1.857142857142858317, 1.857142857142858317, 1.857142857142858317, 1.857142857142858317, 1.857142857142858317, 1.857142857142857428, 1.857142857142857428, 1.857142857142858317, 1.857142857142858317),
 ( 1.000000000000000000, 1.000000000000000000, 1.000000000000000000, 1.000000000000000000, 1.000000000000000000, 1.000000000000000000, 1.000000000000000000, 1.000000000000000000, 1.000000000000000000, 1.000000000000000000) ) ) 
 REPRESENTATION_ITEM ( '' )  SURFACE ( )  );
#24096=CARTESIAN_POINT ( 'NONE',  ( 17.50000000000004974, 49.61376050339585220, 62.33429930757360182 ) ) ;
#24105=CARTESIAN_POINT ( 'NONE',  ( -9.499937800619317585, -5.000000000000002665, -20.18737470931643685 ) ) ;
#24116=CARTESIAN_POINT ( 'NONE',  ( 52.56483885390523625, 48.00000000000000000, -38.23529411764706509 ) ) ;
#24125=ORIENTED_EDGE ( 'NONE', *, *, #35422, .F. ) ;
#24130=ORIENTED_EDGE ( 'NONE', *, *, #52543, .F. ) ;
#24131=EDGE_CURVE ( 'NONE', #25935, #80162, #51450, .T. ) ;
#24132=CARTESIAN_POINT ( 'NONE',  ( 60.62677696744211175, 49.99999999997998401, 24.18439665018642870 ) ) ;
#24143=STYLED_ITEM ( 'NONE', ( #65705 ), #34024 ) ;
#24151=STYLED_ITEM ( 'NONE', ( #83012 ), #32759 ) ;
#24157=CARTESIAN_POINT ( 'NONE',  ( 23.52347158108310410, 41.65284174216176893, -74.94888205883640353 ) ) ;
#24168=CARTESIAN_POINT ( 'NONE',  ( -4.966176470918028052, 41.64999999999999147, -70.47555194646973575 ) ) ;
#24170=EDGE_CURVE ( 'NONE', #81655, #66436, #14210, .T. ) ;
#24207=CARTESIAN_POINT ( 'NONE',  ( -10.00000000000000000, -5.000000000000000000, 2.617993873628187806 ) ) ;
#24214=CARTESIAN_POINT ( 'NONE',  ( -12.50000000000000711, -3.000000000000000000, -78.42624373368740009 ) ) ;
#24215=CARTESIAN_POINT ( 'NONE',  ( 11.69538631874852186, -5.000000000000000000, -81.87730495800397534 ) ) ;
#24237=LINE ( 'NONE', #64664, #46352 ) ;
#24305=CARTESIAN_POINT ( 'NONE',  ( 17.60394295411769150, 45.00000000000001421, 63.08992194734121028 ) ) ;
#24311=CARTESIAN_POINT ( 'NONE',  ( -8.878109361141049760, -5.000000000000000000, -17.03646273725755833 ) ) ;
#24329=CARTESIAN_POINT ( 'NONE',  ( 6.735051087778345824, -4.346205982510036314, -16.86563398496271660 ) ) ;
#24345=CARTESIAN_POINT ( 'NONE',  ( -56.06921707446602454, 40.83906611473297232, -33.41757057980472467 ) ) ;
#24348=CARTESIAN_POINT ( 'NONE',  ( -17.49999999999918643, 49.99999999999941025, 59.71562975593359113 ) ) ;
#24361=CARTESIAN_POINT ( 'NONE',  ( -19.99877541361295741, 41.84885527536232530, -79.71217436998914252 ) ) ;
#24367=CARTESIAN_POINT ( 'NONE',  ( -1.308996937480704004, -4.999999999999988454, -95.00000000000001421 ) ) ;
#24385=CARTESIAN_POINT ( 'NONE',  ( 13.05360465724633912, -5.000000000000000000, -85.14609521163498584 ) ) ;
#24399=CARTESIAN_POINT ( 'NONE',  ( -7.758748231291408892, -5.000000000000000888, -73.00623724569611284 ) ) ;
#24411=CARTESIAN_POINT ( 'NONE',  ( -11.03870218254165181, -4.986327171952302351, -12.57673782977023791 ) ) ;
#24427=EDGE_CURVE ( 'NONE', #102845, #58869, #60679, .T. ) ;
#24430=EDGE_LOOP ( 'NONE', ( #24673, #99861, #57031, #87611 ) ) ;
#24455=CARTESIAN_POINT ( 'NONE',  ( 7.326726166330386647, 41.40616545424374806, -69.28044400771726430 ) ) ;
#24464=CARTESIAN_POINT ( 'NONE',  ( -41.05804556683040829, 49.99999999999998579, 48.04352316237233111 ) ) ;
#24471=CARTESIAN_POINT ( 'NONE',  ( -7.500145657655585829, -5.000000000000005329, -20.99858917502733746 ) ) ;
#24476=CARTESIAN_POINT ( 'NONE',  ( 7.500000000000007105, 39.99999999999970868, -59.88032989331640010 ) ) ;
#24490=CARTESIAN_POINT ( 'NONE',  ( 14.25150717306086889, 43.31689343519231983, -90.90741688367272388 ) ) ;
#24518=CARTESIAN_POINT ( 'NONE',  ( -5.500000000000006217, 42.00000000000000000, -59.88032989329961708 ) ) ;
#24525=FILL_AREA_STYLE ('',( #65483 ) ) ;
#24537=EDGE_CURVE ( 'NONE', #36, #78368, #25735, .T. ) ;
#24538=CARTESIAN_POINT ( 'NONE',  ( -7.452250100395975352, 40.95021212578417646, -69.64366906012794800 ) ) ;
#24573=CARTESIAN_POINT ( 'NONE',  ( 12.50000000000000711, 36.63321530731812459, -57.11196096728948390 ) ) ;
#24585=ORIENTED_EDGE ( 'NONE', *, *, #106117, .F. ) ;
#24593=B_SPLINE_CURVE_WITH_KNOTS ( 'NONE', 3,
 ( #100241, #35017, #28001, #43604, #93758, #51687, #36095, #33954, #59273, #10167, #17750, #35553 ),
 .UNSPECIFIED., .F., .F.,
 ( 4, 2, 2, 2, 2, 4 ),
 ( 0.04761886307670518820, 0.05150820635059603914, 0.05539754962448689701, 0.06317623617226861277, 0.07095492272005031464, 0.07873360926783201652 ),
 .UNSPECIFIED. ) ;
#24621=CARTESIAN_POINT ( 'NONE',  ( 17.50000000000004974, 51.99999999999999289, 59.91915230423961702 ) ) ;
#24629=CARTESIAN_POINT ( 'NONE',  ( 4.999060825136298014, 41.75164249415627182, -70.37937598343344803 ) ) ;
#24630=CARTESIAN_POINT ( 'NONE',  ( -8.044970079966896392, -5.000000000000017764, -15.82739658860585941 ) ) ;
#24652=CARTESIAN_POINT ( 'NONE',  ( 55.22048556080756043, 48.00000000000000000, 34.80214219304977519 ) ) ;
#24664=VERTEX_POINT ( 'NONE', #98312 ) ;
#24673=ORIENTED_EDGE ( 'NONE', *, *, #45590, .T. ) ;
#24675=CARTESIAN_POINT ( 'NONE',  ( 23.95383387565141575, 41.62280648303626407, -74.36842561464139578 ) ) ;
#24713=CARTESIAN_POINT ( 'NONE',  ( -13.14242568365673414, 42.00000000000000000, -92.43215185528094935 ) ) ;
#24732=( LENGTH_UNIT ( ) NAMED_UNIT ( * ) SI_UNIT ( .MILLI., .METRE. ) );
#24733=CARTESIAN_POINT ( 'NONE',  ( -17.49999999999997513, 49.85589862348337675, 63.87662473929367479 ) ) ;
#24742=EDGE_CURVE ( 'NONE', #106540, #77528, #32894, .T. ) ;
#24808=CARTESIAN_POINT ( 'NONE',  ( 6.507454588539320461, 41.74144728082382017, -58.94379944081024547 ) ) ;
#24837=( NAMED_UNIT ( * ) SI_UNIT ( $, .STERADIAN. ) SOLID_ANGLE_UNIT ( ) );
#24847=CARTESIAN_POINT ( 'NONE',  ( 5.075566108724593128, -4.332661967060489339, -17.09624963492156269 ) ) ;
#24849=FILL_AREA_STYLE ('',( #34015 ) ) ;
#24850=CARTESIAN_POINT ( 'NONE',  ( -41.22850014084250603, 41.73474038525400687, -53.82018319452755151 ) ) ;
#24864=CARTESIAN_POINT ( 'NONE',  ( -17.49999999999894840, 49.48689581941425075, 62.41113125631201086 ) ) ;
#24875=VERTEX_POINT ( 'NONE', #102022 ) ;
#24876=ADVANCED_FACE ( 'NONE', ( #28183 ), #80411, .F. ) ;
#24887=CARTESIAN_POINT ( 'NONE',  ( 7.374560640985523996, -5.000000000000002665, -94.59600210749707117 ) ) ;
#24903=CARTESIAN_POINT ( 'NONE',  ( 12.86276638840208086, -5.000000000000000000, -82.77022731229634189 ) ) ;
#24909=CARTESIAN_POINT ( 'NONE',  ( 57.68649645722720010, 38.95207762959029907, -27.56578445358567819 ) ) ;
#24911=ORIENTED_EDGE ( 'NONE', *, *, #4682, .F. ) ;
#24915=CARTESIAN_POINT ( 'NONE',  ( -5.096247963242959145, -4.999999999999997335, -73.00359695307524532 ) ) ;
#24950=CARTESIAN_POINT ( 'NONE',  ( 6.952098966025630489, 40.29466789516767022, -71.12438203459961983 ) ) ;
#24958=EDGE_CURVE ( 'NONE', #81281, #71976, #73489, .T. ) ;
#24969=CARTESIAN_POINT ( 'NONE',  ( 7.392085842482234881, 40.93519689220327962, -70.13194415493437361 ) ) ;
#24973=CARTESIAN_POINT ( 'NONE',  ( -7.500000000000006217, 39.99999999999122480, -59.88032989330939415 ) ) ;
#24989=CARTESIAN_POINT ( 'NONE',  ( 7.109733078360420677, 41.69026692163959069, -59.69141567447950081 ) ) ;
#25001=( BOUNDED_SURFACE ( )  B_SPLINE_SURFACE ( 2, 3, ( 
 ( #37788, #45321, #53916, #27580, #45846, #93865, #59926, #51794, #28633, #12924, #84707, #61516, #10791, #70649, #92791, #68540, #43710, #78718, #78204, #35662, #60978, #18953 ),
 ( #101429, #86327, #60460, #93338, #19488, #52866, #94408, #52325, #103545, #85239, #53409, #11325, #62057, #44255, #101946, #77146, #3262, #36203, #4854, #12393, #103024, #69070 ),
 ( #20024, #4319, #85796, #11868, #44797, #77686, #37254, #3796, #36733, #70116, #69597, #29179, #94944, #21080, #87899, #22116, #13981, #6958, #5890, #40391, #30748, #56562 ) ),
 .UNSPECIFIED., .F., .F., .F. ) 
 B_SPLINE_SURFACE_WITH_KNOTS ( ( 3, 3 ),
 ( 4, 2, 2, 2, 2, 2, 2, 2, 2, 2, 4 ),
 ( 0.000000000000000000, 1.000000000000000000 ),
 ( 3.594963135488010497, 3.839346969278153665, 4.450306553753511807, 5.061266138228869949, 5.672225722704228090, 6.283185307179586232, 6.894144891654944374, 7.505104476130302515, 8.116064060605660657, 8.727023645081018799, 8.971407478871162411 ),
 .UNSPECIFIED. ) 
 GEOMETRIC_REPRESENTATION_ITEM ( )  RATIONAL_B_SPLINE_SURFACE ( (
 ( 1.000000000000000000, 1.000000000000000000, 1.000000000000000000, 1.000000000000000000, 1.000000000000000000, 1.000000000000000000, 1.000000000000000000, 1.000000000000000000, 1.000000000000000000, 1.000000000000000000, 1.000000000000000000, 1.000000000000000000, 1.000000000000000000, 1.000000000000000000, 1.000000000000000000, 1.000000000000000000, 1.000000000000000000, 1.000000000000000000, 1.000000000000000000, 1.000000000000000000, 1.000000000000000000, 1.000000000000000000),
 ( 1.857142857142858317, 1.857142857142858317, 1.857142857142858317, 1.857142857142858317, 1.857142857142858317, 1.857142857142858317, 1.857142857142858317, 1.857142857142858317, 1.857142857142858317, 1.857142857142858317, 1.857142857142858317, 1.857142857142858317, 1.857142857142858317, 1.857142857142858317, 1.857142857142858317, 1.857142857142858317, 1.857142857142858317, 1.857142857142858317, 1.857142857142858317, 1.857142857142858317, 1.857142857142858317, 1.857142857142858317),
 ( 1.000000000000000000, 1.000000000000000000, 1.000000000000000000, 1.000000000000000000, 1.000000000000000000, 1.000000000000000000, 1.000000000000000000, 1.000000000000000000, 1.000000000000000000, 1.000000000000000000, 1.000000000000000000, 1.000000000000000000, 1.000000000000000000, 1.000000000000000000, 1.000000000000000000, 1.000000000000000000, 1.000000000000000000, 1.000000000000000000, 1.000000000000000000, 1.000000000000000000, 1.000000000000000000, 1.000000000000000000) ) ) 
 REPRESENTATION_ITEM ( '' )  SURFACE ( )  );
#25005=CARTESIAN_POINT ( 'NONE',  ( 13.14242568359541607, 42.00000000000000000, -92.43215185542086942 ) ) ;
#25021=CARTESIAN_POINT ( 'NONE',  ( -60.66923414622394262, 50.00000000000000000, 17.93278245653412384 ) ) ;
#25031=( LENGTH_UNIT ( ) NAMED_UNIT ( * ) SI_UNIT ( .MILLI., .METRE. ) );
#25040=MECHANICAL_DESIGN_GEOMETRIC_PRESENTATION_REPRESENTATION('',(#14679),#85310);
#25056=CARTESIAN_POINT ( 'NONE',  ( 19.50011280463133545, 50.00000000000000000, 59.90639435984937222 ) ) ;
#25063=CARTESIAN_POINT ( 'NONE',  ( -7.029557160387159165, 41.29102236549713467, -70.49405803162696316 ) ) ;
#25071=CARTESIAN_POINT ( 'NONE',  ( -9.742892617409784961, -5.000000000000000888, 2.583889972064361107 ) ) ;
#25095=CARTESIAN_POINT ( 'NONE',  ( 12.50000000000000533, 39.74439965334176605, -64.98731535703404916 ) ) ;
#25100=CARTESIAN_POINT ( 'NONE',  ( -7.141975279401744814, -2.999999999999884537, -70.98863559355044117 ) ) ;
#25141=EDGE_CURVE ( 'NONE', #80162, #34787, #15364, .T. ) ;
#25144=SURFACE_STYLE_USAGE ( .BOTH. , #98977 ) ;
#25149=B_SPLINE_CURVE_WITH_KNOTS ( 'NONE', 3,
 ( #77246, #13015, #70217, #76699, #52968, #68643, #86948, #85891, #3360, #45423, #21694, #36305, #69691, #4954, #45942, #3891, #78823, #60549 ),
 .UNSPECIFIED., .F., .F.,
 ( 4, 2, 2, 2, 2, 2, 2, 2, 4 ),
 ( 0.000000000000000000, 0.06250000000000005551, 0.1250000000000001110, 0.1875000000000000833, 0.2500000000000000555, 0.3125000000000000555, 0.3750000000000000555, 0.4375000000000000555, 0.5000000000000000000 ),
 .UNSPECIFIED. ) ;
#25152=CARTESIAN_POINT ( 'NONE',  ( 19.49662282918525591, 49.99981527065408216, 59.98277621002879556 ) ) ;
#25163=CARTESIAN_POINT ( 'NONE',  ( -6.108201232855833496, -4.361520614648816796, -16.81796607653734910 ) ) ;
#25168=( LENGTH_UNIT ( ) NAMED_UNIT ( * ) SI_UNIT ( .MILLI., .METRE. ) );
#25173=CARTESIAN_POINT ( 'NONE',  ( 50.94745919686198476, 50.00000000000000000, -37.05882352941176094 ) ) ;
#25187=CARTESIAN_POINT ( 'NONE',  ( 56.06936961865346802, 48.00000000000000000, -33.41736086621895652 ) ) ;
#25201=CARTESIAN_POINT ( 'NONE',  ( -38.20903166377354410, 18.64284798593150683, 4.122114450676773956 ) ) ;
#25231=PRESENTATION_STYLE_ASSIGNMENT (( #58087 ) ) ;
#25271=CARTESIAN_POINT ( 'NONE',  ( -17.49999999999997513, 49.02358271864453343, 64.04945205936840580 ) ) ;
#25273=PRESENTATION_STYLE_ASSIGNMENT (( #391 ) ) ;
#25277=AXIS2_PLACEMENT_3D ( 'NONE', #102452, #71138, #54395 ) ;
#25298=ORIENTED_EDGE ( 'NONE', *, *, #9311, .F. ) ;
#25336=CARTESIAN_POINT ( 'NONE',  ( -2.912673042965788187E-14, 42.00000000000000000, -90.56128410203886858 ) ) ;
#25342=FACE_BOUND ( 'NONE', #40410, .T. ) ;
#25367=CARTESIAN_POINT ( 'NONE',  ( 18.28855716066948389, 45.00000000000001421, 62.41177028466893972 ) ) ;
#25373=CARTESIAN_POINT ( 'NONE',  ( -6.515460109692552848, -4.999999999999999112, -15.35047127641723996 ) ) ;
#25380=CARTESIAN_POINT ( 'NONE',  ( -1.308996937483428269, -3.000000000000002665, -75.00000000000001421 ) ) ;
#25393=FACE_OUTER_BOUND ( 'NONE', #44709, .T. ) ;
#25394=CARTESIAN_POINT ( 'NONE',  ( -43.42270916030687289, 41.45355254419347801, -50.80364451785244739 ) ) ;
#25398=B_SPLINE_CURVE_WITH_KNOTS ( 'NONE', 3,
 ( #83905, #19237, #34866, #11064 ),
 .UNSPECIFIED., .F., .F.,
 ( 4, 4 ),
 ( 0.000000000000000000, 0.4999999999999988898 ),
 .UNSPECIFIED. ) ;
#25410=CARTESIAN_POINT ( 'NONE',  ( -17.49999999999995737, 47.99999999999996447, 64.09945636502659738 ) ) ;
#25425=CARTESIAN_POINT ( 'NONE',  ( -26.32519096281068727, 41.43537210829613571, -71.18657295512365124 ) ) ;
#25436=CARTESIAN_POINT ( 'NONE',  ( -8.737863884125482983, -4.999999999994546585, -90.03618980230058355 ) ) ;
#25446=EDGE_CURVE ( 'NONE', #71944, #52979, #3915, .T. ) ;
#25458=EDGE_CURVE ( 'NONE', #67117, #36789, #66964, .T. ) ;
#25462=CARTESIAN_POINT ( 'NONE',  ( 61.88407606007120165, 38.95394859066640691, 15.24418052639449073 ) ) ;
#25524=CARTESIAN_POINT ( 'NONE',  ( -6.645513941704877858, 41.91298746401114528, -59.84148600730080858 ) ) ;
#25528=CARTESIAN_POINT ( 'NONE',  ( -62.57092854446853636, 49.99999999999999289, -7.449143581871620512 ) ) ;
#25530=CARTESIAN_POINT ( 'NONE',  ( 4.852941176470592310, -3.000000000000002665, -70.80672828634229177 ) ) ;
#25552=CARTESIAN_POINT ( 'NONE',  ( 13.00569724287416307, 42.57699280172521128, -92.62012237565519968 ) ) ;
#25571=CARTESIAN_POINT ( 'NONE',  ( -58.76133767616301640, 50.00000000000000000, 23.44026136864787446 ) ) ;
#25610=CARTESIAN_POINT ( 'NONE',  ( -4.644559862127823457, 47.99999999999999289, -99.31133601631378838 ) ) ;
#25613=CARTESIAN_POINT ( 'NONE',  ( -7.159011624722488421, 41.04792457232633751, -70.58264774317923695 ) ) ;
#25617=ORIENTED_EDGE ( 'NONE', *, *, #7280, .F. ) ;
#25635=ORIENTED_EDGE ( 'NONE', *, *, #84151, .T. ) ;
#25646=CARTESIAN_POINT ( 'NONE',  ( 12.50000000000000533, 27.20503041222523066, -44.74618841300883076 ) ) ;
#25688=ORIENTED_EDGE ( 'NONE', *, *, #92514, .T. ) ;
#25717=CARTESIAN_POINT ( 'NONE',  ( -9.544165109479243014, -4.999999999999968026, -19.39317919831048442 ) ) ;
#25735=B_SPLINE_CURVE_WITH_KNOTS ( 'NONE', 3,
 ( #16055, #40863, #73755, #63310, #2524, #93684, #30416, #71373 ),
 .UNSPECIFIED., .F., .F.,
 ( 4, 2, 2, 4 ),
 ( 0.000000000000000000, 0.2500000000000000000, 0.5000000000000000000, 1.000000000000000000 ),
 .UNSPECIFIED. ) ;
#25742=CARTESIAN_POINT ( 'NONE',  ( -43.69716417794982277, 48.00000000000000000, 48.48761666242421597 ) ) ;
#25744=B_SPLINE_CURVE_WITH_KNOTS ( 'NONE', 3,
 ( #29292, #102609, #77805, #46493, #38427, #47009, #20686, #38941, #54030, #30329, #21717, #5504, #12515, #96112, #3917, #63221, #30874, #52998, #61645, #36849, #45446, #78321, #54558, #22246, #95581, #37908, #103664, #55093, #11990, #85917, #44920, #45971, #69715, #79383, #104721, #28765, #88023, #79908, #14103, #6017, #95064, #94537, #71292, #4437, #37381, #29814, #71818, #70242, #63753, #103144, #13577, #62174 ),
 .UNSPECIFIED., .F., .F.,
 ( 4, 1, 1, 1, 1, 1, 1, 1, 1, 1, 2, 2, 1, 1, 1, 1, 1, 1, 1, 1, 2, 2, 1, 1, 1, 1, 1, 1, 1, 1, 1, 2, 2, 1, 1, 1, 1, 1, 1, 2, 2, 4 ),
 ( 0.000000000000000000, 0.1250000000003060330, 0.1875000000004590495, 0.2187500000005354606, 0.2343750000005737633, 0.2421875000005931089, 0.2460937500006027678, 0.2480468750006076251, 0.2490234375006100398, 0.2495117187506111223, 0.2497558593756118717, 0.2500000000006126211, 0.3125000000007527312, 0.3437500000008228418, 0.3593750000008577583, 0.3671875000008750778, 0.3710937500008839041, 0.3730468750008880674, 0.3740234375008901768, 0.3745117187508911205, 0.3747558593758917311, 0.3750000000008923418, 0.4375000000010839107, 0.4687500000011795565, 0.4843750000012275736, 0.4921875000012514989, 0.4960937500012632118, 0.4980468750012684298, 0.4990234375012703727, 0.4995117187512707058, 0.4997558593762702062, 0.4998779296887702062, 0.5000000000012702062, 0.6250000000009643397, 0.6875000000008114620, 0.7187500000007353007, 0.7343750000006972201, 0.7421875000006779022, 0.7460937500006681322, 0.7480468750006629142, 0.7500000000006576961, 1.000000000000000000 ),
 .UNSPECIFIED. ) ;
#25769=CARTESIAN_POINT ( 'NONE',  ( 14.33580413386840213, 42.00000000000000000, -89.41414995614803729 ) ) ;
#25778=CARTESIAN_POINT ( 'NONE',  ( -6.406311626395538639, 41.42610740534730240, -70.78720125084922188 ) ) ;
#25798=ADVANCED_FACE ( 'NONE', ( #22644 ), #35670, .F. ) ;
#25807=UNCERTAINTY_MEASURE_WITH_UNIT (LENGTH_MEASURE( 1.000000000000000082E-05 ), #106682, 'distance_accuracy_value', 'NONE');
#25817=ORIENTED_EDGE ( 'NONE', *, *, #27362, .T. ) ;
#25823=CARTESIAN_POINT ( 'NONE',  ( -6.763062896852164663, 41.48827110272769403, -70.48955655162545497 ) ) ;
#25876=CARTESIAN_POINT ( 'NONE',  ( -6.802270553527478114, 41.53789085414797455, -58.74929071759987664 ) ) ;
#25894=SURFACE_STYLE_USAGE ( .BOTH. , #50106 ) ;
#25935=VERTEX_POINT ( 'NONE', #73257 ) ;
#25938=VERTEX_POINT ( 'NONE', #6944 ) ;
#25943=SURFACE_STYLE_FILL_AREA ( #24849 ) ;
#25944=CARTESIAN_POINT ( 'NONE',  ( 6.544091414538025120, -3.000000000000002665, -98.56434427384034791 ) ) ;
#25948=CONICAL_SURFACE ( 'NONE', #29403, 18.72828050308589454, 0.7292773806962717931 ) ;
#25961=MECHANICAL_DESIGN_GEOMETRIC_PRESENTATION_REPRESENTATION('',(#91365),#8736);
#25963=CARTESIAN_POINT ( 'NONE',  ( -19.50000000000047606, 49.99999999999996447, 59.82664205501238541 ) ) ;
#25974=CARTESIAN_POINT ( 'NONE',  ( -33.96054341680977728, 40.58705955278919930, -60.99169518065951934 ) ) ;
#25980=CARTESIAN_POINT ( 'NONE',  ( 0.000000000000000000, -3.000000000000002665, -75.00000000000001421 ) ) ;
#25981=CARTESIAN_POINT ( 'NONE',  ( -6.991644891724774880, 41.20407541762637749, -58.47941460531158953 ) ) ;
#25985=CARTESIAN_POINT ( 'NONE',  ( 6.195804100829465533, 41.59435685053998810, -70.65487364791137281 ) ) ;
#26043=CARTESIAN_POINT ( 'NONE',  ( -7.398423365523743911, 41.20504426844082246, -59.67381271312094526 ) ) ;
#26059=CARTESIAN_POINT ( 'NONE',  ( 7.040774347399620936, 41.35742771039598153, -58.68913404742972517 ) ) ;
#26071=CARTESIAN_POINT ( 'NONE',  ( -53.87663890650263454, 50.00000000000000711, -33.03186720634269591 ) ) ;
#26076=ORIENTED_EDGE ( 'NONE', *, *, #35018, .F. ) ;
#26121=MECHANICAL_DESIGN_GEOMETRIC_PRESENTATION_REPRESENTATION('',(#96680),#15751);
#26152=CARTESIAN_POINT ( 'NONE',  ( -6.809786362084849998, 41.36669071755328986, -70.61902766660038822 ) ) ;
#26158=ORIENTED_EDGE ( 'NONE', *, *, #46849, .F. ) ;
#26218=( NAMED_UNIT ( * ) SI_UNIT ( $, .STERADIAN. ) SOLID_ANGLE_UNIT ( ) );
#26243=EDGE_CURVE ( 'NONE', #35975, #86295, #78064, .T. ) ;
#26245=CARTESIAN_POINT ( 'NONE',  ( -7.149690282015371601, -5.000000000000036415, -15.41216073230092753 ) ) ;
#26269=CARTESIAN_POINT ( 'NONE',  ( -5.363597346089342466, 41.33266196706077267, -58.39526881795508473 ) ) ;
#26277=PRODUCT_DEFINITION_CONTEXT ( 'detailed design', #83806, 'design' ) ;
#26296=CARTESIAN_POINT ( 'NONE',  ( 19.42585305423203224, 41.87255863741783912, -80.48841060219729115 ) ) ;
#26298=FACE_OUTER_BOUND ( 'NONE', #37129, .T. ) ;
#26301=( LENGTH_UNIT ( ) NAMED_UNIT ( * ) SI_UNIT ( .MILLI., .METRE. ) );
#26315=CARTESIAN_POINT ( 'NONE',  ( -1.308996937483428491, 49.99999999999999289, -95.00000000000001421 ) ) ;
#26386=VERTEX_POINT ( 'NONE', #19757 ) ;
#26410=ORIENTED_EDGE ( 'NONE', *, *, #72078, .T. ) ;
#26416=CARTESIAN_POINT ( 'NONE',  ( -11.85444436786843525, 42.00000000000000000, -90.56128410203886858 ) ) ;
#26420=SURFACE_STYLE_FILL_AREA ( #45107 ) ;
#26441=ORIENTED_EDGE ( 'NONE', *, *, #66882, .T. ) ;
#26479=CARTESIAN_POINT ( 'NONE',  ( -17.49999999999721823, 50.01864923522455086, 61.58301093894252176 ) ) ;
#26504=CARTESIAN_POINT ( 'NONE',  ( 6.145467200820246667, -3.000000000000002665, -92.99666842291070168 ) ) ;
#26508=CARTESIAN_POINT ( 'NONE',  ( 6.701893401236465486, 41.44328394225253476, -70.59544911815949320 ) ) ;
#26544=CARTESIAN_POINT ( 'NONE',  ( -11.57838703060089358, -4.921403515191947520, -12.56403927680040589 ) ) ;
#26547=CARTESIAN_POINT ( 'NONE',  ( -7.500000000016720847, 43.33959969848450555, -60.00534814812790785 ) ) ;
#26562=CARTESIAN_POINT ( 'NONE',  ( -6.828042834505470893, 41.63841151066672808, -58.95291702778771281 ) ) ;
#26585=( LENGTH_UNIT ( ) NAMED_UNIT ( * ) SI_UNIT ( .MILLI., .METRE. ) );
#26620=CARTESIAN_POINT ( 'NONE',  ( -7.500000000000004441, 44.25000000000000711, -71.71180648257555390 ) ) ;
#26648=( NAMED_UNIT ( * ) SI_UNIT ( $, .STERADIAN. ) SOLID_ANGLE_UNIT ( ) );
#26664=CARTESIAN_POINT ( 'NONE',  ( -1.308996937480700895, 49.99999999999999289, -75.00000000000001421 ) ) ;
#26668=CARTESIAN_POINT ( 'NONE',  ( -7.126323198032135764, 41.48433374936583107, -70.04207028682751002 ) ) ;
#26788=VERTEX_POINT ( 'NONE', #31283 ) ;
#26795=CARTESIAN_POINT ( 'NONE',  ( -58.76133767616301640, 50.00000000000000000, 23.44026136864787446 ) ) ;
#26805=CARTESIAN_POINT ( 'NONE',  ( -37.29474511894800770, 18.64284798593206105, -9.274907802262537970 ) ) ;
#26819=CARTESIAN_POINT ( 'NONE',  ( 29.92008363729422982, 41.07848214471710691, -66.38191137410871079 ) ) ;
#26839=CARTESIAN_POINT ( 'NONE',  ( 10.48543666094595217, 50.00000000000000000, -78.95657223723276275 ) ) ;
#26883=CARTESIAN_POINT ( 'NONE',  ( 0.000000000000000000, -5.000000000000000000, 10.00000000000000000 ) ) ;
#26886=COLOUR_RGB ( '', 0.40784314, 0.44705882, 0.49803922) ;
#26915=( BOUNDED_CURVE ( )  B_SPLINE_CURVE ( 2, ( #96480, #7971, #81323 ),
 .UNSPECIFIED., .F., .F. ) 
 B_SPLINE_CURVE_WITH_KNOTS ( ( 3, 3 ),
 ( 0.000000000000000000, 1.000000000000000000 ),
 .UNSPECIFIED. ) 
 CURVE ( )  GEOMETRIC_REPRESENTATION_ITEM ( )  RATIONAL_B_SPLINE_CURVE ( ( 1.000000000000000000, 1.857142857142858317, 1.000000000000000000 ) ) 
 REPRESENTATION_ITEM ( '' )  );
#26927=CARTESIAN_POINT ( 'NONE',  ( -6.729774149518023663, 41.69338218132584473, -58.98699202062753244 ) ) ;
#26943=LINE ( 'NONE', #75446, #1454 ) ;
#26951=CARTESIAN_POINT ( 'NONE',  ( -7.500000000000007994, 40.00000000000000000, -72.67206406577980715 ) ) ;
#26959=CARTESIAN_POINT ( 'NONE',  ( -9.999999999999994671, -3.000000000000003109, -83.69100306100425257 ) ) ;
#26981=AXIS2_PLACEMENT_3D ( 'NONE', #40180, #81161, #14300 ) ;
#26993=CARTESIAN_POINT ( 'NONE',  ( -12.12626197893092339, -3.000000000000002665, -94.24800833403701006 ) ) ;
#27010=CARTESIAN_POINT ( 'NONE',  ( -17.49999999999995381, 51.39211690089769746, 62.71362001260538932 ) ) ;
#27021=EDGE_LOOP ( 'NONE', ( #20004, #90289, #53712, #36832 ) ) ;
#27025=CARTESIAN_POINT ( 'NONE',  ( -6.738100187484505454, 41.71798639774085160, -59.05424569925489209 ) ) ;
#27065=CARTESIAN_POINT ( 'NONE',  ( 14.90155535905845952, 42.58002643001236720, -90.01374837836192455 ) ) ;
#27067=( NAMED_UNIT ( * ) SI_UNIT ( $, .STERADIAN. ) SOLID_ANGLE_UNIT ( ) );
#27079=CARTESIAN_POINT ( 'NONE',  ( 12.13034742782427955, 41.99999999999999289, -93.82352941176471006 ) ) ;
#27089=CARTESIAN_POINT ( 'NONE',  ( -8.786988139152953468E-15, 18.64300841652315910, 38.36521369532682257 ) ) ;
#27090=CARTESIAN_POINT ( 'NONE',  ( -19.08873399782305569, 49.65827795561243363, 61.75875619398528471 ) ) ;
#27091=CARTESIAN_POINT ( 'NONE',  ( -7.500000000000007105, 39.99999999999562306, -59.88032989330454825 ) ) ;
#27109=CARTESIAN_POINT ( 'NONE',  ( -3.140974613990812792, -5.000000000000002665, -96.68767211932356531 ) ) ;
#27116=ADVANCED_FACE ( 'NONE', ( #68413, #76478 ), #75955, .T. ) ;
#27132=CARTESIAN_POINT ( 'NONE',  ( 8.913811505010652780, 18.64284798592881032, 37.38269509653739675 ) ) ;
#27142=EDGE_LOOP ( 'NONE', ( #77355, #98300, #83131, #20855, #97682 ) ) ;
#27149=ORIENTED_EDGE ( 'NONE', *, *, #594, .F. ) ;
#27151=CARTESIAN_POINT ( 'NONE',  ( -8.904581707875109942, 49.99999999999999289, -97.29851715192089046 ) ) ;
#27172=CARTESIAN_POINT ( 'NONE',  ( -11.85444436786843525, 42.00000000000000000, -90.56128410203886858 ) ) ;
#27198=CARTESIAN_POINT ( 'NONE',  ( -5.036189802311375807, 50.00000000000001421, -93.73786388411662074 ) ) ;
#27199=CARTESIAN_POINT ( 'NONE',  ( -12.49999999999999289, -3.155919820767365547, -14.15697966438807498 ) ) ;
#27201=UNCERTAINTY_MEASURE_WITH_UNIT (LENGTH_MEASURE( 1.000000000000000082E-05 ), #35919, 'distance_accuracy_value', 'NONE');
#27242=CARTESIAN_POINT ( 'NONE',  ( -17.57685455970505473, 45.00000000000000711, 63.18451563121624304 ) ) ;
#27251=CARTESIAN_POINT ( 'NONE',  ( 5.402795611188940583, 41.73472188612398526, -58.79867419242892623 ) ) ;
#27260=ADVANCED_FACE ( 'NONE', ( #21471 ), #77611, .T. ) ;
#27264=COLOUR_RGB ( '', 0.72549020, 0.75294118, 0.79215686) ;
#27276=SURFACE_STYLE_FILL_AREA ( #100574 ) ;
#27282=CARTESIAN_POINT ( 'NONE',  ( 11.99733130325763319, -4.773999631975849312, -12.57663782514914530 ) ) ;
#27296=B_SPLINE_CURVE_WITH_KNOTS ( 'NONE', 3,
 ( #99112, #27422, #68915, #2552, #61351, #52699, #85625, #53768, #35498, #44095, #93173, #20932 ),
 .UNSPECIFIED., .F., .F.,
 ( 4, 2, 2, 2, 2, 4 ),
 ( 0.000000000000000000, 0.1248429703045113720, 0.2498676475284268006, 0.4999170019762576023, 0.7499663564240884872, 1.000000000000000000 ),
 .UNSPECIFIED. ) ;
#27298=CARTESIAN_POINT ( 'NONE',  ( 64.91565662647984425, 48.00000000000000000, 6.815324757469506167 ) ) ;
#27308=VERTEX_POINT ( 'NONE', #29572 ) ;
#27312=CARTESIAN_POINT ( 'NONE',  ( -4.644767399454820200, -5.000000000000039968, -15.65217902603417066 ) ) ;
#27314=CARTESIAN_POINT ( 'NONE',  ( 17.51243376013908559, 50.00000000000000711, 63.32942081862142913 ) ) ;
#27326=CARTESIAN_POINT ( 'NONE',  ( -7.270302578004622873, -3.659675574298181466, -18.03744543697015956 ) ) ;
#27335=SURFACE_SIDE_STYLE ('',( #20317 ) ) ;
#27337=ADVANCED_FACE ( 'NONE', ( #38192 ), #52079, .T. ) ;
#27338=CARTESIAN_POINT ( 'NONE',  ( 6.764423792815447811, 41.48989066009205118, -70.49176070406230110 ) ) ;
#27339=CARTESIAN_POINT ( 'NONE',  ( -65.26738680893376454, 49.99999999999999289, 0.8120011905356555593 ) ) ;
#27362=EDGE_CURVE ( 'NONE', #3104, #60267, #91026, .T. ) ;
#27369=MECHANICAL_DESIGN_GEOMETRIC_PRESENTATION_REPRESENTATION('',(#42778),#35988);
#27379=CARTESIAN_POINT ( 'NONE',  ( -9.739726766105677669, 49.99999999999999289, -82.38252115500968387 ) ) ;
#27388=CARTESIAN_POINT ( 'NONE',  ( -1.308996938995745207, -3.000000000000003553, -95.00000000000000000 ) ) ;
#27391=EDGE_CURVE ( 'NONE', #74620, #5264, #21356, .T. ) ;
#27422=CARTESIAN_POINT ( 'NONE',  ( 5.688070444776314183, -4.337726323045820287, -16.91120255682890061 ) ) ;
#27456=CARTESIAN_POINT ( 'NONE',  ( -6.821510609914083645, 41.53001914905370029, -70.37925568527511189 ) ) ;
#27469=CARTESIAN_POINT ( 'NONE',  ( -52.56483885390523625, 48.00000000000000000, -38.23529411764706509 ) ) ;
#27475=ORIENTED_EDGE ( 'NONE', *, *, #9863, .F. ) ;
#27479=DIRECTION ( 'NONE',  ( 0.000000000000000000, 0.000000000000000000, 1.000000000000000000 ) ) ;
#27482=CARTESIAN_POINT ( 'NONE',  ( 23.57730434126663255, 18.64316884711714906, 30.67950393662606245 ) ) ;
#27492=CARTESIAN_POINT ( 'NONE',  ( 6.578489868540880359, 41.30622290872879887, -58.38226432520261966 ) ) ;
#27493=CARTESIAN_POINT ( 'NONE',  ( -5.500000000000006217, 42.00000000000000000, -58.69229087761261354 ) ) ;
#27571=CARTESIAN_POINT ( 'NONE',  ( 7.996668422911924701, -3.000000000000002665, -78.85453279918097280 ) ) ;
#27580=CARTESIAN_POINT ( 'NONE',  ( -14.24124568368173094, -4.332661967058738739, -11.33228852116109842 ) ) ;
#27601=SURFACE_SIDE_STYLE ('',( #91764 ) ) ;
#27603=CARTESIAN_POINT ( 'NONE',  ( 7.758748231342716295, -5.000000000000001776, -73.00623724565090811 ) ) ;
#27604=CARTESIAN_POINT ( 'NONE',  ( -10.51296777078104050, 50.00000000000000000, -92.64705882352942012 ) ) ;
#27626=CARTESIAN_POINT ( 'NONE',  ( -7.133125787874796231, 41.57692897371567398, -59.23559257119363508 ) ) ;
#27627=CARTESIAN_POINT ( 'NONE',  ( 4.910934285265537547, 41.41789230214733664, -70.63711736860776114 ) ) ;
#27636=EDGE_CURVE ( 'NONE', #33315, #53479, #47239, .T. ) ;
#27647=CARTESIAN_POINT ( 'NONE',  ( 6.043427762771891310, -5.000000000000002665, -74.51456333905348117 ) ) ;
#27692=UNCERTAINTY_MEASURE_WITH_UNIT (LENGTH_MEASURE( 1.000000000000000082E-05 ), #49666, 'distance_accuracy_value', 'NONE');
#27713=( NAMED_UNIT ( * ) PLANE_ANGLE_UNIT ( ) SI_UNIT ( $, .RADIAN. ) );
#27722=CARTESIAN_POINT ( 'NONE',  ( 58.89338521243953295, 40.83722513022537015, -28.14236001438834478 ) ) ;
#27743=CARTESIAN_POINT ( 'NONE',  ( 3.140974613990258568, 50.00000000000000000, -96.68767211932436112 ) ) ;
#27766=CARTESIAN_POINT ( 'NONE',  ( -5.582554154870011054, 41.37363122748190136, -70.85834493696303582 ) ) ;
#27780=CARTESIAN_POINT ( 'NONE',  ( -18.27524112071357720, 45.00000000000001421, 62.41775947855344242 ) ) ;
#27781=CARTESIAN_POINT ( 'NONE',  ( 3.490407211888509836E-12, -4.332980043422162808, 17.83347932686506354 ) ) ;
#27810=( NAMED_UNIT ( * ) SI_UNIT ( $, .STERADIAN. ) SOLID_ANGLE_UNIT ( ) );
#27816=CARTESIAN_POINT ( 'NONE',  ( 11.47222955920350707, -4.944097607773928260, -12.56918813344000263 ) ) ;
#27826=CARTESIAN_POINT ( 'NONE',  ( 7.500000000000000000, -4.999999999999999112, -36.97043916959989929 ) ) ;
#27831=CARTESIAN_POINT ( 'NONE',  ( 65.26738680890606759, 48.00000000000000000, 0.8120011905328435864 ) ) ;
#27836=CARTESIAN_POINT ( 'NONE',  ( -6.678341091416172048, 41.85887519985161731, -59.41504748149177573 ) ) ;
#27870=PRESENTATION_STYLE_ASSIGNMENT (( #76887 ) ) ;
#27872=CARTESIAN_POINT ( 'NONE',  ( 6.299403769935631558, 41.97741512816498499, -69.49222142767905552 ) ) ;
#27873=CARTESIAN_POINT ( 'NONE',  ( -64.91565662645538737, 49.99999999999999289, 6.815324757469617190 ) ) ;
#27896=CARTESIAN_POINT ( 'NONE',  ( 33.09320956684935311, 40.69741856558304960, -62.14400065382765348 ) ) ;
#27911=CARTESIAN_POINT ( 'NONE',  ( 52.56483885390523625, 48.00000000000000000, -38.23529411764706509 ) ) ;
#27913=CARTESIAN_POINT ( 'NONE',  ( 7.374560640984048732, 50.00000000000000000, -94.59600210749853488 ) ) ;
#27914=ADVANCED_FACE ( 'NONE', ( #30368 ), #36885, .F. ) ;
#27940=VERTEX_POINT ( 'NONE', #72390 ) ;
#27989=CARTESIAN_POINT ( 'NONE',  ( -6.583551121182180665, 41.48989065997584191, -70.62107025447927811 ) ) ;
#27994=CARTESIAN_POINT ( 'NONE',  ( -5.411616755802471701, 41.81753649772627313, -58.91471509483435653 ) ) ;
#28001=CARTESIAN_POINT ( 'NONE',  ( 12.50000000000000178, -1.322514027130966552, -16.28752260425741483 ) ) ;
#28009=CARTESIAN_POINT ( 'NONE',  ( 6.542885630808934927, 41.77241054322398384, -59.03854290128418825 ) ) ;
#28010=CARTESIAN_POINT ( 'NONE',  ( -30.67950393659633335, 18.64316884710269662, -23.57730434127810426 ) ) ;
#28016=ORIENTED_EDGE ( 'NONE', *, *, #45590, .F. ) ;
#28038=CARTESIAN_POINT ( 'NONE',  ( 7.404344845520721030, 40.29318110125479535, -70.39066561776979825 ) ) ;
#28045=PRESENTATION_STYLE_ASSIGNMENT (( #38765 ) ) ;
#28057=CARTESIAN_POINT ( 'NONE',  ( -14.61924042696810488, -4.999999999997926103, -89.34162378225578038 ) ) ;
#28071=CARTESIAN_POINT ( 'NONE',  ( -12.13034742782427955, -79.93083296558610584, -93.82352941176471006 ) ) ;
#28096=CARTESIAN_POINT ( 'NONE',  ( -6.145467200824362486, -3.000000000000002665, -77.00333157709341947 ) ) ;
#28121=ORIENTED_EDGE ( 'NONE', *, *, #82894, .F. ) ;
#28125=PRESENTATION_STYLE_ASSIGNMENT (( #19514 ) ) ;
#28127=CARTESIAN_POINT ( 'NONE',  ( 6.827804075700396602, -4.999999999999998224, -71.19745154229144646 ) ) ;
#28134=CARTESIAN_POINT ( 'NONE',  ( -11.57268198878043286, -4.922585413835529167, -12.56430962643118399 ) ) ;
#28151=CARTESIAN_POINT ( 'NONE',  ( -19.27294821357206089, 49.83929858697661786, 61.40513943499198035 ) ) ;
#28152=( NAMED_UNIT ( * ) SI_UNIT ( $, .STERADIAN. ) SOLID_ANGLE_UNIT ( ) );
#28167=CARTESIAN_POINT ( 'NONE',  ( 5.294000222838083580, 18.59362110858084804, -37.95364038139827301 ) ) ;
#28168=CARTESIAN_POINT ( 'NONE',  ( 12.45023096947980967, -3.972485752774072676, -13.21587846007173361 ) ) ;
#28170=CARTESIAN_POINT ( 'NONE',  ( -3.140956913508186954, -4.999999999999999112, -16.11495416415134940 ) ) ;
#28173=SURFACE_SIDE_STYLE ('',( #53475 ) ) ;
#28183=FACE_OUTER_BOUND ( 'NONE', #22800, .T. ) ;
#28187=( BOUNDED_CURVE ( )  B_SPLINE_CURVE ( 2, ( #67145, #49881, #75212 ),
 .UNSPECIFIED., .F., .T. ) 
 B_SPLINE_CURVE_WITH_KNOTS ( ( 3, 3 ),
 ( 0.000000000000000000, 1.000000000000000000 ),
 .UNSPECIFIED. ) 
 CURVE ( )  GEOMETRIC_REPRESENTATION_ITEM ( )  RATIONAL_B_SPLINE_CURVE ( ( 1.000000000000000000, 1.857142857142858317, 1.000000000000000000 ) ) 
 REPRESENTATION_ITEM ( '' )  );
#28215=CARTESIAN_POINT ( 'NONE',  ( -10.74465425724631373, 49.99999999999999289, -95.72854256506849424 ) ) ;
#28221=CARTESIAN_POINT ( 'NONE',  ( 19.35735956073687802, 49.90708382027017365, 61.17470024478517132 ) ) ;
#28226=( GEOMETRIC_REPRESENTATION_CONTEXT ( 3 ) GLOBAL_UNCERTAINTY_ASSIGNED_CONTEXT ( ( #27692 ) ) GLOBAL_UNIT_ASSIGNED_CONTEXT ( ( #49666, #6545, #105259 ) ) REPRESENTATION_CONTEXT ( 'NONE', 'WORKASPACE' ) );
#28236=CARTESIAN_POINT ( 'NONE',  ( 11.85444436786839084, 42.00000000000000000, -90.56128410203886858 ) ) ;
#28244=CARTESIAN_POINT ( 'NONE',  ( 28.77239501610283412, 40.83805528215972203, 58.36093113040321612 ) ) ;
#28262=CARTESIAN_POINT ( 'NONE',  ( 1.570796324980112679, 50.00000000000000000, -97.00000000000000000 ) ) ;
#28263=DIRECTION ( 'NONE',  ( 0.000000000000000000, 1.000000000000000000, 0.000000000000000000 ) ) ;
#28275=CARTESIAN_POINT ( 'NONE',  ( -1.727368016638141196E-09, 38.95322581935191408, 63.66965480466879512 ) ) ;
#28277=CARTESIAN_POINT ( 'NONE',  ( -7.500000000000000000, -3.000000000000000000, -20.99851272547259384 ) ) ;
#28285=CARTESIAN_POINT ( 'NONE',  ( -6.561889531081967597, 40.92548620270399340, -71.07459846643517665 ) ) ;
#28297=CARTESIAN_POINT ( 'NONE',  ( -17.49999999999997513, 45.00000000000000711, 64.09953197936602010 ) ) ;
#28312=ORIENTED_EDGE ( 'NONE', *, *, #42087, .T. ) ;
#28338=CARTESIAN_POINT ( 'NONE',  ( 9.739726766683151737, 48.00000000000000711, -87.61747884359282068 ) ) ;
#28341=CARTESIAN_POINT ( 'NONE',  ( 2.617478843592800697, -3.000000000000003109, -75.26027323331686603 ) ) ;
#28344=( NAMED_UNIT ( * ) SI_UNIT ( $, .STERADIAN. ) SOLID_ANGLE_UNIT ( ) );
#28349=CARTESIAN_POINT ( 'NONE',  ( -6.780293022259969327, 41.80198833643462564, -59.33023405483342572 ) ) ;
#28362=CARTESIAN_POINT ( 'NONE',  ( 17.61979786233769829, 50.00000000000000711, 62.60467660056798422 ) ) ;
#28388=CARTESIAN_POINT ( 'NONE',  ( -51.78317192863611496, 49.99999999999999289, 39.73656039226784742 ) ) ;
#28389=CARTESIAN_POINT ( 'NONE',  ( 12.50000000000000000, -2.999999999999996891, -14.34180675897363955 ) ) ;
#28409=CARTESIAN_POINT ( 'NONE',  ( 33.08652920850916956, 40.69826037889563253, -62.15288412041942934 ) ) ;
#28413=DIRECTION ( 'NONE',  ( 1.000000000000000000, 0.000000000000000000, -1.160749806054361473E-16 ) ) ;
#28425=CARTESIAN_POINT ( 'NONE',  ( 1.224646799147352073E-15, 49.99999999999999289, -75.00000000000001421 ) ) ;
#28462=EDGE_CURVE ( 'NONE', #61410, #78701, #47031, .T. ) ;
#28472=CARTESIAN_POINT ( 'NONE',  ( -17.97976569284698911, 49.99999999999999289, 61.91457000261350885 ) ) ;
#28506=CARTESIAN_POINT ( 'NONE',  ( -6.299401076687714429, 41.97741539014224088, -69.49222273704066311 ) ) ;
#28511=CARTESIAN_POINT ( 'NONE',  ( -6.586014515853777951, 41.68775576351381318, -58.88021171896449601 ) ) ;
#28532=( NAMED_UNIT ( * ) SI_UNIT ( $, .STERADIAN. ) SOLID_ANGLE_UNIT ( ) );
#28536=CARTESIAN_POINT ( 'NONE',  ( -29.83308852634790043, 42.00000000000000000, -51.76085035113232635 ) ) ;
#28544=CARTESIAN_POINT ( 'NONE',  ( 7.040774347399621824, 41.35742771039598153, -58.68913404742972517 ) ) ;
#28560=CARTESIAN_POINT ( 'NONE',  ( 7.311411528619694344, 40.00000000267693423, -70.68779756257029590 ) ) ;
#28574=( GEOMETRIC_REPRESENTATION_CONTEXT ( 3 ) GLOBAL_UNCERTAINTY_ASSIGNED_CONTEXT ( ( #34346 ) ) GLOBAL_UNIT_ASSIGNED_CONTEXT ( ( #91963, #18638, #26218 ) ) REPRESENTATION_CONTEXT ( 'NONE', 'WORKASPACE' ) );
#28579=CARTESIAN_POINT ( 'NONE',  ( 10.19007819943910143, -5.000000000014482637, -96.34610920171921578 ) ) ;
#28604=CARTESIAN_POINT ( 'NONE',  ( -17.49999999999997513, 52.00000000000000711, 59.91915230424417160 ) ) ;
#28605=ORIENTED_EDGE ( 'NONE', *, *, #98111, .F. ) ;
#28633=CARTESIAN_POINT ( 'NONE',  ( -13.20528892216319683, -4.332661967060645658, 12.52414413171502439 ) ) ;
#28668=CARTESIAN_POINT ( 'NONE',  ( -7.500000000000007105, 40.95611321456068055, -60.73832539154658861 ) ) ;
#28673=LINE ( 'NONE', #77188, #104650 ) ;
#28683=CARTESIAN_POINT ( 'NONE',  ( 6.472171899339533852, 40.92674694738754226, -71.09138916011745835 ) ) ;
#28704=CARTESIAN_POINT ( 'NONE',  ( 3.140974613991526887, -5.000000000000002665, -96.68767211932356531 ) ) ;
#28733=CARTESIAN_POINT ( 'NONE',  ( 9.610124387818546055, -5.000000000000000000, -77.63937538515727965 ) ) ;
#28745=CARTESIAN_POINT ( 'NONE',  ( -2.354803500934600891, 50.00000000000001421, -100.0000000000000000 ) ) ;
#28754=UNCERTAINTY_MEASURE_WITH_UNIT (LENGTH_MEASURE( 1.000000000000000082E-05 ), #93708, 'distance_accuracy_value', 'NONE');
#28762=CARTESIAN_POINT ( 'NONE',  ( -4.905843853654967113, -4.999999999999999112, -16.52456679617691293 ) ) ;
#28765=CARTESIAN_POINT ( 'NONE',  ( 34.55744730647673890, 42.66432393376602761, -62.99136456808676598 ) ) ;
#28774=DIRECTION ( 'NONE',  ( -0.000000000000000000, 1.000000000000000000, -0.000000000000000000 ) ) ;
#28777=CARTESIAN_POINT ( 'NONE',  ( 47.37019975563026719, 41.99999999991776178, 36.40416150969240050 ) ) ;
#28783=CARTESIAN_POINT ( 'NONE',  ( 65.26569950619781935, 39.42419746932910840, 0.7618753667456097389 ) ) ;
#28785=B_SPLINE_CURVE_WITH_KNOTS ( 'NONE', 3,
 ( #81695, #48806, #83315, #82246, #32133, #106520, #99483, #7821, #9953, #57969, #66605, #65011, #50401 ),
 .UNSPECIFIED., .F., .F.,
 ( 4, 1, 1, 1, 1, 1, 2, 2, 4 ),
 ( 0.000000000000000000, 0.2500000000000132117, 0.3750000000000142109, 0.4375000000000099920, 0.4687500000000078826, 0.4843750000000114908, 0.4921875000000120459, 0.5000000000000125455, 1.000000000000000000 ),
 .UNSPECIFIED. ) ;
#28803=CARTESIAN_POINT ( 'NONE',  ( -6.043427762773251111, 50.00000000000000000, -95.48543666094653304 ) ) ;
#28808=CARTESIAN_POINT ( 'NONE',  ( 0.000000000000000000, 0.000000000000000000, 8.000000000000000000 ) ) ;
#28818=CARTESIAN_POINT ( 'NONE',  ( -12.50000000000000000, -3.000000000000003109, -14.34180675897363599 ) ) ;
#28832=( BOUNDED_SURFACE ( )  B_SPLINE_SURFACE ( 2, 3, ( 
 ( #87361, #37243, #104052, #102475, #13441, #30190, #63625, #94396 ),
 ( #103532, #4843, #5377, #94933, #12909, #29167, #45835, #63079 ),
 ( #37776, #95979, #14492, #77675, #3785, #97024, #15037, #47927 ) ),
 .UNSPECIFIED., .F., .F., .F. ) 
 B_SPLINE_SURFACE_WITH_KNOTS ( ( 3, 3 ),
 ( 4, 2, 2, 4 ),
 ( 0.000000000000000000, 1.000000000000000000 ),
 ( 3.001947784535673236, 3.049999786562399784, 3.233185520617186448, 3.281237522643912996 ),
 .UNSPECIFIED. ) 
 GEOMETRIC_REPRESENTATION_ITEM ( )  RATIONAL_B_SPLINE_SURFACE ( (
 ( 1.000000000000000000, 1.000000000000000000, 1.000000000000000000, 1.000000000000000000, 1.000000000000000000, 1.000000000000000000, 1.000000000000000000, 1.000000000000000000),
 ( 1.857142857142858317, 1.857142857142858317, 1.857142857142858317, 1.857142857142858317, 1.857142857142858317, 1.857142857142858317, 1.857142857142858317, 1.857142857142858317),
 ( 1.000000000000000000, 1.000000000000000000, 1.000000000000000000, 1.000000000000000000, 1.000000000000000000, 1.000000000000000000, 1.000000000000000000, 1.000000000000000000) ) ) 
 REPRESENTATION_ITEM ( '' )  SURFACE ( )  );
#28833=CARTESIAN_POINT ( 'NONE',  ( -6.309244321879762474, 40.00000000008454748, -71.19739392704494207 ) ) ;
#28844=CARTESIAN_POINT ( 'NONE',  ( -17.53083185432715396, 45.00000000000000711, 63.44709590376286457 ) ) ;
#28874=CARTESIAN_POINT ( 'NONE',  ( 7.421727621019012844, -2.999999999999999112, -70.37058875308096617 ) ) ;
#28890=CARTESIAN_POINT ( 'NONE',  ( 6.145467199749146125, 47.99999999999999289, -92.99666842398180222 ) ) ;
#28897=CARTESIAN_POINT ( 'NONE',  ( 22.66220480930525127, 50.00000000000000000, 59.06576954297840842 ) ) ;
#28903=CARTESIAN_POINT ( 'NONE',  ( -5.744149845079463468, 41.99823332147487065, -59.60979981975896891 ) ) ;
#28925=SURFACE_STYLE_USAGE ( .BOTH. , #79536 ) ;
#28933=CARTESIAN_POINT ( 'NONE',  ( 0.000000000000000000, 0.000000000000000000, 0.000000000000000000 ) ) ;
#28936=CARTESIAN_POINT ( 'NONE',  ( 6.675188390063539146, 41.63185015293624502, -70.36443416096713577 ) ) ;
#28945=ORIENTED_EDGE ( 'NONE', *, *, #69551, .T. ) ;
#28958=CARTESIAN_POINT ( 'NONE',  ( 17.50000000000002487, 45.90000000000000568, 62.61746187599675295 ) ) ;
#28972=CARTESIAN_POINT ( 'NONE',  ( 52.56491209535273867, 39.42572890907101169, -38.23519342730394044 ) ) ;
#28977=SURFACE_STYLE_FILL_AREA ( #19296 ) ;
#28980=CARTESIAN_POINT ( 'NONE',  ( 5.036189802310915731, 48.00000000000000000, -76.26213611587833441 ) ) ;
#28997=SHAPE_REPRESENTATION_RELATIONSHIP ( 'NONE' , 'NONE' ,  #52881, #75546 ) ;
#29007=FILL_AREA_STYLE ('',( #69943 ) ) ;
#29010=CARTESIAN_POINT ( 'NONE',  ( -5.354260345751012728, 36.72647500040412183, -54.26263299992344713 ) ) ;
#29026=CARTESIAN_POINT ( 'NONE',  ( -36.15880341458275637, 40.31104264147870708, -58.06768400292240528 ) ) ;
#29027=CARTESIAN_POINT ( 'NONE',  ( -18.09799070311343527, 49.99999999999999289, 61.76230565999977529 ) ) ;
#29042=CARTESIAN_POINT ( 'NONE',  ( -12.44754381327812354, 42.20908535986962562, -93.38745647781213677 ) ) ;
#29061=CARTESIAN_POINT ( 'NONE',  ( -1.494796585009948497, -5.000000000000002665, -71.77219432632048779 ) ) ;
#29062=CARTESIAN_POINT ( 'NONE',  ( -5.788216603250401882, 41.97741512851646917, -69.85767952489079846 ) ) ;
#29066=CARTESIAN_POINT ( 'NONE',  ( -11.77542311866812774, -5.000000000000000000, -11.45362038306368646 ) ) ;
#29067=CARTESIAN_POINT ( 'NONE',  ( -5.668939695963768344, 41.88723863199725628, -59.02759498664629945 ) ) ;
#29086=CARTESIAN_POINT ( 'NONE',  ( 7.054522925320324767, 41.71556257522360767, -59.55896313260248576 ) ) ;
#29088=CARTESIAN_POINT ( 'NONE',  ( -5.022013495247517945, 18.64316884711714195, -38.36535705883633085 ) ) ;
#29098=COLOUR_RGB ( '', 0.09019608, 0.27058824, 0.51372549) ;
#29122=CARTESIAN_POINT ( 'NONE',  ( -12.03765877768534942, -4.743370302668000527, -76.84911689414364844 ) ) ;
#29135=CARTESIAN_POINT ( 'NONE',  ( -4.766030446259712505, -5.000000000000002665, -97.32770387339404294 ) ) ;
#29138=( BOUNDED_CURVE ( )  B_SPLINE_CURVE ( 2, ( #95992, #71687, #56022 ),
 .UNSPECIFIED., .F., .F. ) 
 B_SPLINE_CURVE_WITH_KNOTS ( ( 3, 3 ),
 ( 0.000000000000000000, 1.000000000000000000 ),
 .UNSPECIFIED. ) 
 CURVE ( )  GEOMETRIC_REPRESENTATION_ITEM ( )  RATIONAL_B_SPLINE_CURVE ( ( 1.000000000000000000, 1.857142857142858317, 1.000000000000000000 ) ) 
 REPRESENTATION_ITEM ( '' )  );
#29157=ORIENTED_EDGE ( 'NONE', *, *, #41966, .F. ) ;
#29167=CARTESIAN_POINT ( 'NONE',  ( -6.362990258380357034, 42.00000000000000711, -58.90232955951056226 ) ) ;
#29179=CARTESIAN_POINT ( 'NONE',  ( 3.328192429499065685, -5.000000000000000000, 16.34245136408155830 ) ) ;
#29204=CARTESIAN_POINT ( 'NONE',  ( 19.25558504890851097, 49.82459671548976843, 61.44364156091821627 ) ) ;
#29227=CARTESIAN_POINT ( 'NONE',  ( 6.035608966186244650, 41.34018742956621395, -70.92167700592624158 ) ) ;
#29238=CARTESIAN_POINT ( 'NONE',  ( 12.48484554125298907, -3.563252358774177342, -13.68093487574958012 ) ) ;
#29242=CARTESIAN_POINT ( 'NONE',  ( 1.308996937483426937, -5.000000000000002665, -75.00000000000001421 ) ) ;
#29243=MECHANICAL_DESIGN_GEOMETRIC_PRESENTATION_REPRESENTATION('',(#20636),#56734);
#29257=B_SPLINE_SURFACE_WITH_KNOTS ( 'NONE', 3, 3, ( 
 ( #35924, #42909, #51519, #74721, #68795, #58571, #1895, #805, #66650, #67194 ),
 ( #83356, #34849, #67718, #35383, #58011, #68250, #90936, #8930, #99532, #91468 ),
 ( #17584, #86583, #94115, #69846, #36458, #45578, #13179, #20818, #53652, #12123 ),
 ( #53131, #78987, #28349, #5111, #37515, #38042, #61229, #70903, #103793, #78459 ),
 ( #102742, #4579, #45052, #27836, #70378, #60707, #86048, #20280, #77937, #21323 ),
 ( #4045, #12647, #36978, #93590, #61776, #103273, #29423, #29936, #28903, #94673 ),
 ( #62300, #95192, #54159, #87102, #46104, #62821, #19742, #52580, #85504, #11585 ),
 ( #44512, #77401, #3517, #69324, #102204, #25524, #65413, #90216, #56769, #89693 ) ),
 .UNSPECIFIED., .F., .F., .F.,
 ( 4, 2, 2, 4 ),
 ( 4, 2, 2, 2, 4 ),
 ( 0.000000000000000000, 0.2500000000000000000, 0.5000000000000000000, 1.000000000000000000 ),
 ( 0.000000000000000000, 0.1250000000000000000, 0.2500000000000000000, 0.5000000000000000000, 1.000000000000000000 ),
 .UNSPECIFIED. ) ;
#29259=AXIS2_PLACEMENT_3D ( 'NONE', #61461, #79743, #55449 ) ;
#29265=AXIS2_PLACEMENT_3D ( 'NONE', #28933, #19250, #52077 ) ;
#29292=CARTESIAN_POINT ( 'NONE',  ( 52.56483885390523625, 40.83906611471594061, -38.23529411764706509 ) ) ;
#29300=CARTESIAN_POINT ( 'NONE',  ( 33.52312678243841759, 18.64316884716171785, -19.32152200345659665 ) ) ;
#29307=CARTESIAN_POINT ( 'NONE',  ( -64.12661792344870548, 39.42592270507808649, -11.02918813174155588 ) ) ;
#29316=CARTESIAN_POINT ( 'NONE',  ( 1.966965783804971668, 41.99999999999999289, -67.70628254661242806 ) ) ;
#29331=CARTESIAN_POINT ( 'NONE',  ( -16.51907061138353683, 42.00139744608745218, -87.79003255390435356 ) ) ;
#29334=EDGE_CURVE ( 'NONE', #18823, #34787, #103596, .T. ) ;
#29350=CARTESIAN_POINT ( 'NONE',  ( -5.563665798473262036, 41.08730335088894492, -70.97074924948610430 ) ) ;
#29372=CARTESIAN_POINT ( 'NONE',  ( -12.50000000000000711, 39.61136555405652615, -64.51031429804609729 ) ) ;
#29383=CARTESIAN_POINT ( 'NONE',  ( 6.933421894041627453, 41.67527100805288853, -59.13217572147580370 ) ) ;
#29389=CARTESIAN_POINT ( 'NONE',  ( 7.500000000000001776, -7.939616441372559841, -16.39477006944641957 ) ) ;
#29401=CARTESIAN_POINT ( 'NONE',  ( 7.500000000000007105, 42.00000000000000711, -65.90297133634214788 ) ) ;
#29403=AXIS2_PLACEMENT_3D ( 'NONE', #102981, #106678, #57059 ) ;
#29418=CARTESIAN_POINT ( 'NONE',  ( -64.32759900504490247, 48.00000000000000000, -11.06576400629244361 ) ) ;
#29422=CARTESIAN_POINT ( 'NONE',  ( -14.07141259107696918, 41.78883758875669230, -79.52223649356207602 ) ) ;
#29423=CARTESIAN_POINT ( 'NONE',  ( -6.364223809941345067, 41.95991738832010043, -59.61869671383132641 ) ) ;
#29425=CARTESIAN_POINT ( 'NONE',  ( 12.12955763321374114, -4.669738190590866367, -76.82128316853251704 ) ) ;
#29444=PRESENTATION_STYLE_ASSIGNMENT (( #28925 ) ) ;
#29455=CARTESIAN_POINT ( 'NONE',  ( 6.074379128844155318, 41.75280174920714416, -70.48890179791422383 ) ) ;
#29496=CARTESIAN_POINT ( 'NONE',  ( 7.996668422908976837, 49.99999999999999289, -78.85453279918145597 ) ) ;
#29524=( LENGTH_UNIT ( ) NAMED_UNIT ( * ) SI_UNIT ( .MILLI., .METRE. ) );
#29530=COLOUR_RGB ( '', 0.66274510, 0.83137255, 0.94901961) ;
#29536=( LENGTH_UNIT ( ) NAMED_UNIT ( * ) SI_UNIT ( .MILLI., .METRE. ) );
#29537=CARTESIAN_POINT ( 'NONE',  ( -18.92758526587351398, 50.00000000000000711, 60.68418741241684700 ) ) ;
#29551=ORIENTED_EDGE ( 'NONE', *, *, #38218, .F. ) ;
#29572=CARTESIAN_POINT ( 'NONE',  ( 17.50000000000004974, 48.00000000000341771, 64.09949417230997426 ) ) ;
#29573=CARTESIAN_POINT ( 'NONE',  ( -6.403344576203515714, 41.95607710195889695, -69.22843915075077348 ) ) ;
#29579=CARTESIAN_POINT ( 'NONE',  ( -5.662864552301164700, 41.84935256917250967, -58.94136742042883981 ) ) ;
#29588=EDGE_LOOP ( 'NONE', ( #52114, #74857, #100245, #13383, #94025, #80438 ) ) ;
#29597=FACE_OUTER_BOUND ( 'NONE', #14128, .T. ) ;
#29598=CARTESIAN_POINT ( 'NONE',  ( -47.37019975550713724, 41.99999999999999289, 36.40416150952766827 ) ) ;
#29618=DIRECTION ( 'NONE',  ( 0.000000000000000000, 0.000000000000000000, 1.000000000000000000 ) ) ;
#29632=FACE_OUTER_BOUND ( 'NONE', #23160, .T. ) ;
#29646=CARTESIAN_POINT ( 'NONE',  ( -2.751706330279349633, -5.000000000000015987, -99.99999999999998579 ) ) ;
#29678=DIRECTION ( 'NONE',  ( 0.000000000000000000, 1.000000000000000000, 0.000000000000000000 ) ) ;
#29716=CARTESIAN_POINT ( 'NONE',  ( 19.37147048651776871, 49.91798333626284290, 61.09697252333796769 ) ) ;
#29739=CARTESIAN_POINT ( 'NONE',  ( -6.917891564935159998, 41.82074884801031800, -68.91429205806258551 ) ) ;
#29740=CARTESIAN_POINT ( 'NONE',  ( 5.556067581535544697, 40.28998946031890682, -71.04001546082351126 ) ) ;
#29743=CARTESIAN_POINT ( 'NONE',  ( 10.50000000000000711, -5.000000000000000000, -79.51734232575269345 ) ) ;
#29756=CARTESIAN_POINT ( 'NONE',  ( 5.202160958754947551, 4.715235442947979472, -25.39438984414672262 ) ) ;
#29760=CARTESIAN_POINT ( 'NONE',  ( 7.996668422911924701, -3.000000000000002665, -78.85453279918097280 ) ) ;
#29795=( LENGTH_UNIT ( ) NAMED_UNIT ( * ) SI_UNIT ( .MILLI., .METRE. ) );
#29814=CARTESIAN_POINT ( 'NONE',  ( 25.69972685279896751, 43.60477215666053752, -75.16871690720786603 ) ) ;
#29822=CARTESIAN_POINT ( 'NONE',  ( -30.67950393659633335, 18.64316884710269662, -23.57730434127810426 ) ) ;
#29829=CARTESIAN_POINT ( 'NONE',  ( 28.77268538114685015, 39.42481758554652060, 58.36079874883185425 ) ) ;
#29847=CARTESIAN_POINT ( 'NONE',  ( -2.617478844988693432, 48.00000000000000000, -94.73972676610495114 ) ) ;
#29853=CARTESIAN_POINT ( 'NONE',  ( 1.647285698089613781, 39.99999999999999289, -70.00000000000000000 ) ) ;
#29860=CARTESIAN_POINT ( 'NONE',  ( 7.711337099629008485, -4.999999999999998224, -15.67927777788488974 ) ) ;
#29874=CARTESIAN_POINT ( 'NONE',  ( -4.852941176470602080, 40.00000000000033396, -70.80672828634229177 ) ) ;
#29898=CARTESIAN_POINT ( 'NONE',  ( 6.831363830528337289, 41.73171983268898089, -59.17722554277374059 ) ) ;
#29925=CARTESIAN_POINT ( 'NONE',  ( 9.739726766683151737, -3.000000000000003109, -82.38252115640720774 ) ) ;
#29930=CARTESIAN_POINT ( 'NONE',  ( 43.69716417795766006, 49.99999999997997691, 48.48761666245326296 ) ) ;
#29936=CARTESIAN_POINT ( 'NONE',  ( -5.989969354119776490, 41.99624786690075950, -59.62337049591117477 ) ) ;
#29938=CARTESIAN_POINT ( 'NONE',  ( 12.42907082493752569, -4.067133856148627657, -76.73301493501968196 ) ) ;
#29957=CARTESIAN_POINT ( 'NONE',  ( 60.68787119177670064, 50.00000000000000000, 17.09822573326192696 ) ) ;
#29976=CARTESIAN_POINT ( 'NONE',  ( -6.733158593834142280, 41.46658730094299017, -70.54360490943875561 ) ) ;
#30019=CARTESIAN_POINT ( 'NONE',  ( -7.251642494156320673, 41.54835750584366849, -68.91429205799529711 ) ) ;
#30050=CARTESIAN_POINT ( 'NONE',  ( -18.04869413793490551, 50.00000000000000711, 61.82439970906034432 ) ) ;
#30069=CARTESIAN_POINT ( 'NONE',  ( -13.43456000506750847, 42.84369539968772500, -92.03053355450553852 ) ) ;
#30088=( NAMED_UNIT ( * ) PLANE_ANGLE_UNIT ( ) SI_UNIT ( $, .RADIAN. ) );
#30089=CARTESIAN_POINT ( 'NONE',  ( -5.787480046464959393, 41.99999999999999289, -68.91429205815936143 ) ) ;
#30094=CARTESIAN_POINT ( 'NONE',  ( -1.663454779230262526, -5.000000000000002665, 16.34255157462185792 ) ) ;
#30095=CARTESIAN_POINT ( 'NONE',  ( -6.592761362570266570, 41.57274138842281985, -58.68933574041189161 ) ) ;
#30108=CARTESIAN_POINT ( 'NONE',  ( 5.448357755207406505, 41.97585525106359228, -59.38396075874230462 ) ) ;
#30113=ORIENTED_EDGE ( 'NONE', *, *, #90756, .F. ) ;
#30119=EDGE_CURVE ( 'NONE', #55315, #86295, #93281, .T. ) ;
#30130=LINE ( 'NONE', #63017, #20138 ) ;
#30145=ORIENTED_EDGE ( 'NONE', *, *, #72484, .F. ) ;
#30159=CARTESIAN_POINT ( 'NONE',  ( 12.71180608318734251, -4.333298119783789204, 12.63015221159040991 ) ) ;
#30161=ADVANCED_FACE ( 'NONE', ( #6064 ), #73685, .F. ) ;
#30167=SURFACE_SIDE_STYLE ('',( #104024 ) ) ;
#30190=CARTESIAN_POINT ( 'NONE',  ( -6.459123244420534427, 42.00000000000000000, -59.79223455627018780 ) ) ;
#30214=CARTESIAN_POINT ( 'NONE',  ( -37.48925363931288501, 48.00000000000000711, 53.34938573421634800 ) ) ;
#30222=ORIENTED_EDGE ( 'NONE', *, *, #106727, .T. ) ;
#30226=CARTESIAN_POINT ( 'NONE',  ( 18.97538325432419981, 49.43284846044564063, 61.96509015790782371 ) ) ;
#30240=ORIENTED_EDGE ( 'NONE', *, *, #89542, .F. ) ;
#30248=ORIENTED_EDGE ( 'NONE', *, *, #30311, .T. ) ;
#30258=CARTESIAN_POINT ( 'NONE',  ( 12.50000000000000711, -4.999999999999999112, -79.51734232575269345 ) ) ;
#30262=CARTESIAN_POINT ( 'NONE',  ( 18.43654383764750548, 45.00000000000002132, 62.34954961627184389 ) ) ;
#30277=CARTESIAN_POINT ( 'NONE',  ( 7.996668422910221175, -5.000000000000002665, -78.85453279918266389 ) ) ;
#30293=EDGE_LOOP ( 'NONE', ( #31065, #7260, #45068, #58300 ) ) ;
#30311=EDGE_CURVE ( 'NONE', #5264, #53678, #28673, .T. ) ;
#30315=ORIENTED_EDGE ( 'NONE', *, *, #63299, .T. ) ;
#30318=CARTESIAN_POINT ( 'NONE',  ( -51.48757442383523397, 38.95383793070303113, -37.45149417477429665 ) ) ;
#30325=( NAMED_UNIT ( * ) PLANE_ANGLE_UNIT ( ) SI_UNIT ( $, .RADIAN. ) );
#30329=CARTESIAN_POINT ( 'NONE',  ( 43.59534864137770427, 41.43266498251605157, -50.56630447086893554 ) ) ;
#30339=CARTESIAN_POINT ( 'NONE',  ( -30.67950393662606956, 18.64316884711714906, 23.57730434126661834 ) ) ;
#30345=CARTESIAN_POINT ( 'NONE',  ( -57.68978467818401157, 38.95207517830731092, -27.56125053296379690 ) ) ;
#30367=CARTESIAN_POINT ( 'NONE',  ( 8.737863884121436442, 48.00000000000000000, -79.96381019768851672 ) ) ;
#30368=FACE_OUTER_BOUND ( 'NONE', #81638, .T. ) ;
#30415=CARTESIAN_POINT ( 'NONE',  ( -12.50000000000000533, 33.01231111522088923, -51.52182527394435141 ) ) ;
#30416=CARTESIAN_POINT ( 'NONE',  ( 5.484632749660399931, 41.99999999999999289, -59.73832504088978368 ) ) ;
#30426=CARTESIAN_POINT ( 'NONE',  ( 0.000000000000000000, 49.99999999999999289, -95.00000000000000000 ) ) ;
#30427=CARTESIAN_POINT ( 'NONE',  ( 7.395123142502173508, 40.93288834207328364, -59.01287878374339613 ) ) ;
#30437=CARTESIAN_POINT ( 'NONE',  ( 6.256238905933717120, -3.000000000000470290, -71.20382035666703757 ) ) ;
#30448=CARTESIAN_POINT ( 'NONE',  ( 5.500000000000006217, 42.00000000000000000, -59.28631038546474485 ) ) ;
#30462=CARTESIAN_POINT ( 'NONE',  ( 28.89099332389485042, 49.99999999997997691, 58.53034795348389707 ) ) ;
#30473=CARTESIAN_POINT ( 'NONE',  ( 18.42142964856622811, 49.99999999999999289, 61.35851441441231913 ) ) ;
#30484=CARTESIAN_POINT ( 'NONE',  ( 62.57102314643675811, 50.00000000000000000, -7.448774052006193358 ) ) ;
#30501=CARTESIAN_POINT ( 'NONE',  ( -5.787521267941007963, 41.99999999999999289, -59.87256577776128097 ) ) ;
#30502=AXIS2_PLACEMENT_3D ( 'NONE', #62550, #29678, #4303 ) ;
#30534=CARTESIAN_POINT ( 'NONE',  ( 1.836970198721029983E-15, 0.000000000000000000, -15.00000000000000178 ) ) ;
#30539=CARTESIAN_POINT ( 'NONE',  ( 1.308996937483426715, 48.00000000000000000, -95.00000000000000000 ) ) ;
#30559=CARTESIAN_POINT ( 'NONE',  ( 4.175893272575727622, -4.999999999998865796, -7.137815226411304614 ) ) ;
#30562=CARTESIAN_POINT ( 'NONE',  ( -5.292662561255604636, 18.30812576678731318, -37.69621763902263467 ) ) ;
#30563=B_SPLINE_CURVE_WITH_KNOTS ( 'NONE', 3,
 ( #73933, #57740, #25981, #15, #99260, #8143, #50197, #97676, #33506, #91216 ),
 .UNSPECIFIED., .F., .F.,
 ( 4, 2, 2, 2, 4 ),
 ( 0.000000000000000000, 0.2500000000000000000, 0.5000000000000000000, 0.7500000000000000000, 1.000000000000000000 ),
 .UNSPECIFIED. ) ;
#30564=UNCERTAINTY_MEASURE_WITH_UNIT (LENGTH_MEASURE( 1.000000000000000082E-05 ), #46710, 'distance_accuracy_value', 'NONE');
#30581=CARTESIAN_POINT ( 'NONE',  ( -18.27395090668250788, 50.00000000000000000, 61.54374581262641897 ) ) ;
#30591=CARTESIAN_POINT ( 'NONE',  ( 17.50000000000003197, 50.00252300264495631, 59.96656198872853594 ) ) ;
#30614=ADVANCED_FACE ( 'NONE', ( #58761 ), #6719, .T. ) ;
#30712=SURFACE_STYLE_FILL_AREA ( #46856 ) ;
#30713=( LENGTH_UNIT ( ) NAMED_UNIT ( * ) SI_UNIT ( .MILLI., .METRE. ) );
#30748=CARTESIAN_POINT ( 'NONE',  ( 8.354779502921196865, -5.000000000000000000, -14.10835818931967189 ) ) ;
#30757=CARTESIAN_POINT ( 'NONE',  ( -57.77058984079067727, 47.99999999999999289, 30.23507972700047475 ) ) ;
#30771=CARTESIAN_POINT ( 'NONE',  ( 19.13710312715079453, 49.71449728783072430, 61.67626017174043795 ) ) ;
#30795=CARTESIAN_POINT ( 'NONE',  ( -19.35499308550004471, 49.90508958054942212, 61.16028107596535079 ) ) ;
#30801=CARTESIAN_POINT ( 'NONE',  ( 10.50000000000000000, -5.000000000000000000, -34.12705337366765690 ) ) ;
#30820=CARTESIAN_POINT ( 'NONE',  ( -5.036189802311180408, -3.000000000000002665, -93.73786388412156612 ) ) ;
#30823=FILL_AREA_STYLE ('',( #70721 ) ) ;
#30830=CARTESIAN_POINT ( 'NONE',  ( 6.106525010887531302, -4.373161893764474506, -16.80699797897928605 ) ) ;
#30833=CARTESIAN_POINT ( 'NONE',  ( -34.85541380047497739, 42.62464468236102988, -62.58172836409449502 ) ) ;
#30847=CARTESIAN_POINT ( 'NONE',  ( -6.738100187484505454, 41.71798639774085160, -59.05424569925489209 ) ) ;
#30854=CARTESIAN_POINT ( 'NONE',  ( -5.693345023042894582, -5.000000000008853362, -71.09407786876178648 ) ) ;
#30866=UNCERTAINTY_MEASURE_WITH_UNIT (LENGTH_MEASURE( 1.000000000000000082E-05 ), #11343, 'distance_accuracy_value', 'NONE');
#30874=CARTESIAN_POINT ( 'NONE',  ( 40.59093392777655396, 41.82284918420663899, -54.69669182410383002 ) ) ;
#30889=CARTESIAN_POINT ( 'NONE',  ( 20.52959122607359532, 39.42505975791698347, 61.74424966332777842 ) ) ;
#30898=CARTESIAN_POINT ( 'NONE',  ( 52.56483885390523625, 48.00000000000000000, -38.23529411764706509 ) ) ;
#30908=CARTESIAN_POINT ( 'NONE',  ( -1.308996937480702005, 48.00000000000000000, -75.00000000000001421 ) ) ;
#30952=CARTESIAN_POINT ( 'NONE',  ( 6.924711585765389366, 40.92328497145224020, -70.90711766198887744 ) ) ;
#30960=CARTESIAN_POINT ( 'NONE',  ( -12.50000000000000533, 26.94026082310467274, -44.46622975111661447 ) ) ;
#30969=CARTESIAN_POINT ( 'NONE',  ( 7.173660666193409696, 41.42016260144754369, -58.97621127612300285 ) ) ;
#30977=CARTESIAN_POINT ( 'NONE',  ( 7.500000000000001776, 25.40357082213843753, -43.84441647605142123 ) ) ;
#30991=AXIS2_PLACEMENT_3D ( 'NONE', #31623, #62395, #87731 ) ;
#31002=CARTESIAN_POINT ( 'NONE',  ( -39.04923757934999884, 49.99999999997997691, 52.30342408740197158 ) ) ;
#31007=( BOUNDED_SURFACE ( )  B_SPLINE_SURFACE ( 2, 3, ( 
 ( #43208, #101448, #10813, #59949 ),
 ( #27065, #61002, #1664, #76093 ),
 ( #76622, #34621, #2733, #68563 ) ),
 .UNSPECIFIED., .F., .F., .F. ) 
 B_SPLINE_SURFACE_WITH_KNOTS ( ( 3, 3 ),
 ( 4, 4 ),
 ( 0.000000000000000000, 1.000000000000000000 ),
 ( -0.003055531191629554024, 0.000000000000000000 ),
 .UNSPECIFIED. ) 
 GEOMETRIC_REPRESENTATION_ITEM ( )  RATIONAL_B_SPLINE_SURFACE ( (
 ( 1.000000000000000000, 1.000000000000000000, 1.000000000000000000, 1.000000000000000000),
 ( 1.857142857142858317, 1.857142857142858317, 1.857142857142858317, 1.857142857142858317),
 ( 1.000000000000000000, 1.000000000000000000, 1.000000000000000000, 1.000000000000000000) ) ) 
 REPRESENTATION_ITEM ( '' )  SURFACE ( )  );
#31018=CARTESIAN_POINT ( 'NONE',  ( 17.94500235637391938, 50.00000000000001421, 61.96179675157436151 ) ) ;
#31036=CARTESIAN_POINT ( 'NONE',  ( -16.00313894029476458, 43.99315672246724773, -88.49932133476114871 ) ) ;
#31057=VERTEX_POINT ( 'NONE', #104384 ) ;
#31065=ORIENTED_EDGE ( 'NONE', *, *, #38903, .T. ) ;
#31069=CARTESIAN_POINT ( 'NONE',  ( -7.360438360694240956, -5.000000000000000000, -94.60993813356640203 ) ) ;
#31076=CARTESIAN_POINT ( 'NONE',  ( 48.44486421332393178, 38.95340677879040925, -41.63464694080630579 ) ) ;
#31100=STYLED_ITEM ( 'NONE', ( #7439 ), #78669 ) ;
#31102=CARTESIAN_POINT ( 'NONE',  ( 7.500000000000006217, 39.99999999999942446, -59.88032989331673406 ) ) ;
#31104=CARTESIAN_POINT ( 'NONE',  ( 7.137815226410160641, -3.000000000000000000, -4.175893272574602300 ) ) ;
#31107=COLOUR_RGB ( '', 0.31764706, 0.68627451, 0.89019608) ;
#31124=CARTESIAN_POINT ( 'NONE',  ( -52.56491209535032993, 39.42572890908717653, -38.23519342730720183 ) ) ;
#31139=CARTESIAN_POINT ( 'NONE',  ( -5.073014709117809495, -4.333232302193168906, -17.09748285339908946 ) ) ;
#31141=CARTESIAN_POINT ( 'NONE',  ( -10.50000000000000711, -5.000000000000000000, -77.33514508527181874 ) ) ;
#31188=CARTESIAN_POINT ( 'NONE',  ( 6.417056588697860775, 41.92969932971389824, -59.44199684604556211 ) ) ;
#31223=CARTESIAN_POINT ( 'NONE',  ( -12.18578101332841612, -4.618505902438846178, -76.80411978101685122 ) ) ;
#31242=CARTESIAN_POINT ( 'NONE',  ( -2.094395098902536390, -3.000000000000000000, -8.000000000000000000 ) ) ;
#31262=ORIENTED_EDGE ( 'NONE', *, *, #43425, .T. ) ;
#31269=CARTESIAN_POINT ( 'NONE',  ( -1.647285698089608230, 39.99999999999999289, -70.00000000000000000 ) ) ;
#31283=CARTESIAN_POINT ( 'NONE',  ( -9.500000000000000000, -5.000000000000000000, -20.99851272547259384 ) ) ;
#31300=CARTESIAN_POINT ( 'NONE',  ( 19.38208173889043806, 49.92621484804256227, 61.05284527896436941 ) ) ;
#31328=CARTESIAN_POINT ( 'NONE',  ( -19.49484304323879513, 50.00000000000004974, 60.04171137605378306 ) ) ;
#31332=FILL_AREA_STYLE ('',( #90060 ) ) ;
#31337=CARTESIAN_POINT ( 'NONE',  ( 18.32078204077888373, 45.00000000000000711, 62.39758222047188951 ) ) ;
#31354=CARTESIAN_POINT ( 'NONE',  ( -1.570796324980114456, -5.000000000000002665, -73.00000000000001421 ) ) ;
#31365=( NAMED_UNIT ( * ) PLANE_ANGLE_UNIT ( ) SI_UNIT ( $, .RADIAN. ) );
#31374=CARTESIAN_POINT ( 'NONE',  ( 7.493949260784499522, 40.57568730855774675, -68.91429205858018747 ) ) ;
#31381=PRESENTATION_STYLE_ASSIGNMENT (( #104164 ) ) ;
#31385=CARTESIAN_POINT ( 'NONE',  ( -7.230783190337165323, -5.000000000001424638, -70.90935357141312068 ) ) ;
#31392=ORIENTED_EDGE ( 'NONE', *, *, #24170, .T. ) ;
#31396=CARTESIAN_POINT ( 'NONE',  ( -43.88602474737083980, 39.35463593402870686, -47.77194135894280436 ) ) ;
#31403=CARTESIAN_POINT ( 'NONE',  ( -7.996668422917848851, -4.999999999991826094, -91.14546720082944375 ) ) ;
#31422=CARTESIAN_POINT ( 'NONE',  ( 42.77536428084039954, 38.95206598861494740, 47.52331724725532780 ) ) ;
#31439=CARTESIAN_POINT ( 'NONE',  ( 9.739726766104286781, 48.00000000000000000, -82.38252115500969808 ) ) ;
#31445=CARTESIAN_POINT ( 'NONE',  ( -14.75116209839012527, 43.55504285526384933, -90.22050492866908655 ) ) ;
#31478=CARTESIAN_POINT ( 'NONE',  ( 7.320748848010288690, 41.41789156490656154, -68.91429206068630720 ) ) ;
#31484=B_SPLINE_CURVE_WITH_KNOTS ( 'NONE', 3,
 ( #20422, #3114, #93725, #85644, #69454, #75937, #11182, #2036, #36589, #102340 ),
 .UNSPECIFIED., .F., .F.,
 ( 4, 2, 2, 2, 4 ),
 ( 0.000000000000000000, 0.2500000000000000000, 0.5000000000000000000, 0.7500000000000000000, 1.000000000000000000 ),
 .UNSPECIFIED. ) ;
#31514=SURFACE_SIDE_STYLE ('',( #33102 ) ) ;
#31533=ORIENTED_EDGE ( 'NONE', *, *, #105868, .T. ) ;
#31539=DIRECTION ( 'NONE',  ( 0.000000000000000000, 1.000000000000000000, 0.000000000000000000 ) ) ;
#31543=CARTESIAN_POINT ( 'NONE',  ( 18.77149637936522097, 50.00000000000000000, 60.89551101287860746 ) ) ;
#31544=FILL_AREA_STYLE_COLOUR ( '', #48454 ) ;
#31556=CARTESIAN_POINT ( 'NONE',  ( -12.49999999999999822, 0.4010732622483518806, -18.19005086670230398 ) ) ;
#31568=CARTESIAN_POINT ( 'NONE',  ( -6.849721783289899335, 41.84384191736015168, -59.83401399873645232 ) ) ;
#31585=CARTESIAN_POINT ( 'NONE',  ( 0.000000000000000000, -3.331654917651224235, 0.000000000000000000 ) ) ;
#31593=SURFACE_STYLE_FILL_AREA ( #7271 ) ;
#31623=CARTESIAN_POINT ( 'NONE',  ( 12.50000000000000000, -4.999999999999997335, -14.04024970282782547 ) ) ;
#31649=CARTESIAN_POINT ( 'NONE',  ( 17.49999999999692690, 49.91179365273359991, 61.97298340135932193 ) ) ;
#31658=CARTESIAN_POINT ( 'NONE',  ( -7.270302578004622873, -3.659675574298181466, -18.03744543697015956 ) ) ;
#31680=B_SPLINE_CURVE_WITH_KNOTS ( 'NONE', 3,
 ( #2207, #10827, #35155, #27079 ),
 .UNSPECIFIED., .F., .F.,
 ( 4, 4 ),
 ( 0.000000000000000000, 1.000000000000000000 ),
 .UNSPECIFIED. ) ;
#31703=CARTESIAN_POINT ( 'NONE',  ( 6.533698841377278299, 41.84235572472459097, -59.21169212581951058 ) ) ;
#31714=CARTESIAN_POINT ( 'NONE',  ( -6.195804093982627769, 41.59435685013754380, -70.65487364512668478 ) ) ;
#31754=B_SPLINE_CURVE_WITH_KNOTS ( 'NONE', 3,
 ( #93933, #28170, #35730, #102010, #68607, #61046 ),
 .UNSPECIFIED., .F., .F.,
 ( 4, 2, 4 ),
 ( 0.000000000000000000, 0.5000000000000000000, 1.000000000000000000 ),
 .UNSPECIFIED. ) ;
#31756=CARTESIAN_POINT ( 'NONE',  ( -7.999999999999996447, -3.000000000000000000, 2.094395098902548824 ) ) ;
#31761=( NAMED_UNIT ( * ) PLANE_ANGLE_UNIT ( ) SI_UNIT ( $, .RADIAN. ) );
#31762=CARTESIAN_POINT ( 'NONE',  ( -10.50000000000000000, -5.000000000000000000, -11.21398294031087062 ) ) ;
#31776=EDGE_LOOP ( 'NONE', ( #43775, #99550, #102629, #53067 ) ) ;
#31833=CARTESIAN_POINT ( 'NONE',  ( 6.526057752884477203, 41.69808114003689070, -58.86835341771923424 ) ) ;
#31842=CARTESIAN_POINT ( 'NONE',  ( -19.47057824336637211, 49.99002094786000328, 60.40962004294379284 ) ) ;
#31866=SURFACE_SIDE_STYLE ('',( #74413 ) ) ;
#31868=CARTESIAN_POINT ( 'NONE',  ( 62.06337123375777765, 48.00000000000000711, -19.99347512944438421 ) ) ;
#31875=CARTESIAN_POINT ( 'NONE',  ( 7.466456039914962872, -3.088347863567613150, -19.53079660665969541 ) ) ;
#31908=CARTESIAN_POINT ( 'NONE',  ( -20.52361948052543639, 41.82532680694352223, -79.00191459447381703 ) ) ;
#31914=CARTESIAN_POINT ( 'NONE',  ( -9.596002107494335576, -5.000000000000002665, -92.37456064099097830 ) ) ;
#31919=SURFACE_STYLE_USAGE ( .BOTH. , #90669 ) ;
#31921=( BOUNDED_CURVE ( )  B_SPLINE_CURVE ( 2, ( #106196, #97575, #46914 ),
 .UNSPECIFIED., .F., .F. ) 
 B_SPLINE_CURVE_WITH_KNOTS ( ( 3, 3 ),
 ( 0.000000000000000000, 1.000000000000000000 ),
 .UNSPECIFIED. ) 
 CURVE ( )  GEOMETRIC_REPRESENTATION_ITEM ( )  RATIONAL_B_SPLINE_CURVE ( ( 1.000000000000000000, 1.857142857142858317, 1.000000000000000000 ) ) 
 REPRESENTATION_ITEM ( '' )  );
#31929=CARTESIAN_POINT ( 'NONE',  ( -8.733111415123392618, -5.000000000000000000, -94.70106727903508670 ) ) ;
#31935=CARTESIAN_POINT ( 'NONE',  ( 58.05736968067268577, 38.95267796501454427, 26.29552882805327840 ) ) ;
#31937=ORIENTED_EDGE ( 'NONE', *, *, #104526, .F. ) ;
#31940=CARTESIAN_POINT ( 'NONE',  ( -9.500000025475724641, -4.999999999999997335, -69.85526497430338111 ) ) ;
#31996=CARTESIAN_POINT ( 'NONE',  ( 7.278899350266751611, 40.56071393749584075, -70.70219355279998297 ) ) ;
#32004=CARTESIAN_POINT ( 'NONE',  ( -53.14306704977071405, 49.99999999999998579, 33.99800176510388638 ) ) ;
#32087=CARTESIAN_POINT ( 'NONE',  ( -6.806778129255477872, 41.25019534346876782, -70.74215739106598733 ) ) ;
#32093=FILL_AREA_STYLE_COLOUR ( '', #2037 ) ;
#32106=EDGE_LOOP ( 'NONE', ( #50372, #9779, #97309, #40042 ) ) ;
#32133=CARTESIAN_POINT ( 'NONE',  ( 17.50000000000002487, 48.88514111886252067, 64.06409622908613244 ) ) ;
#32143=CARTESIAN_POINT ( 'NONE',  ( -7.137815226409945701, -4.999999999999998224, 4.175893272574815462 ) ) ;
#32167=CARTESIAN_POINT ( 'NONE',  ( 17.49999999999876721, 50.01371676752351192, 60.25403804532950858 ) ) ;
#32175=CARTESIAN_POINT ( 'NONE',  ( -6.016266904914970404, -5.000000000005825562, -16.21640811047240049 ) ) ;
#32205=( NAMED_UNIT ( * ) PLANE_ANGLE_UNIT ( ) SI_UNIT ( $, .RADIAN. ) );
#32228=CARTESIAN_POINT ( 'NONE',  ( 19.43524536873321651, 41.87218652733789526, -80.47567652358424084 ) ) ;
#32229=CARTESIAN_POINT ( 'NONE',  ( 5.744147429006506655, 41.99823327698700837, -59.60979843494948938 ) ) ;
#32263=CARTESIAN_POINT ( 'NONE',  ( -12.36633005457817802, -4.301166014002332894, -76.75180828602299243 ) ) ;
#32264=UNCERTAINTY_MEASURE_WITH_UNIT (LENGTH_MEASURE( 1.000000000000000082E-05 ), #74122, 'distance_accuracy_value', 'NONE');
#32290=CARTESIAN_POINT ( 'NONE',  ( -2.094395098902661623, -3.000000000000000000, 8.000000000000000000 ) ) ;
#32298=CARTESIAN_POINT ( 'NONE',  ( 0.000000000000000000, -5.000000000000000888, -73.00000000000001421 ) ) ;
#32342=CARTESIAN_POINT ( 'NONE',  ( -63.27102371193947761, 47.99999999999999289, 15.76003347376316377 ) ) ;
#32398=CARTESIAN_POINT ( 'NONE',  ( 7.791781413346524410, -2.999999999999999556, -2.093983074874241179 ) ) ;
#32402=CARTESIAN_POINT ( 'NONE',  ( 0.000000000000000000, -3.000000000000002665, -75.00000000000001421 ) ) ;
#32404=CARTESIAN_POINT ( 'NONE',  ( 58.13370862442641140, 48.00000000000000711, -29.53088244907750237 ) ) ;
#32414=CARTESIAN_POINT ( 'NONE',  ( 5.318172249950410269, -4.999999999999983125, -15.46996282975494985 ) ) ;
#32434=CARTESIAN_POINT ( 'NONE',  ( -17.50000000000008171, 49.99999999999968026, 59.91915230424517347 ) ) ;
#32437=CARTESIAN_POINT ( 'NONE',  ( -4.205882352941162416, -4.999999999999998224, -72.69916451482997388 ) ) ;
#32448=CARTESIAN_POINT ( 'NONE',  ( -33.19692928480100846, 40.68433407882878328, -62.00609778940272321 ) ) ;
#32454=CARTESIAN_POINT ( 'NONE',  ( -9.739726766100238464, -5.000000000005447198, -87.61747884500121586 ) ) ;
#32459=CARTESIAN_POINT ( 'NONE',  ( 7.500000000000005329, 42.83333333333329307, -71.71180648257555390 ) ) ;
#32476=CARTESIAN_POINT ( 'NONE',  ( 50.75636146201753718, 38.95350866439012094, 38.88400008374063077 ) ) ;
#32544=CARTESIAN_POINT ( 'NONE',  ( -47.94005199002864259, 49.99999999999999289, 40.89453192823585681 ) ) ;
#32556=CARTESIAN_POINT ( 'NONE',  ( 20.60725157159463805, 18.64284798592509773, -32.43860525503979630 ) ) ;
#32573=FILL_AREA_STYLE_COLOUR ( '', #1483 ) ;
#32586=CARTESIAN_POINT ( 'NONE',  ( -61.09659575455685143, 50.00000000000000000, -16.41787579824995902 ) ) ;
#32587=B_SPLINE_CURVE_WITH_KNOTS ( 'NONE', 3,
 ( #8197, #41107, #42160, #106348 ),
 .UNSPECIFIED., .F., .F.,
 ( 4, 4 ),
 ( 0.000000000000000000, 1.000000000000000000 ),
 .UNSPECIFIED. ) ;
#32599=FACE_OUTER_BOUND ( 'NONE', #51475, .T. ) ;
#32623=CARTESIAN_POINT ( 'NONE',  ( -12.13034742782427955, 48.00000000000000000, -93.82352941176471006 ) ) ;
#32628=CARTESIAN_POINT ( 'NONE',  ( -7.493977375961165421, 40.56334907134074541, -69.29067413203748060 ) ) ;
#32632=ORIENTED_EDGE ( 'NONE', *, *, #55946, .T. ) ;
#32640=CARTESIAN_POINT ( 'NONE',  ( 7.048357505843847903, 41.75164249415616524, -68.91429206277067010 ) ) ;
#32657=( LENGTH_UNIT ( ) NAMED_UNIT ( * ) SI_UNIT ( .MILLI., .METRE. ) );
#32688=PRESENTATION_STYLE_ASSIGNMENT (( #38648 ) ) ;
#32714=CARTESIAN_POINT ( 'NONE',  ( 17.50000000000001066, 51.54267222162374651, 62.45775632500005514 ) ) ;
#32722=CARTESIAN_POINT ( 'NONE',  ( -7.468840097763780328, -3.123202671101336314, -19.53083092318177805 ) ) ;
#32733=ORIENTED_EDGE ( 'NONE', *, *, #23728, .F. ) ;
#32747=EDGE_CURVE ( 'NONE', #102845, #38992, #26943, .T. ) ;
#32748=( LENGTH_UNIT ( ) NAMED_UNIT ( * ) SI_UNIT ( .MILLI., .METRE. ) );
#32759=ADVANCED_FACE ( 'NONE', ( #59817 ), #37008, .T. ) ;
#32762=CARTESIAN_POINT ( 'NONE',  ( -52.56483885390523625, 48.00000000000000000, -38.23529411764706509 ) ) ;
#32766=DIRECTION ( 'NONE',  ( 0.000000000000000000, 1.000000000000000000, 0.000000000000000000 ) ) ;
#32772=CARTESIAN_POINT ( 'NONE',  ( 23.93147354620797529, 41.62439615674134075, -74.39855162740241212 ) ) ;
#32804=CARTESIAN_POINT ( 'NONE',  ( 14.75116209840774495, 43.55504285524111907, -90.22050492864485705 ) ) ;
#32823=CARTESIAN_POINT ( 'NONE',  ( -7.137815226411302838, -3.000000000000000000, -4.175893272573455661 ) ) ;
#32829=FILL_AREA_STYLE ('',( #56527 ) ) ;
#32894=( BOUNDED_CURVE ( )  B_SPLINE_CURVE ( 2, ( #68627, #34679, #67551 ),
 .UNSPECIFIED., .F., .F. ) 
 B_SPLINE_CURVE_WITH_KNOTS ( ( 3, 3 ),
 ( 0.000000000000000000, 1.000000000000000000 ),
 .UNSPECIFIED. ) 
 CURVE ( )  GEOMETRIC_REPRESENTATION_ITEM ( )  RATIONAL_B_SPLINE_CURVE ( ( 1.428571428571429047, 1.428571428571428381, 1.000000000000000000 ) ) 
 REPRESENTATION_ITEM ( '' )  );
#32924=CARTESIAN_POINT ( 'NONE',  ( -9.375019126488638221, -5.000000000000000888, -18.75059979026688595 ) ) ;
#32925=EDGE_CURVE ( 'NONE', #37873, #67790, #7333, .T. ) ;
#32934=ADVANCED_FACE ( 'NONE', ( #26298 ), #92042, .F. ) ;
#32937=CARTESIAN_POINT ( 'NONE',  ( 59.99387666504468086, 48.00000000000000000, 25.54086645653093512 ) ) ;
#32960=VERTEX_POINT ( 'NONE', #25769 ) ;
#32961=CARTESIAN_POINT ( 'NONE',  ( -19.45524037106812543, 49.98193815142347773, 60.61134026580515410 ) ) ;
#32976=CARTESIAN_POINT ( 'NONE',  ( -25.87876790621018941, 41.47384575004832641, -71.78385368780867282 ) ) ;
#32982=CARTESIAN_POINT ( 'NONE',  ( 7.996668422914432028, -4.999999999991826094, -91.14546720080765851 ) ) ;
#32986=CARTESIAN_POINT ( 'NONE',  ( 4.852941176470593199, 42.83333333333328596, -70.80672828634229177 ) ) ;
#32991=CARTESIAN_POINT ( 'NONE',  ( -1.224646799147352665E-15, -3.000000000000002665, -75.00000000000001421 ) ) ;
#33001=CARTESIAN_POINT ( 'NONE',  ( 11.04978436692697308, -5.000000000000000000, -91.95127353814174853 ) ) ;
#33009=CARTESIAN_POINT ( 'NONE',  ( -58.04881918066196533, 38.95268114429830320, 26.31400674393213635 ) ) ;
#33011=VERTEX_POINT ( 'NONE', #88080 ) ;
#33016=EDGE_LOOP ( 'NONE', ( #5175, #11271, #9702, #54968 ) ) ;
#33019=SURFACE_STYLE_USAGE ( .BOTH. , #49150 ) ;
#33065=CARTESIAN_POINT ( 'NONE',  ( 6.978962139004955212, 41.42610740536763103, -70.37780174659977206 ) ) ;
#33066=ADVANCED_FACE ( 'NONE', ( #55150 ), #38998, .T. ) ;
#33072=CARTESIAN_POINT ( 'NONE',  ( -62.01418705508173446, 38.95383793066508815, -16.66584972140234910 ) ) ;
#33088=CARTESIAN_POINT ( 'NONE',  ( 7.274255167503934416, 41.49770586683256113, -59.52552407551726787 ) ) ;
#33102=SURFACE_STYLE_FILL_AREA ( #83211 ) ;
#33124=CARTESIAN_POINT ( 'NONE',  ( 37.46929538816834793, 50.00000000000000000, -55.58823529411764497 ) ) ;
#33152=CARTESIAN_POINT ( 'NONE',  ( 1.177401751624806314, 48.00000000000000711, -100.0000000000000284 ) ) ;
#33154=CARTESIAN_POINT ( 'NONE',  ( -6.921856738059538827, 41.59435685020019235, -70.13580383255586526 ) ) ;
#33180=( NAMED_UNIT ( * ) SI_UNIT ( $, .STERADIAN. ) SOLID_ANGLE_UNIT ( ) );
#33188=CARTESIAN_POINT ( 'NONE',  ( 12.50000000000000533, 38.20397074648182212, -60.24274188675438779 ) ) ;
#33198=CARTESIAN_POINT ( 'NONE',  ( 32.06611684422574626, 38.95383793063784594, 55.63518754870414540 ) ) ;
#33201=( BOUNDED_CURVE ( )  B_SPLINE_CURVE ( 2, ( #89344, #99534, #58573 ),
 .UNSPECIFIED., .F., .F. ) 
 B_SPLINE_CURVE_WITH_KNOTS ( ( 3, 3 ),
 ( 0.000000000000000000, 1.000000000000000000 ),
 .UNSPECIFIED. ) 
 CURVE ( )  GEOMETRIC_REPRESENTATION_ITEM ( )  RATIONAL_B_SPLINE_CURVE ( ( 1.000000000000000000, 1.857142857142858317, 1.000000000000000000 ) ) 
 REPRESENTATION_ITEM ( '' )  );
#33236=CARTESIAN_POINT ( 'NONE',  ( 18.92590207683029035, 49.07586612980317398, 62.10725160223120866 ) ) ;
#33247=CARTESIAN_POINT ( 'NONE',  ( -7.499944090893143844, -3.043005460619030877, -20.23003913617138139 ) ) ;
#33271=PRESENTATION_STYLE_ASSIGNMENT (( #105539 ) ) ;
#33282=CARTESIAN_POINT ( 'NONE',  ( -16.68184208835464233, 18.64284798593346082, -34.62135284426452131 ) ) ;
#33315=VERTEX_POINT ( 'NONE', #10324 ) ;
#33358=CARTESIAN_POINT ( 'NONE',  ( -12.49999999999999822, -4.999999999999999112, -11.21398294031200393 ) ) ;
#33403=CARTESIAN_POINT ( 'NONE',  ( 6.123233995736763324E-16, 48.00000000000000000, -75.00000000000001421 ) ) ;
#33404=CARTESIAN_POINT ( 'NONE',  ( -6.738100187484505454, 41.71798639774085160, -59.05424569925489209 ) ) ;
#33420=CARTESIAN_POINT ( 'NONE',  ( 45.60838156035057978, 42.00000000000004263, -79.13121736032620390 ) ) ;
#33470=CARTESIAN_POINT ( 'NONE',  ( -38.92110675614357973, 42.05584489377135782, -56.99232464755446870 ) ) ;
#33472=B_SPLINE_CURVE_WITH_KNOTS ( 'NONE', 3,
 ( #75391, #81870, #7996, #51107 ),
 .UNSPECIFIED., .F., .F.,
 ( 4, 4 ),
 ( 0.000000000000000000, 1.000000000000000000 ),
 .UNSPECIFIED. ) ;
#33483=CARTESIAN_POINT ( 'NONE',  ( -17.49999999999737099, 50.00908096117626656, 61.65219700479646292 ) ) ;
#33496=CARTESIAN_POINT ( 'NONE',  ( -19.45775703410437885, 41.87129219958859494, -80.44515592358796141 ) ) ;
#33505=CARTESIAN_POINT ( 'NONE',  ( 7.996668422910221175, -5.000000000000002665, -78.85453279918266389 ) ) ;
#33506=CARTESIAN_POINT ( 'NONE',  ( -5.694238940269539917, 41.34481807419808064, -58.37580806326324989 ) ) ;
#33509=MECHANICAL_DESIGN_GEOMETRIC_PRESENTATION_REPRESENTATION('',(#52423),#93793);
#33510=CARTESIAN_POINT ( 'NONE',  ( 7.500000000000005329, 44.25000000000000000, -68.91429205785459544 ) ) ;
#33514=( BOUNDED_SURFACE ( )  B_SPLINE_SURFACE ( 2, 3, ( 
 ( #15105, #29743, #63688, #94997, #30801, #96574, #47467, #55022 ),
 ( #70170, #30258, #62618, #78775, #47992, #95504, #7009, #62105 ),
 ( #63147, #54484, #21133, #86900, #12973, #87430, #13505, #46428 ) ),
 .UNSPECIFIED., .F., .F., .F. ) 
 B_SPLINE_SURFACE_WITH_KNOTS ( ( 3, 3 ),
 ( 4, 2, 2, 4 ),
 ( 0.000000000000000000, 1.000000000000000000 ),
 ( -0.06656819121499020497, -0.06329489543879425473, 0.001517242213116295688, 0.005444315861320837488 ),
 .UNSPECIFIED. ) 
 GEOMETRIC_REPRESENTATION_ITEM ( )  RATIONAL_B_SPLINE_SURFACE ( (
 ( 1.000000000000000000, 1.000000000000000000, 1.000000000000000000, 1.000000000000000000, 1.000000000000000000, 1.000000000000000000, 1.000000000000000000, 1.000000000000000000),
 ( 1.857142857142858317, 1.857142857142858317, 1.857142857142858317, 1.857142857142858317, 1.857142857142858317, 1.857142857142858317, 1.857142857142858317, 1.857142857142858317),
 ( 1.000000000000000000, 1.000000000000000000, 1.000000000000000000, 1.000000000000000000, 1.000000000000000000, 1.000000000000000000, 1.000000000000000000, 1.000000000000000000) ) ) 
 REPRESENTATION_ITEM ( '' )  SURFACE ( )  );
#33523=CARTESIAN_POINT ( 'NONE',  ( -7.814460424981007236, -5.000000000000000000, -95.45715767408282204 ) ) ;
#33530=CARTESIAN_POINT ( 'NONE',  ( -38.27578887202430025, 38.95432122817999954, 51.21386531492692029 ) ) ;
#33563=CARTESIAN_POINT ( 'NONE',  ( -9.417877086999621149E-14, 35.24549338070647764, 53.20147685480977628 ) ) ;
#33584=CARTESIAN_POINT ( 'NONE',  ( 7.398498005860211890, 40.00000000200842010, -70.41866429880424505 ) ) ;
#33592=CARTESIAN_POINT ( 'NONE',  ( -8.334564508161101060, 38.95383793066860534, 63.67138272020815037 ) ) ;
#33595=CARTESIAN_POINT ( 'NONE',  ( -61.03778855244135571, 49.99999999999999289, -15.95112753556822760 ) ) ;
#33607=CARTESIAN_POINT ( 'NONE',  ( 7.439138809193584834, 41.00331669213974806, -59.84461289586582922 ) ) ;
#33631=CARTESIAN_POINT ( 'NONE',  ( -19.50010530980351220, 50.00000000000000000, 59.90637122617393828 ) ) ;
#33641=ADVANCED_FACE ( 'NONE', ( #57671 ), #94945, .T. ) ;
#33683=CARTESIAN_POINT ( 'NONE',  ( -7.414908815205982329, 40.55825190657662915, -70.34918218187874572 ) ) ;
#33690=DIRECTION ( 'NONE',  ( 0.000000000000000000, 0.000000000000000000, 1.000000000000000000 ) ) ;
#33691=CARTESIAN_POINT ( 'NONE',  ( -7.996316163937361665, -5.000000000000001776, -6.145999768515051365 ) ) ;
#33715=CARTESIAN_POINT ( 'NONE',  ( 12.50000000000000711, 39.93267479482753401, -65.69976313914253296 ) ) ;
#33726=CARTESIAN_POINT ( 'NONE',  ( 50.91589357091642398, 38.95383793061586886, 39.12903940718169338 ) ) ;
#33805=CARTESIAN_POINT ( 'NONE',  ( 63.03617022296134564, 48.00000000000000000, -16.93907820452146851 ) ) ;
#33848=CARTESIAN_POINT ( 'NONE',  ( -6.912476948941361776, 40.56175638174910603, -71.08408186729455736 ) ) ;
#33893=( NAMED_UNIT ( * ) SI_UNIT ( $, .STERADIAN. ) SOLID_ANGLE_UNIT ( ) );
#33894=( NAMED_UNIT ( * ) SI_UNIT ( $, .STERADIAN. ) SOLID_ANGLE_UNIT ( ) );
#33898=( NAMED_UNIT ( * ) SI_UNIT ( $, .STERADIAN. ) SOLID_ANGLE_UNIT ( ) );
#33954=CARTESIAN_POINT ( 'NONE',  ( 12.50000000000000533, 9.372078270843420711, -27.37193597126559297 ) ) ;
#33971=CARTESIAN_POINT ( 'NONE',  ( 5.902962692465450800, 41.87327339699977813, -59.02279353628207303 ) ) ;
#33993=CARTESIAN_POINT ( 'NONE',  ( 17.71556303271838928, 45.00000000000000711, 62.84553702592653224 ) ) ;
#33999=CARTESIAN_POINT ( 'NONE',  ( -9.434035901591116158, -5.000000000000000888, -19.23908757048410578 ) ) ;
#34005=CARTESIAN_POINT ( 'NONE',  ( -17.49999999999996447, 46.94999999999998153, 62.61746187599676716 ) ) ;
#34015=FILL_AREA_STYLE_COLOUR ( '', #36630 ) ;
#34016=CARTESIAN_POINT ( 'NONE',  ( 14.33052326666366838, -3.000000000000002665, -89.63170281049063703 ) ) ;
#34024=ADVANCED_FACE ( 'NONE', ( #38274 ), #71133, .F. ) ;
#34034=CARTESIAN_POINT ( 'NONE',  ( -18.95009564030707949, 49.33583170005315566, 62.02326760999472555 ) ) ;
#34046=CARTESIAN_POINT ( 'NONE',  ( -6.641837642500876271, 41.74662713182689089, -59.04567091375639620 ) ) ;
#34047=CARTESIAN_POINT ( 'NONE',  ( -19.68889612315570048, 41.86194541559208204, -80.13187903333529505 ) ) ;
#34055=CARTESIAN_POINT ( 'NONE',  ( -7.996668422906947349, -3.000000000000002665, -91.14546720082398679 ) ) ;
#34059=CARTESIAN_POINT ( 'NONE',  ( 6.457005528859116161, 41.52802923978755700, -70.63630686878374831 ) ) ;
#34109=ORIENTED_EDGE ( 'NONE', *, *, #86587, .F. ) ;
#34129=CARTESIAN_POINT ( 'NONE',  ( -5.075741750048029743, -4.332638003024074536, -17.09621982684887698 ) ) ;
#34137=CONICAL_SURFACE ( 'NONE', #65131, 18.72828050308589454, 0.7292773806962717931 ) ;
#34157=DIRECTION ( 'NONE',  ( 0.000000000000000000, 0.000000000000000000, 1.000000000000000000 ) ) ;
#34196=CARTESIAN_POINT ( 'NONE',  ( -47.37019975550713724, 41.99999999999999289, 36.40416150952766827 ) ) ;
#34211=CARTESIAN_POINT ( 'NONE',  ( 14.88296266491841635, 41.91403693906578098, -82.91974649391508478 ) ) ;
#34220=CARTESIAN_POINT ( 'NONE',  ( -12.48209226849267317, -3.606693023214783356, -13.63090450099858053 ) ) ;
#34224=CARTESIAN_POINT ( 'NONE',  ( -7.013017686808002971, 40.92324844527869487, -70.84400559904489114 ) ) ;
#34234=CARTESIAN_POINT ( 'NONE',  ( -2.583674962488347493, -5.000000000000000000, 9.743244787954280284 ) ) ;
#34268=CARTESIAN_POINT ( 'NONE',  ( 51.48757442383973881, 38.95383793068620548, -37.45149417477089315 ) ) ;
#34281=CARTESIAN_POINT ( 'NONE',  ( 9.500000000000000000, -5.000000000000000000, -20.99851272547260095 ) ) ;
#34291=ORIENTED_EDGE ( 'NONE', *, *, #37140, .F. ) ;
#34292=CARTESIAN_POINT ( 'NONE',  ( -9.500000000000003553, -5.000000000000000000, -68.91429205785459544 ) ) ;
#34331=EDGE_CURVE ( 'NONE', #58519, #36397, #70493, .T. ) ;
#34344=CARTESIAN_POINT ( 'NONE',  ( 7.500000000000007105, -3.000000000000000000, -68.91429205785459544 ) ) ;
#34346=UNCERTAINTY_MEASURE_WITH_UNIT (LENGTH_MEASURE( 1.000000000000000082E-05 ), #91963, 'distance_accuracy_value', 'NONE');
#34352=CARTESIAN_POINT ( 'NONE',  ( -28.00203968317432057, 50.00000000000000000, 56.72941417029706201 ) ) ;
#34361=CARTESIAN_POINT ( 'NONE',  ( 17.50000000000002842, 50.00000000000000000, 63.82142195508322402 ) ) ;
#34378=CARTESIAN_POINT ( 'NONE',  ( 16.20053603399965070, 41.96864385763039706, -84.86819136098323213 ) ) ;
#34394=CARTESIAN_POINT ( 'NONE',  ( 1.469576158976823356E-15, 50.00000000000000000, -73.00000000000001421 ) ) ;
#34439=DIRECTION ( 'NONE',  ( 1.000000000000000000, 0.000000000000000000, 1.160749806054361473E-16 ) ) ;
#34506=CARTESIAN_POINT ( 'NONE',  ( -88.20421627925436781, 42.00000000000000000, 23.70422451878991765 ) ) ;
#34513=CARTESIAN_POINT ( 'NONE',  ( 5.363597346081439454, 41.33266196706086504, -58.39526881795586633 ) ) ;
#34515=CARTESIAN_POINT ( 'NONE',  ( -7.500000000000007105, 42.00000000000000711, -58.09827136975972195 ) ) ;
#34527=CARTESIAN_POINT ( 'NONE',  ( 17.56579856165942388, 45.00000000000002132, 63.22721773057084249 ) ) ;
#34549=PRESENTATION_STYLE_ASSIGNMENT (( #75493 ) ) ;
#34570=CARTESIAN_POINT ( 'NONE',  ( -19.49999999999970512, 49.99999999999990052, 59.71562975593384692 ) ) ;
#34593=ORIENTED_EDGE ( 'NONE', *, *, #45167, .F. ) ;
#34621=CARTESIAN_POINT ( 'NONE',  ( 15.33074037313114246, 43.81340351859345361, -89.42371653412330090 ) ) ;
#34623=CARTESIAN_POINT ( 'NONE',  ( 19.49683355508617311, 49.99979114368868949, 59.98567652804494799 ) ) ;
#34651=CARTESIAN_POINT ( 'NONE',  ( -7.493944919676032157, 40.57567429012536309, -59.86116873889386625 ) ) ;
#34659=EDGE_LOOP ( 'NONE', ( #50199, #94060, #51582, #22289 ) ) ;
#34668=CARTESIAN_POINT ( 'NONE',  ( -6.043427762771305112, -5.000000000000002665, -95.48543666094731464 ) ) ;
#34679=CARTESIAN_POINT ( 'NONE',  ( -4.852941176792862521, 41.29999999999999005, -70.80672828645249695 ) ) ;
#34683=B_SPLINE_CURVE_WITH_KNOTS ( 'NONE', 3,
 ( #104071, #6426, #47947, #30214, #6966, #73284, #71694, #30757, #106179, #32342, #63643, #72243, #79801, #98107, #47424, #5899, #96531, #22663 ),
 .UNSPECIFIED., .F., .F.,
 ( 4, 2, 2, 2, 2, 2, 2, 2, 4 ),
 ( 0.5671276150162705143, 0.6212366631392367555, 0.6753457112622028857, 0.7294547593851690159, 0.7835638075081352572, 0.8376728556311014984, 0.8917819037540676286, 0.9458909518770337588, 1.000000000000000000 ),
 .UNSPECIFIED. ) ;
#34685=EDGE_CURVE ( 'NONE', #86295, #55315, #38238, .T. ) ;
#34728=B_SPLINE_CURVE_WITH_KNOTS ( 'NONE', 3,
 ( #95885, #54319, #4744, #103436, #71580, #103955, #62985, #54865 ),
 .UNSPECIFIED., .F., .F.,
 ( 4, 2, 2, 4 ),
 ( 0.000000000000000000, 0.5000000000000000000, 0.7500000000000000000, 1.000000000000000000 ),
 .UNSPECIFIED. ) ;
#34733=CARTESIAN_POINT ( 'NONE',  ( 88.20421627921849961, 42.00000000000000000, -23.70422451876603631 ) ) ;
#34741=CARTESIAN_POINT ( 'NONE',  ( -65.06413714112721891, 40.83767784448016158, 0.8155869308389190886 ) ) ;
#34756=CARTESIAN_POINT ( 'NONE',  ( -9.739726766105677669, 49.99999999999999289, -82.38252115500968387 ) ) ;
#34759=CARTESIAN_POINT ( 'NONE',  ( 12.13034742782427955, 48.00000000000000000, -93.82352941176471006 ) ) ;
#34762=CARTESIAN_POINT ( 'NONE',  ( -6.974441889477841272, 41.03925918661743566, -70.79755109234586996 ) ) ;
#34770=CARTESIAN_POINT ( 'NONE',  ( 4.852941176470595863, 39.99999999999999289, -70.80672828634229177 ) ) ;
#34787=VERTEX_POINT ( 'NONE', #14754 ) ;
#34795=CARTESIAN_POINT ( 'NONE',  ( 12.50000000000000355, 27.55321248621640606, -45.11687107644303296 ) ) ;
#34822=CARTESIAN_POINT ( 'NONE',  ( 0.000000000000000000, -3.000000000000000000, 8.000000000000000000 ) ) ;
#34824=CARTESIAN_POINT ( 'NONE',  ( -7.149999999999890221, 41.65000000000012648, -59.82695526680724640 ) ) ;
#34843=CARTESIAN_POINT ( 'NONE',  ( -39.04923757935653583, 48.00000000000000000, 52.30342408741262972 ) ) ;
#34849=CARTESIAN_POINT ( 'NONE',  ( -6.731699483773395443, 41.74873219887699349, -59.11937119210400482 ) ) ;
#34866=CARTESIAN_POINT ( 'NONE',  ( -1.647285698089624884, -3.000000000000002665, -70.00000000000000000 ) ) ;
#34871=CARTESIAN_POINT ( 'NONE',  ( 7.500000000000003553, -3.000000000000000888, -36.97043916959993481 ) ) ;
#34879=CARTESIAN_POINT ( 'NONE',  ( -62.59524157945776324, 49.99999999999999289, 18.50207713769457030 ) ) ;
#34906=CARTESIAN_POINT ( 'NONE',  ( 23.97434870411618846, 41.62134556306904898, -74.34079015579241911 ) ) ;
#34921=CARTESIAN_POINT ( 'NONE',  ( 1.469576158976823356E-15, 50.00000000000000000, -73.00000000000001421 ) ) ;
#34954=STYLED_ITEM ( 'NONE', ( #36429 ), #96260 ) ;
#34958=CARTESIAN_POINT ( 'NONE',  ( -17.49999999999997513, 50.00000000000000000, 63.82142195434425958 ) ) ;
#34965=( NAMED_UNIT ( * ) PLANE_ANGLE_UNIT ( ) SI_UNIT ( $, .RADIAN. ) );
#34999=CARTESIAN_POINT ( 'NONE',  ( 9.500000000000001776, -5.000000000000000000, -36.97043916959993481 ) ) ;
#35017=CARTESIAN_POINT ( 'NONE',  ( 12.50000000000000000, -2.171334581115599516, -15.32410535964003095 ) ) ;
#35018=EDGE_CURVE ( 'NONE', #33011, #53678, #20417, .T. ) ;
#35029=CARTESIAN_POINT ( 'NONE',  ( 45.60838156032635027, 42.00000000000000000, 79.13121736029046360 ) ) ;
#35038=CARTESIAN_POINT ( 'NONE',  ( 6.744833588908348609, 41.44195294531055396, -58.57194835312484571 ) ) ;
#35048=CARTESIAN_POINT ( 'NONE',  ( -6.145467199749147014, -3.000000000000003109, -77.00333157601822620 ) ) ;
#35075=CARTESIAN_POINT ( 'NONE',  ( 14.61924042696503712, -3.000000000000002665, -89.34162378225711620 ) ) ;
#35093=CARTESIAN_POINT ( 'NONE',  ( -17.49999999999998579, 51.12013589170755523, 63.06608111886978207 ) ) ;
#35116=CARTESIAN_POINT ( 'NONE',  ( -5.036189802311180408, -3.000000000000002665, -93.73786388412156612 ) ) ;
#35143=CARTESIAN_POINT ( 'NONE',  ( 7.141975279388227626, -3.000000000000119016, -70.98863559356006192 ) ) ;
#35155=CARTESIAN_POINT ( 'NONE',  ( 13.14242568359541607, 42.00000000000000000, -92.43215185542086942 ) ) ;
#35156=UNCERTAINTY_MEASURE_WITH_UNIT (LENGTH_MEASURE( 1.000000000000000082E-05 ), #70053, 'distance_accuracy_value', 'NONE');
#35169=CARTESIAN_POINT ( 'NONE',  ( -7.126148247341457242, 41.12758119229482645, -58.55282700859728351 ) ) ;
#35254=CARTESIAN_POINT ( 'NONE',  ( -23.70422451879018055, 42.00000000000000000, 88.20421627933653497 ) ) ;
#35262=CARTESIAN_POINT ( 'NONE',  ( -64.71215703819380849, 40.83860938991785616, 6.807632145269733925 ) ) ;
#35278=CARTESIAN_POINT ( 'NONE',  ( -6.145467200823436116, 49.99999999999999289, -92.99666842290275781 ) ) ;
#35281=CARTESIAN_POINT ( 'NONE',  ( -12.48827636465884083, -3.503589027571160308, -13.74991316378451423 ) ) ;
#35288=EDGE_CURVE ( 'NONE', #84701, #26386, #8499, .T. ) ;
#35307=SURFACE_STYLE_USAGE ( .BOTH. , #59028 ) ;
#35383=CARTESIAN_POINT ( 'NONE',  ( -6.566498363475146149, 41.80386921324385696, -59.12741086741073104 ) ) ;
#35399=CARTESIAN_POINT ( 'NONE',  ( -17.49999999999996803, 47.99999999999997868, 64.09949417230998847 ) ) ;
#35406=UNCERTAINTY_MEASURE_WITH_UNIT (LENGTH_MEASURE( 1.000000000000000082E-05 ), #81083, 'distance_accuracy_value', 'NONE');
#35410=AXIS2_PLACEMENT_3D ( 'NONE', #42747, #76698, #34157 ) ;
#35412=CARTESIAN_POINT ( 'NONE',  ( 6.546995434871612396, 41.93635067897446334, -69.23592083470533964 ) ) ;
#35414=CARTESIAN_POINT ( 'NONE',  ( 61.09659575456475977, 50.00000000000000000, -16.41787579823443366 ) ) ;
#35422=EDGE_CURVE ( 'NONE', #32960, #16973, #21255, .T. ) ;
#35498=CARTESIAN_POINT ( 'NONE',  ( 7.347171990167082001, -3.439186728100506851, -18.43985286355972519 ) ) ;
#35553=CARTESIAN_POINT ( 'NONE',  ( 12.49989493515518646, 18.64301898209307140, -36.27145154709465658 ) ) ;
#35563=CARTESIAN_POINT ( 'NONE',  ( 11.85444436786839084, 42.00000000000000000, -90.56128410203886858 ) ) ;
#35566=DIRECTION ( 'NONE',  ( 0.000000000000000000, -1.000000000000000000, -0.000000000000000000 ) ) ;
#35571=CARTESIAN_POINT ( 'NONE',  ( 6.516858182563246338, 41.40454334770866751, -58.45804045544070959 ) ) ;
#35589=CARTESIAN_POINT ( 'NONE',  ( 7.428753218262151847, 40.00000000162874869, -70.23138194497943232 ) ) ;
#35600=VECTOR ( 'NONE', #12718, 1000.000000000000114 ) ;
#35612=CARTESIAN_POINT ( 'NONE',  ( 14.73122683063179217, -3.000000000000002665, -81.05502296679115659 ) ) ;
#35613=CARTESIAN_POINT ( 'NONE',  ( 13.24502500596364740, -3.000000000000001776, -77.83160543688525479 ) ) ;
#35654=CARTESIAN_POINT ( 'NONE',  ( -1.308996937480702005, -3.000000000000002665, -95.00000000000000000 ) ) ;
#35659=ORIENTED_EDGE ( 'NONE', *, *, #77534, .F. ) ;
#35662=CARTESIAN_POINT ( 'NONE',  ( 10.34493385746861627, -4.332661967061061326, -14.59917742215513314 ) ) ;
#35666=B_SPLINE_CURVE_WITH_KNOTS ( 'NONE', 3,
 ( #41188, #155, #97289, #1222, #74070, #98867, #56827, #89748, #15845, #48726 ),
 .UNSPECIFIED., .F., .F.,
 ( 4, 2, 2, 2, 4 ),
 ( 0.000000000000000000, 0.5000000000000000000, 0.7500000000000000000, 0.8750000000000000000, 1.000000000000000000 ),
 .UNSPECIFIED. ) ;
#35670=CONICAL_SURFACE ( 'NONE', #30502, 15.00000000000000178, 0.7292773806962717931 ) ;
#35697=CARTESIAN_POINT ( 'NONE',  ( -12.06346645439339937, -4.728929080161973886, -12.59383595213993523 ) ) ;
#35701=CARTESIAN_POINT ( 'NONE',  ( -7.500000000000003553, -0.03736385522455209357, -23.73594627047615901 ) ) ;
#35712=CARTESIAN_POINT ( 'NONE',  ( -19.10613678898662471, 49.68048510767285109, 61.72917303677328960 ) ) ;
#35713=CARTESIAN_POINT ( 'NONE',  ( -7.416285793330573028, 41.02764771990347015, -59.17152505158298936 ) ) ;
#35714=CARTESIAN_POINT ( 'NONE',  ( 6.616217471285501084, 40.56071481283028390, -71.17595774755042726 ) ) ;
#35729=CARTESIAN_POINT ( 'NONE',  ( -2.093983074874246508, -3.000000000000000444, 7.791781413346522633 ) ) ;
#35730=CARTESIAN_POINT ( 'NONE',  ( -1.589967640018407291, -5.000000000000000888, -16.33917143506446124 ) ) ;
#35758=EDGE_CURVE ( 'NONE', #5970, #78368, #5825, .T. ) ;
#35777=( NAMED_UNIT ( * ) PLANE_ANGLE_UNIT ( ) SI_UNIT ( $, .RADIAN. ) );
#35784=CARTESIAN_POINT ( 'NONE',  ( 19.50000000000223466, 49.99999999999952394, 59.71562975593440115 ) ) ;
#35798=CARTESIAN_POINT ( 'NONE',  ( -1.905220702120325443E-14, 42.00000000000000711, -59.23741894013591036 ) ) ;
#35804=ORIENTED_EDGE ( 'NONE', *, *, #27636, .T. ) ;
#35806=CARTESIAN_POINT ( 'NONE',  ( 62.84401523694076275, 40.83901776069048850, -16.86776260340353062 ) ) ;
#35816=CARTESIAN_POINT ( 'NONE',  ( 8.169585525225409484, 41.99999999999999289, -72.41994148081866456 ) ) ;
#35824=CARTESIAN_POINT ( 'NONE',  ( 10.48543666094595217, 50.00000000000000000, -78.95657223723276275 ) ) ;
#35825=CARTESIAN_POINT ( 'NONE',  ( -12.40258157393384764, -4.192292395472819955, -12.98887677823726960 ) ) ;
#35851=CARTESIAN_POINT ( 'NONE',  ( -6.836424185777212337, 40.92324829897224703, -70.97025588718011591 ) ) ;
#35864=CARTESIAN_POINT ( 'NONE',  ( -18.03527632919914581, 45.00000000000000711, 62.54344397016589596 ) ) ;
#35877=CARTESIAN_POINT ( 'NONE',  ( 12.13034742782427955, 41.99999999999999289, -93.82352941176471006 ) ) ;
#35882=B_SPLINE_CURVE_WITH_KNOTS ( 'NONE', 3,
 ( #5243, #97406, #6273, #64025 ),
 .UNSPECIFIED., .F., .F.,
 ( 4, 4 ),
 ( 0.000000000000000000, 1.000000000000000000 ),
 .UNSPECIFIED. ) ;
#35919=( LENGTH_UNIT ( ) NAMED_UNIT ( * ) SI_UNIT ( .MILLI., .METRE. ) );
#35924=CARTESIAN_POINT ( 'NONE',  ( -6.738100187484505454, 41.71798639774085160, -59.05424569925489209 ) ) ;
#35956=CARTESIAN_POINT ( 'NONE',  ( 5.308064239167483933, 41.67430808361707761, -70.56675995020941627 ) ) ;
#35958=CARTESIAN_POINT ( 'NONE',  ( -5.774137037018697960, 50.00000000000000000, 63.00000000000000000 ) ) ;
#35960=( GEOMETRIC_REPRESENTATION_CONTEXT ( 3 ) GLOBAL_UNCERTAINTY_ASSIGNED_CONTEXT ( ( #43488 ) ) GLOBAL_UNIT_ASSIGNED_CONTEXT ( ( #78700, #86832, #7332 ) ) REPRESENTATION_CONTEXT ( 'NONE', 'WORKASPACE' ) );
#35975=VERTEX_POINT ( 'NONE', #32991 ) ;
#35981=CARTESIAN_POINT ( 'NONE',  ( 48.49756656482988859, 39.00440506456347123, -41.54750411436693014 ) ) ;
#35988=( GEOMETRIC_REPRESENTATION_CONTEXT ( 3 ) GLOBAL_UNCERTAINTY_ASSIGNED_CONTEXT ( ( #93638 ) ) GLOBAL_UNIT_ASSIGNED_CONTEXT ( ( #32748, #32205, #17613 ) ) REPRESENTATION_CONTEXT ( 'NONE', 'WORKASPACE' ) );
#35998=SURFACE_SIDE_STYLE ('',( #28977 ) ) ;
#36000=CARTESIAN_POINT ( 'NONE',  ( -1.570796324976843295, 50.00000000000000000, -73.00000000000001421 ) ) ;
#36007=ORIENTED_EDGE ( 'NONE', *, *, #41762, .T. ) ;
#36065=CARTESIAN_POINT ( 'NONE',  ( 12.00013170160693576, 50.00000000000001421, -83.40936345627085302 ) ) ;
#36081=CARTESIAN_POINT ( 'NONE',  ( -4.999060807336862311, 41.75164249415626472, -70.37937597734750739 ) ) ;
#36086=CARTESIAN_POINT ( 'NONE',  ( -11.93400008872653295, -5.000000000000000888, 11.28327264068946079 ) ) ;
#36095=CARTESIAN_POINT ( 'NONE',  ( 12.50000000000000355, 5.730253167712460183, -23.74922868128247089 ) ) ;
#36105=CARTESIAN_POINT ( 'NONE',  ( -7.754160006507099467, 42.00000000000000711, -59.23741894013591036 ) ) ;
#36121=FACE_OUTER_BOUND ( 'NONE', #83965, .T. ) ;
#36135=CARTESIAN_POINT ( 'NONE',  ( 7.500000000000005329, 40.28748004600710431, -68.91429205818927528 ) ) ;
#36163=EDGE_CURVE ( 'NONE', #48298, #105469, #9623, .T. ) ;
#36184=FACE_OUTER_BOUND ( 'NONE', #80054, .T. ) ;
#36203=CARTESIAN_POINT ( 'NONE',  ( 15.73927229776362680, -4.999999999999999112, -7.856667017202335401 ) ) ;
#36224=CARTESIAN_POINT ( 'NONE',  ( 7.500000000000003553, -2.999999999999999112, -68.91429205785459544 ) ) ;
#36236=CARTESIAN_POINT ( 'NONE',  ( -5.168696396656956793, 1.295298111819218168, -22.28139744604624184 ) ) ;
#36252=CARTESIAN_POINT ( 'NONE',  ( -7.010778356522921584, 41.61257608818559817, -59.09056163754224400 ) ) ;
#36253=CARTESIAN_POINT ( 'NONE',  ( 4.852941176470594975, 40.00000000000031974, -70.80672828634230598 ) ) ;
#36268=CARTESIAN_POINT ( 'NONE',  ( 5.307793834089975071, 21.57984177784170754, -40.64461319766989789 ) ) ;
#36269=CARTESIAN_POINT ( 'NONE',  ( 12.49154685109993856, -3.434808443366712982, -13.82992914247694038 ) ) ;
#36270=CARTESIAN_POINT ( 'NONE',  ( -7.791781413346523522, -3.000000000000000444, -2.093983074874246952 ) ) ;
#36271=CARTESIAN_POINT ( 'NONE',  ( 6.943035990376878352, 41.50417910381163011, -58.81491866537869129 ) ) ;
#36273=CARTESIAN_POINT ( 'NONE',  ( 1.570796324980112679, -5.000000000000002665, -73.00000000000001421 ) ) ;
#36276=CARTESIAN_POINT ( 'NONE',  ( -7.500000000000007105, 39.99999999999998579, -68.91429205786793943 ) ) ;
#36305=CARTESIAN_POINT ( 'NONE',  ( 8.716576110311626380, -5.000000000000000000, -5.062272329164819951 ) ) ;
#36320=CARTESIAN_POINT ( 'NONE',  ( 19.16305615217603631, 49.74182397839735614, 61.63059818732328665 ) ) ;
#36337=PRESENTATION_STYLE_ASSIGNMENT (( #10406 ) ) ;
#36345=CARTESIAN_POINT ( 'NONE',  ( -20.51763481795492794, 40.83832659751297456, 61.74835002636409342 ) ) ;
#36364=CARTESIAN_POINT ( 'NONE',  ( -10.48543666094594684, 50.00000000000000000, -78.95657223723274853 ) ) ;
#36376=CARTESIAN_POINT ( 'NONE',  ( -2.617478843592807358, 48.00000000000000711, -75.26027323331686603 ) ) ;
#36392=CARTESIAN_POINT ( 'NONE',  ( -6.499946559453495531, 41.29102226313802504, -70.87268749769670251 ) ) ;
#36397=VERTEX_POINT ( 'NONE', #56963 ) ;
#36419=CARTESIAN_POINT ( 'NONE',  ( -34.50896137839294653, 42.67077640914953918, -63.05802169876201191 ) ) ;
#36429=PRESENTATION_STYLE_ASSIGNMENT (( #11022 ) ) ;
#36442=CARTESIAN_POINT ( 'NONE',  ( -17.17069302869450809, -4.333298119783913549, 5.126212997795625448 ) ) ;
#36445=CARTESIAN_POINT ( 'NONE',  ( 9.999999999999996447, 48.00000000000000711, -83.69100306100425257 ) ) ;
#36448=CARTESIAN_POINT ( 'NONE',  ( 5.036189803708992052, -3.000000000000002665, -93.73786388354254484 ) ) ;
#36458=CARTESIAN_POINT ( 'NONE',  ( -6.533698963947263572, 41.84235549011117428, -59.21169165894567499 ) ) ;
#36467=CARTESIAN_POINT ( 'NONE',  ( 17.54033449406726675, 50.00000000000000711, 62.99969680185511578 ) ) ;
#36473=ORIENTED_EDGE ( 'NONE', *, *, #35758, .T. ) ;
#36489=CARTESIAN_POINT ( 'NONE',  ( 5.625019092414621724, 41.66287055497627279, -70.61600277306789053 ) ) ;
#36490=CARTESIAN_POINT ( 'NONE',  ( 11.54772599577024295, 50.00000000000000000, 62.20121126512098186 ) ) ;
#36515=EDGE_CURVE ( 'NONE', #46431, #71163, #1995, .T. ) ;
#36522=CARTESIAN_POINT ( 'NONE',  ( 40.54980110599892384, 41.80014750453505457, -54.75324010490675164 ) ) ;
#36529=CARTESIAN_POINT ( 'NONE',  ( 11.68767211932355998, 50.00000000000000000, -88.14097461399491351 ) ) ;
#36571=PRESENTATION_STYLE_ASSIGNMENT (( #78047 ) ) ;
#36573=CARTESIAN_POINT ( 'NONE',  ( -17.51746965587035376, 50.00000000000000711, 63.25210749506708652 ) ) ;
#36589=CARTESIAN_POINT ( 'NONE',  ( -9.289581398512320121, 50.00000000000000711, -94.32893702008476566 ) ) ;
#36609=CARTESIAN_POINT ( 'NONE',  ( -6.302263409432467434, 41.90661423625755333, -70.03646363488827831 ) ) ;
#36614=CARTESIAN_POINT ( 'NONE',  ( -13.88435755502521474, 42.00000000000000000, -90.88030988970933777 ) ) ;
#36629=CARTESIAN_POINT ( 'NONE',  ( -52.56483885390524335, 49.99999999999999289, -38.23529411764707220 ) ) ;
#36630=COLOUR_RGB ( '', 0.09019608, 0.27058824, 0.51372549) ;
#36632=CARTESIAN_POINT ( 'NONE',  ( 57.69562748396959506, 41.99999999991776178, -15.50526908263404735 ) ) ;
#36641=CARTESIAN_POINT ( 'NONE',  ( 6.802270527994665805, 41.53789237612667762, -58.74929213582391441 ) ) ;
#36661=CARTESIAN_POINT ( 'NONE',  ( 7.187174312956649658, 40.29457745722108086, -70.92326172191368983 ) ) ;
#36683=CARTESIAN_POINT ( 'NONE',  ( 14.73122683063088445, -5.000000000000002665, -81.05502296679124186 ) ) ;
#36711=ORIENTED_EDGE ( 'NONE', *, *, #5503, .F. ) ;
#36733=CARTESIAN_POINT ( 'NONE',  ( -12.10102349785729281, -5.000000000000000000, 11.47683805494447107 ) ) ;
#36753=CARTESIAN_POINT ( 'NONE',  ( 0.000000000000000000, -5.000000000000000000, 8.000000000000000000 ) ) ;
#36756=( NAMED_UNIT ( * ) PLANE_ANGLE_UNIT ( ) SI_UNIT ( $, .RADIAN. ) );
#36766=FILL_AREA_STYLE_COLOUR ( '', #46581 ) ;
#36777=CARTESIAN_POINT ( 'NONE',  ( 4.852941176821355285, 40.28748324523049007, -70.80672828646224559 ) ) ;
#36779=COLOUR_RGB ( '', 0.66274510, 0.83137255, 0.94901961) ;
#36789=VERTEX_POINT ( 'NONE', #84840 ) ;
#36796=CARTESIAN_POINT ( 'NONE',  ( -11.99999999999999467, -5.000000000000002665, -86.57079632497431021 ) ) ;
#36805=PRESENTATION_STYLE_ASSIGNMENT (( #3876 ) ) ;
#36824=CARTESIAN_POINT ( 'NONE',  ( 3.122695042037154867, -5.000000000000000000, -96.69538631874429768 ) ) ;
#36832=ORIENTED_EDGE ( 'NONE', *, *, #25458, .F. ) ;
#36835=CARTESIAN_POINT ( 'NONE',  ( 8.904581707871560781, 49.99999999999999289, -97.29851715190670802 ) ) ;
#36843=CARTESIAN_POINT ( 'NONE',  ( 19.07202809346016892, 49.63760697579803605, 61.78692401718791416 ) ) ;
#36849=CARTESIAN_POINT ( 'NONE',  ( 39.25203474886774302, 42.00920105620009082, -56.53737387468299147 ) ) ;
#36856=CARTESIAN_POINT ( 'NONE',  ( 0.000000000000000000, 45.00000000000000711, 0.000000000000000000 ) ) ;
#36859=CARTESIAN_POINT ( 'NONE',  ( 5.022013495247499293, 18.64316884711714195, -38.36535705883633085 ) ) ;
#36866=CARTESIAN_POINT ( 'NONE',  ( -58.89674073997064596, 40.83722256636393411, -28.13773381937142304 ) ) ;
#36876=CARTESIAN_POINT ( 'NONE',  ( 7.135888613856973706, 39.99999999999999289, -71.74865085751117988 ) ) ;
#36885=PLANE ( 'NONE',  #64527 ) ;
#36889=CARTESIAN_POINT ( 'NONE',  ( -7.493949047870493096, 40.57569111244914950, -68.91429205788598722 ) ) ;
#36898=CARTESIAN_POINT ( 'NONE',  ( 6.806778131844891000, 41.25019534418786549, -70.74215739200818120 ) ) ;
#36908=CARTESIAN_POINT ( 'NONE',  ( -6.519732893028145071, 40.56016492163267628, -71.18560187175323506 ) ) ;
#36945=CARTESIAN_POINT ( 'NONE',  ( 7.500000000000003553, -2.999999999999876099, -69.80246343544249044 ) ) ;
#36956=CARTESIAN_POINT ( 'NONE',  ( -6.965116046117190152, 41.61856606226410094, -70.00485699691064667 ) ) ;
#36963=CARTESIAN_POINT ( 'NONE',  ( 8.737863883542575039, 48.00000000000000711, -79.96381019629100706 ) ) ;
#36968=CARTESIAN_POINT ( 'NONE',  ( 6.145467199749147014, -3.000000000000002665, -77.00333157601819778 ) ) ;
#36972=FILL_AREA_STYLE_COLOUR ( '', #49090 ) ;
#36978=CARTESIAN_POINT ( 'NONE',  ( -6.914391365018432545, 41.80417567437852711, -59.57688295187696781 ) ) ;
#36998=CARTESIAN_POINT ( 'NONE',  ( 28.69487864981134351, 50.00000000000000711, 56.30615108626901133 ) ) ;
#37008=( BOUNDED_SURFACE ( )  B_SPLINE_SURFACE ( 2, 3, ( 
 ( #25336, #26416, #50615, #49573, #100253, #58199, #1539, #74899, #8582, #18852, #34506, #10175, #51697, #75979, #9106, #43614, #91125, #66834, #2076, #35029, #98648, #16682, #67892, #74373, #99724, #100780, #58752, #84614, #450, #10700, #33420, #76506, #35563, #66294 ),
 ( #85688, #36105, #37696, #28536, #70561, #78106, #45231, #19928, #86758, #102383, #103447, #62469, #29598, #53825, #4224, #86231, #53311, #94308, #95360, #21497, #37159, #44699, #70021, #79164, #61953, #12826, #36632, #54334, #101849, #12303, #87277, #45747, #3161, #102920 ),
 ( #20470, #29088, #13354, #68976, #61416, #28010, #60880, #46281, #5295, #52771, #94846, #20991, #3706, #93770, #68437, #78623, #93234, #4757, #101330, #11765, #27482, #77586, #60359, #69497, #19397, #52229, #85139, #11232, #44157, #77045, #48906, #103967, #96949, #23084 ) ),
 .UNSPECIFIED., .F., .T., .F. ) 
 B_SPLINE_SURFACE_WITH_KNOTS ( ( 3, 3 ),
 ( 4, 2, 2, 2, 2, 2, 2, 2, 2, 2, 2, 2, 2, 2, 2, 2, 4 ),
 ( 0.000000000000000000, 1.000000000000000000 ),
 ( 3.141592653589793116, 3.534291735288517700, 3.926990816987241395, 4.319689898685965090, 4.712388980384689674, 5.105088062083414258, 5.497787143782137953, 5.890486225480861648, 6.283185307179586232, 6.675884388878310816, 7.068583470577034511, 7.461282552275758206, 7.853981633974482790, 8.246680715673207374, 8.639379797371930181, 9.032078879070654764, 9.424777960769379348 ),
 .UNSPECIFIED. ) 
 GEOMETRIC_REPRESENTATION_ITEM ( )  RATIONAL_B_SPLINE_SURFACE ( (
 ( 1.000000000000000000, 1.000000000000000000, 1.000000000000000000, 1.000000000000000000, 1.000000000000000000, 1.000000000000000000, 1.000000000000000000, 1.000000000000000000, 1.000000000000000000, 1.000000000000000000, 1.000000000000000000, 1.000000000000000000, 1.000000000000000000, 1.000000000000000000, 1.000000000000000000, 1.000000000000000000, 1.000000000000000000, 1.000000000000000000, 1.000000000000000000, 1.000000000000000000, 1.000000000000000000, 1.000000000000000000, 1.000000000000000000, 1.000000000000000000, 1.000000000000000000, 1.000000000000000000, 1.000000000000000000, 1.000000000000000000, 1.000000000000000000, 1.000000000000000000, 1.000000000000000000, 1.000000000000000000, 1.000000000000000000, 1.000000000000000000),
 ( 1.857142857142858317, 1.857142857142858317, 1.857142857142860981, 1.857142857142860981, 1.857142857142858317, 1.857142857142858317, 1.857142857142858317, 1.857142857142858317, 1.857142857142858317, 1.857142857142858317, 1.857142857142858317, 1.857142857142858317, 1.857142857142858317, 1.857142857142858317, 1.857142857142858317, 1.857142857142858317, 1.857142857142858317, 1.857142857142858317, 1.857142857142858317, 1.857142857142858317, 1.857142857142858317, 1.857142857142858317, 1.857142857142858317, 1.857142857142858317, 1.857142857142858317, 1.857142857142858317, 1.857142857142858317, 1.857142857142858317, 1.857142857142858317, 1.857142857142858317, 1.857142857142858317, 1.857142857142858317, 1.857142857142858317, 1.857142857142858317),
 ( 1.000000000000000000, 1.000000000000000000, 1.000000000000000000, 1.000000000000000000, 1.000000000000000000, 1.000000000000000000, 1.000000000000000000, 1.000000000000000000, 1.000000000000000000, 1.000000000000000000, 1.000000000000000000, 1.000000000000000000, 1.000000000000000000, 1.000000000000000000, 1.000000000000000000, 1.000000000000000000, 1.000000000000000000, 1.000000000000000000, 1.000000000000000000, 1.000000000000000000, 1.000000000000000000, 1.000000000000000000, 1.000000000000000000, 1.000000000000000000, 1.000000000000000000, 1.000000000000000000, 1.000000000000000000, 1.000000000000000000, 1.000000000000000000, 1.000000000000000000, 1.000000000000000000, 1.000000000000000000, 1.000000000000000000, 1.000000000000000000) ) ) 
 REPRESENTATION_ITEM ( '' )  SURFACE ( )  );
#37010=CARTESIAN_POINT ( 'NONE',  ( 6.921856739985489781, 41.59435684990518922, -70.13580383465753698 ) ) ;
#37033=CARTESIAN_POINT ( 'NONE',  ( 32.59513272651155802, 40.75989716404614427, -62.80708417208141725 ) ) ;
#37043=CARTESIAN_POINT ( 'NONE',  ( 16.52731600354976393, 43.98685737190852763, -87.77869701378344303 ) ) ;
#37050=EDGE_CURVE ( 'NONE', #105469, #26386, #81634, .T. ) ;
#37067=PRESENTATION_STYLE_ASSIGNMENT (( #96346 ) ) ;
#37079=CARTESIAN_POINT ( 'NONE',  ( -5.322902945112135242, 24.87962054568887282, -43.61635594746744715 ) ) ;
#37097=CARTESIAN_POINT ( 'NONE',  ( -19.11030064134297035, 50.00000000000000711, 60.43649428885221653 ) ) ;
#37104=FACE_OUTER_BOUND ( 'NONE', #83276, .T. ) ;
#37111=EDGE_LOOP ( 'NONE', ( #61574, #45860, #2364, #12315 ) ) ;
#37125=VERTEX_POINT ( 'NONE', #1648 ) ;
#37129=EDGE_LOOP ( 'NONE', ( #3411, #212, #101844, #84236 ) ) ;
#37131=CARTESIAN_POINT ( 'NONE',  ( -7.048357505843686255, 41.75164249415629314, -68.91429205804081448 ) ) ;
#37133=DIRECTION ( 'NONE',  ( 0.000000000000000000, 0.000000000000000000, 1.000000000000000000 ) ) ;
#37135=CARTESIAN_POINT ( 'NONE',  ( -15.92666961941153758, -5.000000000000000000, 4.023340478472887227 ) ) ;
#37136=CARTESIAN_POINT ( 'NONE',  ( -6.232334879375827974, 41.74193240945501771, -58.83489572151871982 ) ) ;
#37140=EDGE_CURVE ( 'NONE', #15506, #57232, #51264, .T. ) ;
#37159=CARTESIAN_POINT ( 'NONE',  ( 36.40416150948652785, 42.00000000008225953, 47.37019975542485639 ) ) ;
#37165=VERTEX_POINT ( 'NONE', #101436 ) ;
#37180=CARTESIAN_POINT ( 'NONE',  ( 0.000000000000000000, -5.000000000000000000, 0.000000000000000000 ) ) ;
#37190=CARTESIAN_POINT ( 'NONE',  ( -11.33049201282551977, -4.963977770834580916, -77.06423821558743725 ) ) ;
#37202=CARTESIAN_POINT ( 'NONE',  ( -10.19007819943908011, -5.000000000014482637, -96.34610920171921578 ) ) ;
#37243=CARTESIAN_POINT ( 'NONE',  ( 7.416129379029737123, 42.00000000000000000, -59.68109090346935375 ) ) ;
#37254=CARTESIAN_POINT ( 'NONE',  ( -16.49565406582427940, -5.000000000000000000, 2.458857127971593393 ) ) ;
#37277=CARTESIAN_POINT ( 'NONE',  ( 19.33986106772935543, 49.89322054401328188, 61.21774086638057355 ) ) ;
#37304=CARTESIAN_POINT ( 'NONE',  ( 6.188824268254729866, 41.46400356848157998, -70.81766461687159619 ) ) ;
#37314=EDGE_CURVE ( 'NONE', #8448, #86295, #46106, .T. ) ;
#37320=CARTESIAN_POINT ( 'NONE',  ( 12.48211703288669838, -3.606465591134454751, -13.63114202488422855 ) ) ;
#37321=CARTESIAN_POINT ( 'NONE',  ( -4.916373759799321341, -3.000000000000000444, 6.397334739185440711 ) ) ;
#37326=CARTESIAN_POINT ( 'NONE',  ( -3.140974613990845210, -5.000000000000002665, -73.31232788067644890 ) ) ;
#37339=STYLED_ITEM ( 'NONE', ( #82055 ), #100763 ) ;
#37347=DIRECTION ( 'NONE',  ( 0.000000000000000000, 1.000000000000000000, 0.000000000000000000 ) ) ;
#37375=CARTESIAN_POINT ( 'NONE',  ( 17.50000000000004974, 48.00000000000341771, 64.09949417230997426 ) ) ;
#37379=SURFACE_STYLE_USAGE ( .BOTH. , #102606 ) ;
#37381=CARTESIAN_POINT ( 'NONE',  ( 25.85123526981803010, 43.59342998289417892, -74.96042727038405928 ) ) ;
#37392=CARTESIAN_POINT ( 'NONE',  ( -1.905220702120325443E-14, 42.00000000000000711, -59.23741894013591036 ) ) ;
#37400=CARTESIAN_POINT ( 'NONE',  ( -51.48757442383521266, 38.95383793070303113, -37.45149417477429665 ) ) ;
#37409=CARTESIAN_POINT ( 'NONE',  ( -7.135888613856518958, 39.99999999999999289, -71.74865085751089566 ) ) ;
#37416=CARTESIAN_POINT ( 'NONE',  ( 5.036189802310915731, 48.00000000000000000, -76.26213611587833441 ) ) ;
#37429=CARTESIAN_POINT ( 'NONE',  ( 9.363581568756892182, -5.000000000000000000, -18.67428222363854218 ) ) ;
#37433=CARTESIAN_POINT ( 'NONE',  ( -9.500000000000000000, -5.000000000000000000, -20.99851272547259384 ) ) ;
#37434=CARTESIAN_POINT ( 'NONE',  ( 0.000000000000000000, -79.93083296558610584, -85.00000000000000000 ) ) ;
#37436=EDGE_LOOP ( 'NONE', ( #104189, #28945, #105200, #60602, #11513, #62854, #105351, #29157, #66308, #62986 ) ) ;
#37440=CARTESIAN_POINT ( 'NONE',  ( -6.472170351928723697, 40.92674623573195447, -71.09138923453632231 ) ) ;
#37469=CARTESIAN_POINT ( 'NONE',  ( -12.50000000000000178, 37.35939052609327859, -58.38223258370340574 ) ) ;
#37477=CARTESIAN_POINT ( 'NONE',  ( 6.907083959255991168, 41.55068448857264229, -58.85924345847777062 ) ) ;
#37484=CARTESIAN_POINT ( 'NONE',  ( 6.931554132376503752, -2.999999999999883649, -71.13906995425703883 ) ) ;
#37510=CARTESIAN_POINT ( 'NONE',  ( -64.32759900501736183, 49.99999999999999289, -11.06576400629343659 ) ) ;
#37515=CARTESIAN_POINT ( 'NONE',  ( -6.583805027033739599, 41.87230883119009661, -59.35876460053138715 ) ) ;
#37523=CARTESIAN_POINT ( 'NONE',  ( 17.93387092058976151, 50.00000000000000711, 61.97722397227583713 ) ) ;
#37531=CARTESIAN_POINT ( 'NONE',  ( -3.733787657005604999, 42.00000000000000000, -68.31039150692600970 ) ) ;
#37535=CARTESIAN_POINT ( 'NONE',  ( 61.31082008514584913, 50.00000000000000000, 14.70291697493483696 ) ) ;
#37545=CARTESIAN_POINT ( 'NONE',  ( 5.652564027754396925, 41.79847498694749675, -70.46163205703543042 ) ) ;
#37555=ORIENTED_EDGE ( 'NONE', *, *, #166, .T. ) ;
#37557=UNCERTAINTY_MEASURE_WITH_UNIT (LENGTH_MEASURE( 1.000000000000000082E-05 ), #24732, 'distance_accuracy_value', 'NONE');
#37569=CARTESIAN_POINT ( 'NONE',  ( 17.50000000000002487, 48.00000000000000000, 62.61746187599675295 ) ) ;
#37577=EDGE_CURVE ( 'NONE', #88824, #48298, #50677, .T. ) ;
#37632=CARTESIAN_POINT ( 'NONE',  ( -40.54980470635882028, 41.80014700451209109, -54.75323515523022877 ) ) ;
#37633=CARTESIAN_POINT ( 'NONE',  ( -17.92955758770686003, 50.00000000000000711, 61.98266528452947455 ) ) ;
#37666=CARTESIAN_POINT ( 'NONE',  ( 7.500000000000007105, 40.00000000000069633, -70.73267643392320281 ) ) ;
#37670=SURFACE_STYLE_FILL_AREA ( #96407 ) ;
#37671=CARTESIAN_POINT ( 'NONE',  ( -6.804095716565868202, 41.75280174922988152, -69.96721254779907895 ) ) ;
#37677=CARTESIAN_POINT ( 'NONE',  ( -5.902962327514317487, 41.87327319969161010, -59.02279321040224147 ) ) ;
#37696=CARTESIAN_POINT ( 'NONE',  ( -15.50526908257195835, 42.00000000000000000, -57.69562748404377572 ) ) ;
#37729=CYLINDRICAL_SURFACE ( 'NONE', #71670, 15.00000000000000000 ) ;
#37732=CARTESIAN_POINT ( 'NONE',  ( -11.60474022310126152, -4.919048487763364008, -76.97896355671299773 ) ) ;
#37744=CARTESIAN_POINT ( 'NONE',  ( -8.572890873561306080, -5.000000000000002665, -75.22730630429823862 ) ) ;
#37745=CARTESIAN_POINT ( 'NONE',  ( 8.480908980104139516, -4.333298119783806968, 15.78559285094131148 ) ) ;
#37758=B_SPLINE_CURVE_WITH_KNOTS ( 'NONE', 3,
 ( #79957, #62229, #103714, #47057, #56190, #55145, #104775, #103193, #39529, #21245, #23351, #89128, #22829, #15229, #47586, #54604, #48115, #29860, #38993, #55661, #71870, #87545, #71339, #80482, #46542, #72406, #79435, #81014, #63271, #21768, #88075, #105310, #63804, #54080, #37429, #14153, #46020, #87021, #37961 ),
 .UNSPECIFIED., .F., .F.,
 ( 4, 1, 1, 1, 2, 2, 1, 1, 1, 1, 1, 2, 2, 1, 1, 1, 1, 1, 2, 2, 1, 1, 1, 1, 1, 1, 2, 2, 4 ),
 ( 0.000000000000000000, 0.06250000000000072164, 0.09375000000000111022, 0.1093750000000013323, 0.1171875000000015682, 0.1250000000000017764, 0.1875000000000041633, 0.2187500000000052180, 0.2343750000000056621, 0.2421875000000059674, 0.2460937500000059674, 0.2480468750000058564, 0.2500000000000057176, 0.3750000000000043854, 0.4375000000000034972, 0.4687500000000037748, 0.4843750000000037748, 0.4921875000000037192, 0.4960937500000044409, 0.5000000000000051070, 0.6250000000000281997, 0.6875000000000405231, 0.7187500000000471845, 0.7343750000000498490, 0.7421875000000507372, 0.7460937500000517364, 0.7480468750000521805, 0.7500000000000526246, 1.000000000000000000 ),
 .UNSPECIFIED. ) ;
#37776=CARTESIAN_POINT ( 'NONE',  ( 8.162336134653109809, 41.33266196706049556, -58.07023218170494516 ) ) ;
#37788=CARTESIAN_POINT ( 'NONE',  ( -7.811152745362720751, -4.332661967060489339, -16.03212449091516945 ) ) ;
#37803=( BOUNDED_CURVE ( )  B_SPLINE_CURVE ( 2, ( #57956, #91419, #16446 ),
 .UNSPECIFIED., .F., .F. ) 
 B_SPLINE_CURVE_WITH_KNOTS ( ( 3, 3 ),
 ( 0.000000000000000000, 1.000000000000000000 ),
 .UNSPECIFIED. ) 
 CURVE ( )  GEOMETRIC_REPRESENTATION_ITEM ( )  RATIONAL_B_SPLINE_CURVE ( ( 1.428571428571429047, 1.428571428571408397, 1.000000000000000000 ) ) 
 REPRESENTATION_ITEM ( '' )  );
#37810=( BOUNDED_SURFACE ( )  B_SPLINE_SURFACE ( 2, 3, ( 
 ( #97359, #7813, #89820, #48273 ),
 ( #90341, #47743, #22981, #23513 ),
 ( #88754, #14847, #24052, #47216 ) ),
 .UNSPECIFIED., .F., .F., .F. ) 
 B_SPLINE_SURFACE_WITH_KNOTS ( ( 3, 3 ),
 ( 4, 4 ),
 ( 0.000000000000000000, 1.000000000000000000 ),
 ( -1.530452813897690353E-17, 0.06873863542433759910 ),
 .UNSPECIFIED. ) 
 GEOMETRIC_REPRESENTATION_ITEM ( )  RATIONAL_B_SPLINE_SURFACE ( (
 ( 1.000000000000000000, 1.000000000000000000, 1.000000000000000000, 1.000000000000000000),
 ( 1.857142857142858317, 1.857142857142858317, 1.857142857142858317, 1.857142857142858317),
 ( 1.000000000000000000, 1.000000000000000000, 1.000000000000000000, 1.000000000000000000) ) ) 
 REPRESENTATION_ITEM ( '' )  SURFACE ( )  );
#37814=CARTESIAN_POINT ( 'NONE',  ( 18.91765080832239221, 48.32805959737323320, 62.18241223506090165 ) ) ;
#37835=CARTESIAN_POINT ( 'NONE',  ( -19.05430908020328573, 49.61020930493598513, 61.81757898065636425 ) ) ;
#37836=CARTESIAN_POINT ( 'NONE',  ( 5.597109213676861650, 41.52722297769237514, -70.77038839093803801 ) ) ;
#37858=CARTESIAN_POINT ( 'NONE',  ( 5.036189802311931807, -3.000000000000002665, -76.26213611587876073 ) ) ;
#37862=CARTESIAN_POINT ( 'NONE',  ( -51.48757442383523397, 38.95383793070303113, -37.45149417477429665 ) ) ;
#37873=VERTEX_POINT ( 'NONE', #72643 ) ;
#37878=CARTESIAN_POINT ( 'NONE',  ( 7.320748848010288690, 41.41789156490656154, -68.91429206068630720 ) ) ;
#37885=AXIS2_PLACEMENT_3D ( 'NONE', #37180, #6344, #71101 ) ;
#37899=CARTESIAN_POINT ( 'NONE',  ( -40.93388221928996984, 39.67581419069122717, -51.72194110475966511 ) ) ;
#37908=CARTESIAN_POINT ( 'NONE',  ( 39.05596081242668305, 42.03682209387911684, -56.80693097134772529 ) ) ;
#37920=CARTESIAN_POINT ( 'NONE',  ( 57.69562748396144514, 41.99999999999999289, 15.50526908259264225 ) ) ;
#37927=CARTESIAN_POINT ( 'NONE',  ( -64.33156063945668279, 39.42582946629362084, 9.759223879856712358 ) ) ;
#37948=VECTOR ( 'NONE', #32766, 1000.000000000000000 ) ;
#37949=CARTESIAN_POINT ( 'NONE',  ( -8.737863884121635394, 48.00000000000000000, -90.03618980231102853 ) ) ;
#37961=CARTESIAN_POINT ( 'NONE',  ( 9.500000000000000000, -5.000000000000000000, -20.99851272547260095 ) ) ;
#37964=CARTESIAN_POINT ( 'NONE',  ( -4.852941176470590534, 25.66666666666755248, -70.80672828634229177 ) ) ;
#38013=CARTESIAN_POINT ( 'NONE',  ( 7.230783165913826416, -2.999999999999999112, -70.90935356275363688 ) ) ;
#38019=CARTESIAN_POINT ( 'NONE',  ( 11.21300718243333883, -4.973729321444529283, -12.57639419883998855 ) ) ;
#38037=CARTESIAN_POINT ( 'NONE',  ( 51.78317192861597107, 50.00000000002003731, 39.73656039222791492 ) ) ;
#38042=CARTESIAN_POINT ( 'NONE',  ( -6.394717965045618513, 41.92174107680550321, -59.37671525613893664 ) ) ;
#38044=CARTESIAN_POINT ( 'NONE',  ( 12.32841007366230635, -4.394465204956419235, -76.76276077223143091 ) ) ;
#38060=EDGE_LOOP ( 'NONE', ( #25298, #16514, #21991, #76964 ) ) ;
#38064=UNCERTAINTY_MEASURE_WITH_UNIT (LENGTH_MEASURE( 1.000000000000000082E-05 ), #56485, 'distance_accuracy_value', 'NONE');
#38077=DIRECTION ( 'NONE',  ( 0.000000000000000000, 0.000000000000000000, 1.000000000000000000 ) ) ;
#38082=CARTESIAN_POINT ( 'NONE',  ( -7.004291982367333524, 40.56179000230169862, -71.01843131766943884 ) ) ;
#38090=CARTESIAN_POINT ( 'NONE',  ( 7.439207106853293894, 40.67211991679438654, -59.07662331495946262 ) ) ;
#38092=CARTESIAN_POINT ( 'NONE',  ( 12.13034742782427955, 48.00000000000000000, -93.82352941176471006 ) ) ;
#38100=( GEOMETRIC_REPRESENTATION_CONTEXT ( 3 ) GLOBAL_UNCERTAINTY_ASSIGNED_CONTEXT ( ( #8494 ) ) GLOBAL_UNIT_ASSIGNED_CONTEXT ( ( #12194, #3047, #20360 ) ) REPRESENTATION_CONTEXT ( 'NONE', 'WORKASPACE' ) );
#38133=( LENGTH_UNIT ( ) NAMED_UNIT ( * ) SI_UNIT ( .MILLI., .METRE. ) );
#38142=CARTESIAN_POINT ( 'NONE',  ( -5.219506489253183723, 6.759691074813323652, -27.25072272683319952 ) ) ;
#38155=CARTESIAN_POINT ( 'NONE',  ( -18.85365065124617701, 50.00000000000001421, 60.78410979961230964 ) ) ;
#38173=CARTESIAN_POINT ( 'NONE',  ( -13.38606538552758884, 42.81373475612566182, -92.09720263395749384 ) ) ;
#38187=ORIENTED_EDGE ( 'NONE', *, *, #89542, .T. ) ;
#38192=FACE_OUTER_BOUND ( 'NONE', #8684, .T. ) ;
#38193=CARTESIAN_POINT ( 'NONE',  ( -5.504991060908163369, 41.95607664920181179, -69.87069165643147528 ) ) ;
#38197=CARTESIAN_POINT ( 'NONE',  ( 16.24800036964924388, -5.000000000000000000, 2.396130137889210587 ) ) ;
#38198=CARTESIAN_POINT ( 'NONE',  ( -5.903045970190874847, 41.64520878214334232, -58.65814377447863137 ) ) ;
#38213=CARTESIAN_POINT ( 'NONE',  ( 6.245851208105055896, 41.90677386778757096, -59.22337204205300054 ) ) ;
#38218=EDGE_CURVE ( 'NONE', #48298, #53479, #83936, .T. ) ;
#38238=B_SPLINE_CURVE_WITH_KNOTS ( 'NONE', 3,
 ( #85491, #2953, #77390, #77924, #12110, #68783, #36963, #19729, #36445, #68236, #28338, #101664, #69830, #28890, #61763, #61214, #69312, #94102 ),
 .UNSPECIFIED., .F., .F.,
 ( 4, 2, 2, 2, 2, 2, 2, 2, 4 ),
 ( 0.000000000000000000, 0.06250000000000000000, 0.1250000000000000000, 0.1875000000000000000, 0.2500000000000000000, 0.3125000000000000000, 0.3750000000000000000, 0.4375000000000000000, 0.5000000000000000000 ),
 .UNSPECIFIED. ) ;
#38264=CARTESIAN_POINT ( 'NONE',  ( -13.24502500595601795, -3.000000000000003553, -77.83160543687115762 ) ) ;
#38274=FACE_OUTER_BOUND ( 'NONE', #86079, .T. ) ;
#38288=FILL_AREA_STYLE_COLOUR ( '', #9987 ) ;
#38330=CARTESIAN_POINT ( 'NONE',  ( 19.11197997874395327, 49.68659357142563238, 61.71932382479903367 ) ) ;
#38354=CARTESIAN_POINT ( 'NONE',  ( -19.45095198684093063, 49.97783521840197807, 60.61741209756609550 ) ) ;
#38356=PRESENTATION_STYLE_ASSIGNMENT (( #61564 ) ) ;
#38360=CARTESIAN_POINT ( 'NONE',  ( 18.78726065216163477, 45.00000000000000000, 62.22585866237294994 ) ) ;
#38373=CARTESIAN_POINT ( 'NONE',  ( 8.737863884122765157, -5.000000000000000888, -79.96381019769943066 ) ) ;
#38375=PLANE ( 'NONE',  #65552 ) ;
#38406=FILL_AREA_STYLE ('',( #53509 ) ) ;
#38427=CARTESIAN_POINT ( 'NONE',  ( 44.98274357202011231, 41.27416156066848885, -48.65895178432889168 ) ) ;
#38428=EDGE_CURVE ( 'NONE', #69383, #51961, #65976, .T. ) ;
#38431=ADVANCED_FACE ( 'NONE', ( #105447 ), #34137, .T. ) ;
#38437=CARTESIAN_POINT ( 'NONE',  ( 47.37019975555959661, 42.00000000000001421, -36.40416150955741870 ) ) ;
#38442=CARTESIAN_POINT ( 'NONE',  ( -63.17583207858296390, 39.42583197079326851, 15.57582698347478001 ) ) ;
#38460=CARTESIAN_POINT ( 'NONE',  ( -5.036189802311180408, 48.00000000000000000, -76.26213611587843388 ) ) ;
#38466=FACE_OUTER_BOUND ( 'NONE', #30293, .T. ) ;
#38507=CARTESIAN_POINT ( 'NONE',  ( -12.50000000000000711, 39.48967685716225873, -64.09116616746609907 ) ) ;
#38524=CARTESIAN_POINT ( 'NONE',  ( 7.500000000000003553, -0.03736385522455209357, -23.73594627047615901 ) ) ;
#38543=CARTESIAN_POINT ( 'NONE',  ( 58.90678327781098034, 40.83906611471667958, -28.11551192243881658 ) ) ;
#38547=CARTESIAN_POINT ( 'NONE',  ( -55.22048556080422799, 49.99999999999999289, 34.80214219305234025 ) ) ;
#38557=( GEOMETRIC_REPRESENTATION_CONTEXT ( 3 ) GLOBAL_UNCERTAINTY_ASSIGNED_CONTEXT ( ( #3032 ) ) GLOBAL_UNIT_ASSIGNED_CONTEXT ( ( #5940, #86377, #28152 ) ) REPRESENTATION_CONTEXT ( 'NONE', 'WORKASPACE' ) );
#38563=CARTESIAN_POINT ( 'NONE',  ( 18.48458798779867607, 50.00000000000001421, 61.27751401116201890 ) ) ;
#38578=CARTESIAN_POINT ( 'NONE',  ( -15.41108402501092201, 43.84921859367801034, -89.31326227421881470 ) ) ;
#38583=CARTESIAN_POINT ( 'NONE',  ( 7.048357505843847903, 41.75164249415616524, -68.91429206277067010 ) ) ;
#38585=DIRECTION ( 'NONE',  ( 0.000000000000000000, 0.000000000000000000, 1.000000000000000000 ) ) ;
#38627=CARTESIAN_POINT ( 'NONE',  ( -2.617478844990583031, 48.00000000000000000, -75.26027323389584467 ) ) ;
#38630=SURFACE_STYLE_FILL_AREA ( #79069 ) ;
#38648=SURFACE_STYLE_USAGE ( .BOTH. , #64508 ) ;
#38650=CARTESIAN_POINT ( 'NONE',  ( -5.221097366536865181, 6.947291620979282101, -27.42108746706259836 ) ) ;
#38663=CARTESIAN_POINT ( 'NONE',  ( -28.49160854680623700, 41.56004624539016845, -71.33051414923416189 ) ) ;
#38664=CARTESIAN_POINT ( 'NONE',  ( -17.84986807784454044, 49.99999999999999289, 62.10144122030740022 ) ) ;
#38667=CARTESIAN_POINT ( 'NONE',  ( -17.49999999999995381, 51.54267222161957562, 62.45775632501238306 ) ) ;
#38674=CARTESIAN_POINT ( 'NONE',  ( 17.50000000000392220, 50.01864923522649065, 61.58301093894417022 ) ) ;
#38679=VERTEX_POINT ( 'NONE', #101870 ) ;
#38683=EDGE_CURVE ( 'NONE', #35975, #14419, #64644, .T. ) ;
#38684=DIRECTION ( 'NONE',  ( 0.000000000000000000, 1.000000000000000000, 0.000000000000000000 ) ) ;
#38731=ORIENTED_EDGE ( 'NONE', *, *, #57664, .T. ) ;
#38765=SURFACE_STYLE_USAGE ( .BOTH. , #61450 ) ;
#38777=CARTESIAN_POINT ( 'NONE',  ( 12.49955057316562090, -4.332870170068738425, -12.71907580248059233 ) ) ;
#38780=CARTESIAN_POINT ( 'NONE',  ( -58.90678327781357382, 40.83906611473262416, -28.11551192243389607 ) ) ;
#38782=CARTESIAN_POINT ( 'NONE',  ( 8.000000000000000000, -4.999999999999998224, 2.094395098902538166 ) ) ;
#38825=EDGE_CURVE ( 'NONE', #81898, #19635, #46699, .T. ) ;
#38843=CARTESIAN_POINT ( 'NONE',  ( 19.23241393038752278, 49.80479087863259480, 61.49459632677954346 ) ) ;
#38872=( NAMED_UNIT ( * ) SI_UNIT ( $, .STERADIAN. ) SOLID_ANGLE_UNIT ( ) );
#38890=CARTESIAN_POINT ( 'NONE',  ( 9.999999999999996447, -5.000000000000002665, -86.30899693748767731 ) ) ;
#38903=EDGE_CURVE ( 'NONE', #36789, #37165, #28187, .T. ) ;
#38904=( LENGTH_UNIT ( ) NAMED_UNIT ( * ) SI_UNIT ( .MILLI., .METRE. ) );
#38906=CARTESIAN_POINT ( 'NONE',  ( -3.122695041978579056, 50.00000000000000711, -96.69538631875555268 ) ) ;
#38907=CARTESIAN_POINT ( 'NONE',  ( -24.28924816910272710, 43.70283635897345675, -77.10780450745573944 ) ) ;
#38919=CARTESIAN_POINT ( 'NONE',  ( -18.91769957617901809, 48.49892424865640805, 62.17828500952143145 ) ) ;
#38923=CARTESIAN_POINT ( 'NONE',  ( -7.421727621021489973, -3.000000000000118128, -70.37058875307404548 ) ) ;
#38925=EDGE_LOOP ( 'NONE', ( #55794, #52106, #100747, #31392, #103399, #17092 ) ) ;
#38941=CARTESIAN_POINT ( 'NONE',  ( 43.73099574044837823, 41.41642832801956331, -50.37982054108119456 ) ) ;
#38944=EDGE_CURVE ( 'NONE', #27308, #46431, #28785, .T. ) ;
#38951=CARTESIAN_POINT ( 'NONE',  ( 7.754160006592983656, 42.00000000000000711, 59.23741894013591036 ) ) ;
#38957=CARTESIAN_POINT ( 'NONE',  ( 39.08459411749380052, 39.42618201486132534, 52.27850612433365995 ) ) ;
#38965=EDGE_CURVE ( 'NONE', #94321, #22777, #9542, .T. ) ;
#38992=VERTEX_POINT ( 'NONE', #96729 ) ;
#38993=CARTESIAN_POINT ( 'NONE',  ( 8.074093511841809345, -5.000000000000000000, -15.92331255328525330 ) ) ;
#38998=CYLINDRICAL_SURFACE ( 'NONE', #18837, 15.00000000000000000 ) ;
#39007=EDGE_CURVE ( 'NONE', #86317, #82792, #67334, .T. ) ;
#39028=CARTESIAN_POINT ( 'NONE',  ( -12.50000000000000711, 18.64303733123573537, -36.27143273323382999 ) ) ;
#39038=CARTESIAN_POINT ( 'NONE',  ( 6.828042838857774299, 41.63841260098274688, -58.95291818684747653 ) ) ;
#39048=( BOUNDED_SURFACE ( )  B_SPLINE_SURFACE ( 2, 3, ( 
 ( #6014, #63750, #105256, #8674, #58290, #72866, #7077, #105775, #23297, #89077, #65326, #40514, #56685, #24887, #57211, #98214, #89608, #6542, #49660, #41576, #90130, #31914, #16773, #23840, #56132, #57739, #97148, #90663, #64792, #74462, #80961, #542, #16232, #49117 ),
 ( #48590, #82569, #97675, #73932, #15702, #33505, #7596, #15173, #48062, #39993, #81479, #72353, #32982, #73391, #106292, #82017, #66379, #24367, #99259, #64280, #8142, #31403, #25436, #32454, #14625, #41049, #47537, #80432, #14, #65853, #39474, #98731, #1630, #99809 ),
 ( #25980, #43702, #76061, #51244, #18943, #27571, #85228, #59916, #51786, #74987, #93326, #58841, #76594, #26504, #92237, #11315, #10783, #35654, #92783, #35116, #18391, #34055, #2705, #42103, #66929, #84699, #91734, #10266, #69063, #28096, #101936, #50706, #68532, #101420 ) ),
 .UNSPECIFIED., .F., .T., .F. ) 
 B_SPLINE_SURFACE_WITH_KNOTS ( ( 3, 3 ),
 ( 4, 2, 2, 2, 2, 2, 2, 2, 2, 2, 2, 2, 2, 2, 2, 2, 4 ),
 ( 0.000000000000000000, 1.000000000000000000 ),
 ( 0.000000000000000000, 0.3926990816987241395, 0.7853981633974482790, 1.178097245096172418, 1.570796326794896558, 1.963495408493620697, 2.356194490192344837, 2.748893571891068976, 3.141592653589793116, 3.534291735288517255, 3.926990816987241395, 4.319689898685965090, 4.712388980384689674, 5.105088062083414258, 5.497787143782137953, 5.890486225480861648, 6.283185307179586232 ),
 .UNSPECIFIED. ) 
 GEOMETRIC_REPRESENTATION_ITEM ( )  RATIONAL_B_SPLINE_SURFACE ( (
 ( 1.000000000000000000, 1.000000000000000000, 1.000000000000000000, 1.000000000000000000, 1.000000000000000000, 1.000000000000000000, 1.000000000000000000, 1.000000000000000000, 1.000000000000000000, 1.000000000000000000, 1.000000000000000000, 1.000000000000000000, 1.000000000000000000, 1.000000000000000000, 1.000000000000000000, 1.000000000000000000, 1.000000000000000000, 1.000000000000000000, 1.000000000000000000, 1.000000000000000000, 1.000000000000000000, 1.000000000000000000, 1.000000000000000000, 1.000000000000000000, 1.000000000000000000, 1.000000000000000000, 1.000000000000000000, 1.000000000000000000, 1.000000000000000000, 1.000000000000000000, 1.000000000000000000, 1.000000000000000000, 1.000000000000000000, 1.000000000000000000),
 ( 1.857142857142858317, 1.857142857142858317, 1.857142857142858317, 1.857142857142858317, 1.857142857142858317, 1.857142857142858317, 1.857142857142858317, 1.857142857142858317, 1.857142857142858317, 1.857142857142858317, 1.857142857142858317, 1.857142857142858317, 1.857142857142858317, 1.857142857142858317, 1.857142857142858317, 1.857142857142858317, 1.857142857142858317, 1.857142857142858317, 1.857142857142858317, 1.857142857142858317, 1.857142857142858317, 1.857142857142858317, 1.857142857142858317, 1.857142857142858317, 1.857142857142858317, 1.857142857142858317, 1.857142857142858317, 1.857142857142858317, 1.857142857142858317, 1.857142857142858317, 1.857142857142858317, 1.857142857142858317, 1.857142857142858317, 1.857142857142858317),
 ( 1.000000000000000000, 1.000000000000000000, 1.000000000000000000, 1.000000000000000000, 1.000000000000000000, 1.000000000000000000, 1.000000000000000000, 1.000000000000000000, 1.000000000000000000, 1.000000000000000000, 1.000000000000000000, 1.000000000000000000, 1.000000000000000000, 1.000000000000000000, 1.000000000000000000, 1.000000000000000000, 1.000000000000000000, 1.000000000000000000, 1.000000000000000000, 1.000000000000000000, 1.000000000000000000, 1.000000000000000000, 1.000000000000000000, 1.000000000000000000, 1.000000000000000000, 1.000000000000000000, 1.000000000000000000, 1.000000000000000000, 1.000000000000000000, 1.000000000000000000, 1.000000000000000000, 1.000000000000000000, 1.000000000000000000, 1.000000000000000000) ) ) 
 REPRESENTATION_ITEM ( '' )  SURFACE ( )  );
#39074=CARTESIAN_POINT ( 'NONE',  ( -56.06936961864204250, 48.00000000000000000, -33.41736086623469504 ) ) ;
#39112=CARTESIAN_POINT ( 'NONE',  ( 6.503370466877179012, 41.93912984867880311, -59.84719185825785104 ) ) ;
#39117=CARTESIAN_POINT ( 'NONE',  ( -6.924711584187146052, 40.92328497002484511, -70.90711766174086961 ) ) ;
#39119=( GEOMETRIC_REPRESENTATION_CONTEXT ( 3 ) GLOBAL_UNCERTAINTY_ASSIGNED_CONTEXT ( ( #93459 ) ) GLOBAL_UNIT_ASSIGNED_CONTEXT ( ( #86710, #21977, #78581 ) ) REPRESENTATION_CONTEXT ( 'NONE', 'WORKASPACE' ) );
#39135=EDGE_LOOP ( 'NONE', ( #101594, #61827, #61116, #80224, #17606, #74106 ) ) ;
#39141=CARTESIAN_POINT ( 'NONE',  ( -3.122376895879317882, -5.000000000000000000, -73.30448186995486992 ) ) ;
#39147=PRESENTATION_STYLE_ASSIGNMENT (( #48261 ) ) ;
#39154=CARTESIAN_POINT ( 'NONE',  ( 2.617478844990903664, 48.00000000000000000, -75.26027323389595836 ) ) ;
#39174=CARTESIAN_POINT ( 'NONE',  ( 8.000000000000000000, -3.000000000000000000, -2.094395098902536834 ) ) ;
#39194=( NAMED_UNIT ( * ) PLANE_ANGLE_UNIT ( ) SI_UNIT ( $, .RADIAN. ) );
#39203=ORIENTED_EDGE ( 'NONE', *, *, #50497, .T. ) ;
#39204=CARTESIAN_POINT ( 'NONE',  ( 17.50000000000006040, 50.79875088430608798, 63.37001662959071524 ) ) ;
#39209=EDGE_CURVE ( 'NONE', #81288, #59054, #18239, .T. ) ;
#39214=CARTESIAN_POINT ( 'NONE',  ( -7.464071982070691114, -3.053493056027888120, -19.53076229012244269 ) ) ;
#39237=CARTESIAN_POINT ( 'NONE',  ( 1.724765290377481275, -5.000000000000002665, -69.73714729961211845 ) ) ;
#39264=CARTESIAN_POINT ( 'NONE',  ( 5.500000000000325073, 41.99999999999999289, -59.88032989331690459 ) ) ;
#39317=CARTESIAN_POINT ( 'NONE',  ( 7.137815226410046066, -3.000000000000000000, 4.175893272574714210 ) ) ;
#39341=AXIS2_PLACEMENT_3D ( 'NONE', #83901, #1909, #49397 ) ;
#39379=CARTESIAN_POINT ( 'NONE',  ( 18.93524409176044898, 49.17398178157321098, 62.07515712285433551 ) ) ;
#39387=B_SPLINE_SURFACE_WITH_KNOTS ( 'NONE', 3, 3, ( 
 ( #3006, #3550, #12153, #77964, #101177, #36489, #35956, #84995 ),
 ( #27338, #93625, #102236, #45613, #29455, #37545, #45085, #61261 ),
 ( #60737, #28936, #94147, #4079, #20320, #61809, #94702, #11078 ),
 ( #37010, #44004, #76889, #102771, #52608, #62327, #53164, #86081 ),
 ( #93082, #69877, #20849, #68829, #2464, #85537, #86617, #12680 ),
 ( #84464, #101707, #70411, #78485, #27872, #4613, #11617, #44546 ),
 ( #77435, #68280, #51551, #35412, #10557, #43473, #60216, #76350 ),
 ( #46649, #38583, #6721, #80599, #13208, #47170, #71448, #97319 ) ),
 .UNSPECIFIED., .F., .F., .F.,
 ( 4, 2, 2, 4 ),
 ( 4, 2, 2, 4 ),
 ( 0.000000000000000000, 0.2500000000000000000, 0.5000000000000000000, 1.000000000000000000 ),
 ( 0.000000000000000000, 0.2500000000000000000, 0.5000000000000000000, 1.000000000000000000 ),
 .UNSPECIFIED. ) ;
#39407=SURFACE_STYLE_USAGE ( .BOTH. , #5945 ) ;
#39426=CARTESIAN_POINT ( 'NONE',  ( 2.617478844989858722, -3.000000000000002665, -75.26027323389553203 ) ) ;
#39438=CARTESIAN_POINT ( 'NONE',  ( 6.731961105520387179, -4.334285474477063360, -16.87634736349912501 ) ) ;
#39440=CARTESIAN_POINT ( 'NONE',  ( -12.00013170160693576, 50.00000000000001421, -86.59063654372916119 ) ) ;
#39448=CARTESIAN_POINT ( 'NONE',  ( 7.500000000000007105, 39.99999999999998579, -68.91429205785453860 ) ) ;
#39456=( LENGTH_UNIT ( ) NAMED_UNIT ( * ) SI_UNIT ( .MILLI., .METRE. ) );
#39467=CARTESIAN_POINT ( 'NONE',  ( -49.99542551630922560, 38.95362649332037108, -39.50291754361181518 ) ) ;
#39474=CARTESIAN_POINT ( 'NONE',  ( -5.036189802309444907, -5.000000000000002665, -76.26213611588271135 ) ) ;
#39488=CARTESIAN_POINT ( 'NONE',  ( 11.76480859346303554, -5.000000000000000000, -79.34597263090529395 ) ) ;
#39491=EDGE_CURVE ( 'NONE', #21200, #81655, #73611, .T. ) ;
#39495=CARTESIAN_POINT ( 'NONE',  ( 14.81477527478923228, 39.42585065352723461, 63.35881087812447277 ) ) ;
#39514=CARTESIAN_POINT ( 'NONE',  ( -9.739726766104087829, 48.00000000000000000, -87.61747884499078509 ) ) ;
#39521=CARTESIAN_POINT ( 'NONE',  ( -14.81732167757165008, 41.99559907176403328, -87.50313943119428473 ) ) ;
#39529=CARTESIAN_POINT ( 'NONE',  ( 6.542296142763995626, -4.999999999999999112, -15.34579906099600599 ) ) ;
#39555=CARTESIAN_POINT ( 'NONE',  ( 6.809786364711801099, 41.36669071793862429, -70.61902766783229879 ) ) ;
#39565=CARTESIAN_POINT ( 'NONE',  ( -12.50000000000000711, 34.76080778227605350, -54.01526194481859733 ) ) ;
#39576=CARTESIAN_POINT ( 'NONE',  ( 25.95755237148832961, 18.64284798592537129, -28.33950252048799001 ) ) ;
#39607=CARTESIAN_POINT ( 'NONE',  ( 64.32759900501075379, 49.99999999999999289, -11.06576400629166912 ) ) ;
#39622=FACE_OUTER_BOUND ( 'NONE', #78389, .T. ) ;
#39702=CARTESIAN_POINT ( 'NONE',  ( -2.094395098902536390, -4.999999999999998224, -8.000000000000000000 ) ) ;
#39717=CARTESIAN_POINT ( 'NONE',  ( 6.232496355896457452, 41.83455062734740437, -59.02481358918409171 ) ) ;
#39727=CARTESIAN_POINT ( 'NONE',  ( 17.50000000000004619, 51.99978697404952044, 59.99316026186414064 ) ) ;
#39730=DIRECTION ( 'NONE',  ( -0.8086898285216187476, 0.000000000000000000, -0.5882352941176471894 ) ) ;
#39736=CARTESIAN_POINT ( 'NONE',  ( -7.145220222863677861, -5.000000000000017764, -15.42794826860982305 ) ) ;
#39738=CARTESIAN_POINT ( 'NONE',  ( 7.493944697689368439, 40.57567825174881904, -59.86116849737391021 ) ) ;
#39761=FILL_AREA_STYLE ('',( #66142 ) ) ;
#39789=CARTESIAN_POINT ( 'NONE',  ( 5.935763094077899815, 41.97455539652511192, -59.37421805147159404 ) ) ;
#39795=ORIENTED_EDGE ( 'NONE', *, *, #66882, .F. ) ;
#39841=CARTESIAN_POINT ( 'NONE',  ( 2.617993873628327250, -5.000000000000000000, 10.00000000000000000 ) ) ;
#39848=CARTESIAN_POINT ( 'NONE',  ( -10.50000000000000711, -5.000000000000000000, -79.51734232575269345 ) ) ;
#39849=CARTESIAN_POINT ( 'NONE',  ( 1.590954573998430099, -4.999999999999999112, -73.00000000000001421 ) ) ;
#39865=ORIENTED_EDGE ( 'NONE', *, *, #38428, .F. ) ;
#39913=CARTESIAN_POINT ( 'NONE',  ( 6.738100180926640093, 41.71798714554645215, -59.05424661244425266 ) ) ;
#39919=ADVANCED_FACE ( 'NONE', ( #23680 ), #20650, .T. ) ;
#39923=CARTESIAN_POINT ( 'NONE',  ( -19.45165646949288885, 49.97831066704853953, 60.61089002369819667 ) ) ;
#39946=CARTESIAN_POINT ( 'NONE',  ( -17.49999999999996803, 46.94999999999998153, 64.09953197957064219 ) ) ;
#39955=CARTESIAN_POINT ( 'NONE',  ( 6.617039711668479818, -4.368567403894799916, -16.80329192430645335 ) ) ;
#39958=CARTESIAN_POINT ( 'NONE',  ( -43.29298354046672159, 41.46939958648897573, -50.98198775960019447 ) ) ;
#39993=CARTESIAN_POINT ( 'NONE',  ( 9.999999999999996447, -5.000000000000002665, -86.30899693748767731 ) ) ;
#40013=CARTESIAN_POINT ( 'NONE',  ( -28.16608175993714269, 38.95286782169205253, 57.17295417723011042 ) ) ;
#40020=ORIENTED_EDGE ( 'NONE', *, *, #55828, .T. ) ;
#40030=CARTESIAN_POINT ( 'NONE',  ( -10.68563486923847705, -4.999065512597902661, -12.55094748029354790 ) ) ;
#40036=CARTESIAN_POINT ( 'NONE',  ( -14.91339176601158734, 41.98696008795855050, -86.62219925848569346 ) ) ;
#40042=ORIENTED_EDGE ( 'NONE', *, *, #90756, .T. ) ;
#40055=CARTESIAN_POINT ( 'NONE',  ( 8.990409435383423187, -4.999999999999999112, -71.93151781320761984 ) ) ;
#40067=CARTESIAN_POINT ( 'NONE',  ( 7.078150634444296152, 41.46400361730934492, -70.18186710228739855 ) ) ;
#40082=EDGE_CURVE ( 'NONE', #32960, #54991, #15729, .T. ) ;
#40084=EDGE_CURVE ( 'NONE', #59054, #74620, #98065, .T. ) ;
#40088=CARTESIAN_POINT ( 'NONE',  ( 7.484956712770276965, 40.70737338351729306, -59.65999187730301401 ) ) ;
#40105=CARTESIAN_POINT ( 'NONE',  ( 13.49450391516581504, 42.88037855346097871, -91.94812430286241067 ) ) ;
#40113=CARTESIAN_POINT ( 'NONE',  ( 64.32759900502375672, 40.83906611471775250, -11.06576400654987147 ) ) ;
#40124=CARTESIAN_POINT ( 'NONE',  ( 12.26069947439007457, -4.513567243280836472, -76.78238181720162459 ) ) ;
#40127=CARTESIAN_POINT ( 'NONE',  ( 0.000000000000000000, 47.00000000000000000, 56.99999999999999289 ) ) ;
#40130=CARTESIAN_POINT ( 'NONE',  ( 6.817720316173498496, 41.26212635516822758, -58.42655815993595780 ) ) ;
#40144=CARTESIAN_POINT ( 'NONE',  ( -12.49999999999999822, 9.372078614953675668, -27.37193630958070401 ) ) ;
#40180=CARTESIAN_POINT ( 'NONE',  ( -12.50000000000000000, -4.999999999999997335, -14.04024970282782547 ) ) ;
#40240=CARTESIAN_POINT ( 'NONE',  ( 17.50000000000003908, 51.99999999999945288, 59.71562975592906497 ) ) ;
#40250=CARTESIAN_POINT ( 'NONE',  ( -6.689814467817122967, -4.999999999994103383, -16.20004731218735827 ) ) ;
#40275=CARTESIAN_POINT ( 'NONE',  ( 58.90678327788049273, 50.00000000002003731, -28.11551192221532247 ) ) ;
#40288=CARTESIAN_POINT ( 'NONE',  ( -4.491425985185824032, 18.64284798592936809, 38.16738163467832123 ) ) ;
#40302=CARTESIAN_POINT ( 'NONE',  ( 5.675015017080928814, 41.92512468593253772, -59.11382255160837929 ) ) ;
#40354=CARTESIAN_POINT ( 'NONE',  ( -7.137815226409941260, -3.000000000000000000, 4.175893272574811910 ) ) ;
#40355=CARTESIAN_POINT ( 'NONE',  ( 0.000000000000000000, 47.00000000000000000, 0.000000000000000000 ) ) ;
#40365=EDGE_LOOP ( 'NONE', ( #91453, #93362, #105003, #82548 ) ) ;
#40391=CARTESIAN_POINT ( 'NONE',  ( 9.479859806995825977, -5.000000000000000000, -13.37835090744263944 ) ) ;
#40410=EDGE_LOOP ( 'NONE', ( #94294, #94204 ) ) ;
#40425=( BOUNDED_CURVE ( )  B_SPLINE_CURVE ( 2, ( #32623, #99976, #65496 ),
 .UNSPECIFIED., .F., .F. ) 
 B_SPLINE_CURVE_WITH_KNOTS ( ( 3, 3 ),
 ( 0.000000000000000000, 1.000000000000000000 ),
 .UNSPECIFIED. ) 
 CURVE ( )  GEOMETRIC_REPRESENTATION_ITEM ( )  RATIONAL_B_SPLINE_CURVE ( ( 1.000000000000000000, 1.857142857142858317, 1.000000000000000000 ) ) 
 REPRESENTATION_ITEM ( '' )  );
#40433=CARTESIAN_POINT ( 'NONE',  ( 6.943035990376877464, 41.50417910381163011, -58.81491866537869129 ) ) ;
#40450=CARTESIAN_POINT ( 'NONE',  ( 17.53610142485861445, 45.00000000000000000, 63.40563617903067950 ) ) ;
#40456=CARTESIAN_POINT ( 'NONE',  ( -4.651132217449170270, -5.000000000000000000, -15.66661053588738106 ) ) ;
#40464=CARTESIAN_POINT ( 'NONE',  ( -6.145467200824362486, -3.000000000000002665, -77.00333157709341947 ) ) ;
#40465=CARTESIAN_POINT ( 'NONE',  ( 64.32470902915412125, 48.00000000000002842, 10.67393577672274496 ) ) ;
#40472=CARTESIAN_POINT ( 'NONE',  ( 7.007554382048097885, -4.192628124804436140, -17.12907408884460381 ) ) ;
#40475=CARTESIAN_POINT ( 'NONE',  ( -38.05267008021335329, 42.17823295822772423, -58.18622768867230377 ) ) ;
#40492=CARTESIAN_POINT ( 'NONE',  ( -7.090506018371190322, 41.24767894959148151, -58.61600934880981839 ) ) ;
#40496=CARTESIAN_POINT ( 'NONE',  ( -17.49999999999999289, 49.17341269449792662, 64.03715209376036910 ) ) ;
#40511=CARTESIAN_POINT ( 'NONE',  ( -14.73061733093910419, 41.88685485518190177, -82.04000854990557912 ) ) ;
#40514=CARTESIAN_POINT ( 'NONE',  ( 10.48543666094595217, -5.000000000000002665, -91.04342776276725147 ) ) ;
#40519=CARTESIAN_POINT ( 'NONE',  ( 4.852941176470593199, 41.41666666666666430, -70.80672828634229177 ) ) ;
#40529=CARTESIAN_POINT ( 'NONE',  ( 12.51690618612821204, -5.000000000000000000, -88.70140625282380142 ) ) ;
#40545=MECHANICAL_DESIGN_GEOMETRIC_PRESENTATION_REPRESENTATION('',(#18171),#28574);
#40573=CARTESIAN_POINT ( 'NONE',  ( -6.738100187484505454, 41.71798639774085160, -59.05424569925489209 ) ) ;
#40595=CARTESIAN_POINT ( 'NONE',  ( -7.343808464831893090, 40.90987269173472640, -58.79603257166633057 ) ) ;
#40601=CARTESIAN_POINT ( 'NONE',  ( -59.10637965291887497, 50.00000000000001421, -21.83934624968677340 ) ) ;
#40612=CARTESIAN_POINT ( 'NONE',  ( 7.413001015142842931, 41.14546113202533206, -59.83891282166461423 ) ) ;
#40624=CARTESIAN_POINT ( 'NONE',  ( 13.54749644447708512, 42.91257261702131842, -91.87527161981162749 ) ) ;
#40637=CARTESIAN_POINT ( 'NONE',  ( -9.797174393178825657E-16, -3.000000000000000000, 8.000000000000000000 ) ) ;
#40643=CARTESIAN_POINT ( 'NONE',  ( -50.18984356160270011, 50.00000000000000000, 38.51389699557558544 ) ) ;
#40650=CARTESIAN_POINT ( 'NONE',  ( 14.75116209840774495, 43.55504285524111907, -90.22050492864485705 ) ) ;
#40681=CARTESIAN_POINT ( 'NONE',  ( -7.418912472240797307, 41.12212780509316445, -69.28711574108936588 ) ) ;
#40707=ORIENTED_EDGE ( 'NONE', *, *, #99508, .F. ) ;
#40709=CARTESIAN_POINT ( 'NONE',  ( 17.92907372343373851, 41.95109139595307823, -82.51358908730536257 ) ) ;
#40732=( BOUNDED_SURFACE ( )  B_SPLINE_SURFACE ( 2, 3, ( 
 ( #102052, #93976, #93452, #69703, #95052, #100993, #3903, #19601, #62161, #52432 ),
 ( #86437, #28215, #27151, #92898, #28745, #54017, #19063, #36835, #51904, #78836 ),
 ( #2822, #84817, #12501, #101533, #61630, #85349, #60039, #4425, #86960, #20672 ) ),
 .UNSPECIFIED., .F., .F., .F. ) 
 B_SPLINE_SURFACE_WITH_KNOTS ( ( 3, 3 ),
 ( 4, 2, 2, 2, 4 ),
 ( 0.000000000000000000, 1.000000000000000000 ),
 ( -0.9419214012998446961, -0.4709607006499223480, 5.551115123125782702E-17, 0.4709607006499224591, 0.9419214012998448071 ),
 .UNSPECIFIED. ) 
 GEOMETRIC_REPRESENTATION_ITEM ( )  RATIONAL_B_SPLINE_SURFACE ( (
 ( 1.000000000000000000, 1.000000000000000000, 1.000000000000000000, 1.000000000000000000, 1.000000000000000000, 1.000000000000000000, 1.000000000000000000, 1.000000000000000000, 1.000000000000000000, 1.000000000000000000),
 ( 1.857142857142858317, 1.857142857142858317, 1.857142857142858317, 1.857142857142858317, 1.857142857142858317, 1.857142857142858317, 1.857142857142858317, 1.857142857142858317, 1.857142857142858317, 1.857142857142858317),
 ( 1.000000000000000000, 1.000000000000000000, 1.000000000000000000, 1.000000000000000000, 1.000000000000000000, 1.000000000000000000, 1.000000000000000000, 1.000000000000000000, 1.000000000000000000, 1.000000000000000000) ) ) 
 REPRESENTATION_ITEM ( '' )  SURFACE ( )  );
#40742=CARTESIAN_POINT ( 'NONE',  ( -2.617993873628169599, -5.000000000000000000, -10.00000000000000000 ) ) ;
#40768=CARTESIAN_POINT ( 'NONE',  ( 17.50000000000462208, 50.03760136707476391, 61.20291971386502894 ) ) ;
#40775=CARTESIAN_POINT ( 'NONE',  ( -6.106525010887766669, -4.373161893764723196, -16.80699797897936421 ) ) ;
#40818=ADVANCED_FACE ( 'NONE', ( #21061 ), #87541, .T. ) ;
#40833=CARTESIAN_POINT ( 'NONE',  ( 0.000000000000000000, -5.000000000000000000, 0.000000000000000000 ) ) ;
#40863=CARTESIAN_POINT ( 'NONE',  ( 5.425084639653764640, 41.91238126396859798, -59.10640578674440349 ) ) ;
#40889=CARTESIAN_POINT ( 'NONE',  ( -4.175893272574848325, -4.999999999999998224, 7.137815226409911951 ) ) ;
#40917=CARTESIAN_POINT ( 'NONE',  ( 6.201636426617084574E-15, 39.99999999999999289, -70.00365511371767013 ) ) ;
#40970=CARTESIAN_POINT ( 'NONE',  ( 6.729774171815768646, 41.69338307640796160, -58.98699303515817149 ) ) ;
#40972=ORIENTED_EDGE ( 'NONE', *, *, #61183, .T. ) ;
#41010=CARTESIAN_POINT ( 'NONE',  ( 6.109877454823632092, -4.349879335532680358, -16.82893417409523806 ) ) ;
#41012=CARTESIAN_POINT ( 'NONE',  ( -9.609938133586723552, 50.00000000000000000, -92.36043836067815960 ) ) ;
#41013=CARTESIAN_POINT ( 'NONE',  ( -38.98600622022465245, 42.04669058375750978, -56.90310263554037817 ) ) ;
#41030=CARTESIAN_POINT ( 'NONE',  ( -17.49999999999716849, 49.96115704434736671, 61.85088014401372902 ) ) ;
#41049=CARTESIAN_POINT ( 'NONE',  ( -9.999999999999996447, -5.000000000000002665, -83.69100306252320820 ) ) ;
#41064=CARTESIAN_POINT ( 'NONE',  ( 12.60460666744324776, -5.000000000000000000, -81.60912347660379851 ) ) ;
#41072=CARTESIAN_POINT ( 'NONE',  ( -61.88098488124455088, 38.95394723122979030, 15.25653196629931152 ) ) ;
#41082=( LENGTH_UNIT ( ) NAMED_UNIT ( * ) SI_UNIT ( .MILLI., .METRE. ) );
#41107=CARTESIAN_POINT ( 'NONE',  ( 4.852941176470590534, 11.33333333333377269, -70.80672828634229177 ) ) ;
#41111=CARTESIAN_POINT ( 'NONE',  ( -7.251694485742912200, 41.54830549313345500, -59.82648083153709706 ) ) ;
#41128=CIRCLE ( 'NONE', #54886, 56.99999999999999289 ) ;
#41142=CARTESIAN_POINT ( 'NONE',  ( -58.26710234651028486, 50.00000000000000711, 24.08968871770548503 ) ) ;
#41154=CARTESIAN_POINT ( 'NONE',  ( 7.190574343477907249, 41.61619628126704384, -59.53992283653117568 ) ) ;
#41172=SURFACE_SIDE_STYLE ('',( #76178 ) ) ;
#41188=CARTESIAN_POINT ( 'NONE',  ( -4.966176470918042263, 41.64999999999998437, -70.47555194646970733 ) ) ;
#41193=CARTESIAN_POINT ( 'NONE',  ( 5.929271423532769703, 41.34548894888533965, -58.36914690832966102 ) ) ;
#41215=CARTESIAN_POINT ( 'NONE',  ( -7.200568795987419612, 40.92548677439322091, -70.61799334047601917 ) ) ;
#41244=CARTESIAN_POINT ( 'NONE',  ( 45.37589407622110116, 39.17805204455682144, -45.78238044965556952 ) ) ;
#41250=CARTESIAN_POINT ( 'NONE',  ( 12.50000000000000711, 39.83843345462788221, -65.33751927206047583 ) ) ;
#41263=CARTESIAN_POINT ( 'NONE',  ( 63.67138272020815748, 38.95383793066860534, 8.334564508068442734 ) ) ;
#41274=CARTESIAN_POINT ( 'NONE',  ( -8.000000000000003553, -3.000000000000000000, -2.094395098902523511 ) ) ;
#41282=DIRECTION ( 'NONE',  ( 0.000000000000000000, -1.000000000000000000, 0.000000000000000000 ) ) ;
#41304=CARTESIAN_POINT ( 'NONE',  ( 19.03324747453112664, 49.57630456594926471, 61.85387798834953088 ) ) ;
#41311=CARTESIAN_POINT ( 'NONE',  ( -8.447961717372509227, -4.999999999999993783, -16.27270454676588329 ) ) ;
#41326=CARTESIAN_POINT ( 'NONE',  ( 7.500000000000000888, -3.000671055698259870, -20.99923901233272971 ) ) ;
#41333=EDGE_LOOP ( 'NONE', ( #69563, #63656, #12038, #61136 ) ) ;
#41335=CARTESIAN_POINT ( 'NONE',  ( 51.78317192862468943, 48.00000000000000000, 39.73656039225600978 ) ) ;
#41347=VECTOR ( 'NONE', #95301, 1000.000000000000000 ) ;
#41351=CARTESIAN_POINT ( 'NONE',  ( -17.49999999999996803, 47.99999999999997868, 64.09949417230998847 ) ) ;
#41358=B_SPLINE_CURVE_WITH_KNOTS ( 'NONE', 3,
 ( #73889, #7032, #32404, #31868, #81435, #73347, #7551, #40465, #106245, #32937, #17800, #52266, #18894, #9146, #91687, #1031, #11266, #43652 ),
 .UNSPECIFIED., .F., .F.,
 ( 4, 2, 2, 2, 2, 2, 2, 2, 4 ),
 ( 0.000000000000000000, 0.05410904812296605387, 0.1082180962459321077, 0.1623271443688981686, 0.2164361924918642155, 0.2705452406148303734, 0.3246542887377965036, 0.3787633368607626894, 0.4328723849837288196 ),
 .UNSPECIFIED. ) ;
#41400=VECTOR ( 'NONE', #18919, 1000.000000000000000 ) ;
#41494=CARTESIAN_POINT ( 'NONE',  ( 6.674329244388144566, 41.70627487048766113, -58.97405642351494492 ) ) ;
#41505=CARTESIAN_POINT ( 'NONE',  ( -1.778928937981819391, -4.332661967047337193, -18.07496135556788985 ) ) ;
#41517=CARTESIAN_POINT ( 'NONE',  ( -7.474779730927227028, -5.000000000000000888, -15.57446526240806506 ) ) ;
#41534=CARTESIAN_POINT ( 'NONE',  ( 5.074726305366539236, -4.333190174238139569, -17.09701513331991407 ) ) ;
#41536=CARTESIAN_POINT ( 'NONE',  ( -14.61924042696621306, -3.000000000000002665, -89.34162378225479983 ) ) ;
#41537=CARTESIAN_POINT ( 'NONE',  ( -43.54105046090145237, 41.43920833560382988, -50.64095212750816444 ) ) ;
#41554=ADVANCED_FACE ( 'NONE', ( #52205 ), #97950, .T. ) ;
#41557=CARTESIAN_POINT ( 'NONE',  ( -19.50000000000008527, 49.99999999999981526, 59.56761335716138461 ) ) ;
#41570=CARTESIAN_POINT ( 'NONE',  ( -24.19259889269783415, 41.60565019191297154, -74.04692782006098639 ) ) ;
#41576=CARTESIAN_POINT ( 'NONE',  ( -6.043427762771305112, -5.000000000000002665, -95.48543666094731464 ) ) ;
#41580=CARTESIAN_POINT ( 'NONE',  ( 7.500000000000005329, 41.41666666666666430, -68.91429205785459544 ) ) ;
#41604=CARTESIAN_POINT ( 'NONE',  ( -2.897774986000545283, 38.95261239556568000, 63.66823351328071112 ) ) ;
#41654=CARTESIAN_POINT ( 'NONE',  ( 4.651269564039822946, -4.999999999999991118, -15.66707428873065311 ) ) ;
#41664=ORIENTED_EDGE ( 'NONE', *, *, #4403, .F. ) ;
#41691=LINE ( 'NONE', #65965, #3247 ) ;
#41706=CARTESIAN_POINT ( 'NONE',  ( 4.205882352941182845, -5.000000000000000000, -72.69916451482998809 ) ) ;
#41747=CARTESIAN_POINT ( 'NONE',  ( -7.096116585352607586, 40.56175661586830472, -70.95279415358434960 ) ) ;
#41755=CARTESIAN_POINT ( 'NONE',  ( 4.881098022930994595, 41.14559726925936900, -70.72437870144329963 ) ) ;
#41758=CARTESIAN_POINT ( 'NONE',  ( -4.966176470918042263, 41.64999999999998437, -70.47555194646970733 ) ) ;
#41760=CARTESIAN_POINT ( 'NONE',  ( 17.50000000000002842, 45.00000000000000711, -500000.0000000000582 ) ) ;
#41762=EDGE_CURVE ( 'NONE', #66436, #84701, #7678, .T. ) ;
#41782=CARTESIAN_POINT ( 'NONE',  ( 12.50000000000000355, 40.11561338586450631, -66.43777432280938910 ) ) ;
#41804=CARTESIAN_POINT ( 'NONE',  ( -7.251694485742912200, 41.54830549313345500, -59.82648083153709706 ) ) ;
#41822=CARTESIAN_POINT ( 'NONE',  ( 6.492511067189947305, 41.78432740739263096, -59.03547063838888675 ) ) ;
#41836=COLOUR_RGB ( '', 0.66274510, 0.83137255, 0.94901961) ;
#41840=CARTESIAN_POINT ( 'NONE',  ( 5.313748243244007519, 41.99394926078451107, -69.45901782876110531 ) ) ;
#41845=( BOUNDED_SURFACE ( )  B_SPLINE_SURFACE ( 2, 3, ( 
 ( #51396, #27172, #99953, #43321, #59514, #76203, #3394, #2306, #50332, #60063, #17995, #50856, #77283, #83762, #102075, #35254, #44387, #9870, #2846, #42783, #68677, #17468, #75674, #83240, #10924, #1775, #34733, #67604, #92923, #69206, #9333, #19088, #28236, #92387 ),
 ( #35798, #101557, #85376, #91353, #93476, #42243, #19626, #51927, #75132, #84841, #52459, #1228, #34196, #85929, #61656, #104195, #62700, #38951, #102618, #79396, #45982, #28777, #95074, #37920, #69727, #54037, #21207, #94546, #38437, #78332, #12000, #22256, #55105, #37392 ),
 ( #70253, #95592, #20698, #103154, #4448, #29822, #53536, #44932, #87506, #70782, #86466, #63232, #30339, #12524, #21728, #86982, #54569, #103677, #3926, #13051, #45457, #13586, #78861, #53006, #5513, #88035, #77817, #29300, #96124, #71828, #14115, #62188, #36859, #46502 ) ),
 .UNSPECIFIED., .F., .T., .F. ) 
 B_SPLINE_SURFACE_WITH_KNOTS ( ( 3, 3 ),
 ( 4, 2, 2, 2, 2, 2, 2, 2, 2, 2, 2, 2, 2, 2, 2, 2, 4 ),
 ( 0.000000000000000000, 1.000000000000000000 ),
 ( 3.141592653589793116, 3.534291735288517700, 3.926990816987241395, 4.319689898685965090, 4.712388980384689674, 5.105088062083414258, 5.497787143782137953, 5.890486225480861648, 6.283185307179586232, 6.675884388878310816, 7.068583470577034511, 7.461282552275758206, 7.853981633974482790, 8.246680715673207374, 8.639379797371930181, 9.032078879070654764, 9.424777960769379348 ),
 .UNSPECIFIED. ) 
 GEOMETRIC_REPRESENTATION_ITEM ( )  RATIONAL_B_SPLINE_SURFACE ( (
 ( 1.000000000000000000, 1.000000000000000000, 1.000000000000000000, 1.000000000000000000, 1.000000000000000000, 1.000000000000000000, 1.000000000000000000, 1.000000000000000000, 1.000000000000000000, 1.000000000000000000, 1.000000000000000000, 1.000000000000000000, 1.000000000000000000, 1.000000000000000000, 1.000000000000000000, 1.000000000000000000, 1.000000000000000000, 1.000000000000000000, 1.000000000000000000, 1.000000000000000000, 1.000000000000000000, 1.000000000000000000, 1.000000000000000000, 1.000000000000000000, 1.000000000000000000, 1.000000000000000000, 1.000000000000000000, 1.000000000000000000, 1.000000000000000000, 1.000000000000000000, 1.000000000000000000, 1.000000000000000000, 1.000000000000000000, 1.000000000000000000),
 ( 1.857142857142858317, 1.857142857142858317, 1.857142857142860981, 1.857142857142860981, 1.857142857142858317, 1.857142857142858317, 1.857142857142858317, 1.857142857142858317, 1.857142857142858317, 1.857142857142858317, 1.857142857142858317, 1.857142857142858317, 1.857142857142858317, 1.857142857142858317, 1.857142857142858317, 1.857142857142858317, 1.857142857142858317, 1.857142857142858317, 1.857142857142858317, 1.857142857142858317, 1.857142857142858317, 1.857142857142858317, 1.857142857142858317, 1.857142857142858317, 1.857142857142858317, 1.857142857142858317, 1.857142857142858317, 1.857142857142858317, 1.857142857142858317, 1.857142857142858317, 1.857142857142858317, 1.857142857142858317, 1.857142857142858317, 1.857142857142858317),
 ( 1.000000000000000000, 1.000000000000000000, 1.000000000000000000, 1.000000000000000000, 1.000000000000000000, 1.000000000000000000, 1.000000000000000000, 1.000000000000000000, 1.000000000000000000, 1.000000000000000000, 1.000000000000000000, 1.000000000000000000, 1.000000000000000000, 1.000000000000000000, 1.000000000000000000, 1.000000000000000000, 1.000000000000000000, 1.000000000000000000, 1.000000000000000000, 1.000000000000000000, 1.000000000000000000, 1.000000000000000000, 1.000000000000000000, 1.000000000000000000, 1.000000000000000000, 1.000000000000000000, 1.000000000000000000, 1.000000000000000000, 1.000000000000000000, 1.000000000000000000, 1.000000000000000000, 1.000000000000000000, 1.000000000000000000, 1.000000000000000000) ) ) 
 REPRESENTATION_ITEM ( '' )  SURFACE ( )  );
#41866=CARTESIAN_POINT ( 'NONE',  ( 39.04923757935661399, 48.00000000000000000, 52.30342408741256577 ) ) ;
#41876=CARTESIAN_POINT ( 'NONE',  ( -26.50079164160752399, 18.64284798593038772, 27.83217509638362586 ) ) ;
#41890=CARTESIAN_POINT ( 'NONE',  ( 20.59266090671921745, 41.82625683843084374, -78.90645973795369628 ) ) ;
#41909=( NAMED_UNIT ( * ) PLANE_ANGLE_UNIT ( ) SI_UNIT ( $, .RADIAN. ) );
#41949=DIRECTION ( 'NONE',  ( 1.160749806054361473E-16, 0.000000000000000000, -1.000000000000000000 ) ) ;
#41951=SURFACE_STYLE_FILL_AREA ( #32829 ) ;
#41966=EDGE_CURVE ( 'NONE', #46431, #20, #46652, .T. ) ;
#41999=CARTESIAN_POINT ( 'NONE',  ( -7.090506018371190322, 41.24767894959148151, -58.61600934880981839 ) ) ;
#42023=ORIENTED_EDGE ( 'NONE', *, *, #51531, .T. ) ;
#42025=CARTESIAN_POINT ( 'NONE',  ( 6.338673411933466895, 41.81695763293575396, -59.02782193812689115 ) ) ;
#42043=CARTESIAN_POINT ( 'NONE',  ( 18.02665060324837398, 45.00000000000000711, 62.54981906107154543 ) ) ;
#42048=CARTESIAN_POINT ( 'NONE',  ( -9.366761589750341344, -5.000000000000001776, -18.69503824872587572 ) ) ;
#42055=CARTESIAN_POINT ( 'NONE',  ( -18.91791044776116237, 46.94999999999998153, 62.18611311450883505 ) ) ;
#42056=CARTESIAN_POINT ( 'NONE',  ( -7.500000000000002665, -4.999999999999998224, -68.91429205908086431 ) ) ;
#42065=CARTESIAN_POINT ( 'NONE',  ( 15.17227823171669243, -3.000000000000002665, -86.54073391195466058 ) ) ;
#42082=CARTESIAN_POINT ( 'NONE',  ( -17.50000000000917311, 50.03760136707322204, 61.20291971386541263 ) ) ;
#42087=EDGE_CURVE ( 'NONE', #72021, #25938, #11498, .T. ) ;
#42095=CARTESIAN_POINT ( 'NONE',  ( -14.91271302809441401, 41.98564543112699710, -86.62215342991694911 ) ) ;
#42103=CARTESIAN_POINT ( 'NONE',  ( -9.739726766104286781, -3.000000000000002665, -87.61747884499033034 ) ) ;
#42131=CARTESIAN_POINT ( 'NONE',  ( -5.902907888919633805, -5.000000000000000888, -73.20788160634965891 ) ) ;
#42160=CARTESIAN_POINT ( 'NONE',  ( 4.852941176470587870, 25.66666666666755248, -70.80672828634229177 ) ) ;
#42185=VECTOR ( 'NONE', #38585, 1000.000000000000000 ) ;
#42227=CARTESIAN_POINT ( 'NONE',  ( -7.500000000000003553, 18.65452285268246513, -40.72535638071818909 ) ) ;
#42243=CARTESIAN_POINT ( 'NONE',  ( -47.37019975542479955, 42.00000000008224532, -36.40416150956886554 ) ) ;
#42269=CARTESIAN_POINT ( 'NONE',  ( 7.855360403618686149, 47.99999999999999289, -97.83275449052108286 ) ) ;
#42273=CARTESIAN_POINT ( 'NONE',  ( -7.226138746538454782, 41.34018742858377493, -70.07054302848561633 ) ) ;
#42283=CARTESIAN_POINT ( 'NONE',  ( -6.145819459793597339, -5.000000000000000000, -7.996135855215887212 ) ) ;
#42373=CARTESIAN_POINT ( 'NONE',  ( -9.109994089937119455, -4.999999999999461764, -17.31936419814998374 ) ) ;
#42378=FILL_AREA_STYLE ('',( #38288 ) ) ;
#42396=CARTESIAN_POINT ( 'NONE',  ( 60.66923414622826982, 50.00000000000000000, 17.93278245653309710 ) ) ;
#42429=( NAMED_UNIT ( * ) PLANE_ANGLE_UNIT ( ) SI_UNIT ( $, .RADIAN. ) );
#42441=CARTESIAN_POINT ( 'NONE',  ( -9.999999999999989342, 49.99999999999999289, -83.69100306251235111 ) ) ;
#42481=CARTESIAN_POINT ( 'NONE',  ( -17.49999999999997513, 50.00000000000000000, 63.82142195434425958 ) ) ;
#42548=ORIENTED_EDGE ( 'NONE', *, *, #6613, .F. ) ;
#42552=CARTESIAN_POINT ( 'NONE',  ( 6.955654034292342303, 41.30888721648646822, -58.54628189783632308 ) ) ;
#42554=CARTESIAN_POINT ( 'NONE',  ( -5.500000000000007994, 42.00000000000000000, -71.41947339646975479 ) ) ;
#42555=EDGE_LOOP ( 'NONE', ( #93647, #58741, #31937, #44025 ) ) ;
#42569=B_SPLINE_CURVE_WITH_KNOTS ( 'NONE', 3,
 ( #72286, #38360, #71224, #30262, #105191, #31337, #1565, #58776, #8608, #25367, #91672, #477, #49599, #42043, #57152, #7533, #16711, #73330, #1008, #33993, #90065, #82507, #91152, #58224, #24305, #83039, #50131, #34527, #16171, #9658, #40450, #65261, #98150, #106229, #9131, #42571, #98670 ),
 .UNSPECIFIED., .F., .F.,
 ( 4, 1, 1, 1, 1, 1, 2, 2, 1, 1, 1, 2, 2, 2, 1, 1, 1, 2, 2, 1, 1, 1, 1, 2, 2, 4 ),
 ( 0.000000000000000000, 0.1250000000000957567, 0.1875000000001431355, 0.2187500000001631750, 0.2343750000001732225, 0.2421875000001741385, 0.2460937500001765532, 0.2500000000001789680, 0.3125000000001895706, 0.3437500000002005063, 0.3593750000002058909, 0.3671875000002068345, 0.3750000000002077782, 0.5000000000001820766, 0.5625000000001837419, 0.5937500000001907363, 0.6093750000001949552, 0.6171875000001970646, 0.6250000000001990630, 0.6875000000002183809, 0.7187500000002283729, 0.7343750000002405853, 0.7421875000002466916, 0.7460937500002428058, 0.7500000000002389200, 1.000000000000000000 ),
 .UNSPECIFIED. ) ;
#42571=CARTESIAN_POINT ( 'NONE',  ( 17.50000000000001066, 45.00000000000000711, 63.82889773232136577 ) ) ;
#42597=CARTESIAN_POINT ( 'NONE',  ( -5.293743209235371339, -3.000000000000002665, -99.09939186120345767 ) ) ;
#42615=CARTESIAN_POINT ( 'NONE',  ( -19.16305615217759950, 49.74182397839572900, 61.63059818732714490 ) ) ;
#42630=CARTESIAN_POINT ( 'NONE',  ( -25.18435656174467141, 41.53024528245975944, -72.71459547366467291 ) ) ;
#42670=( NAMED_UNIT ( * ) PLANE_ANGLE_UNIT ( ) SI_UNIT ( $, .RADIAN. ) );
#42680=CARTESIAN_POINT ( 'NONE',  ( -11.53688828317231874, -4.929764295086950021, -12.56596437507229247 ) ) ;
#42700=CARTESIAN_POINT ( 'NONE',  ( -7.182275917706625101, 41.30104301296705671, -58.77094024890655533 ) ) ;
#42723=UNCERTAINTY_MEASURE_WITH_UNIT (LENGTH_MEASURE( 1.000000000000000082E-05 ), #82239, 'distance_accuracy_value', 'NONE');
#42741=CARTESIAN_POINT ( 'NONE',  ( 32.23780387954349891, 18.64284798592760239, 20.91998874883894644 ) ) ;
#42747=CARTESIAN_POINT ( 'NONE',  ( 0.000000000000000000, 47.00000000000000000, 0.000000000000000000 ) ) ;
#42778=STYLED_ITEM ( 'NONE', ( #33271 ), #27337 ) ;
#42783=CARTESIAN_POINT ( 'NONE',  ( 45.60838156032635027, 42.00000000000000000, 79.13121736029046360 ) ) ;
#42792=CARTESIAN_POINT ( 'NONE',  ( 64.12443038224847669, 40.83928227018758861, -11.04305639294624264 ) ) ;
#42809=CARTESIAN_POINT ( 'NONE',  ( -11.43775816216262697, 48.00000000000000711, -94.77568223238722567 ) ) ;
#42813=CARTESIAN_POINT ( 'NONE',  ( -7.311409912948124479, 40.00000000004124701, -70.68780158692078430 ) ) ;
#42818=ADVANCED_FACE ( 'NONE', ( #54212 ), #87374, .T. ) ;
#42823=CARTESIAN_POINT ( 'NONE',  ( 4.933292146132942868, 41.54835750584369691, -70.57172791956975288 ) ) ;
#42847=CARTESIAN_POINT ( 'NONE',  ( 12.50000000000000533, 32.24110320235760696, -50.45876292934040208 ) ) ;
#42875=FACE_OUTER_BOUND ( 'NONE', #47098, .T. ) ;
#42897=( NAMED_UNIT ( * ) SI_UNIT ( $, .STERADIAN. ) SOLID_ANGLE_UNIT ( ) );
#42909=CARTESIAN_POINT ( 'NONE',  ( -6.690415133250795954, 41.73276121203647904, -59.04972748448755482 ) ) ;
#42920=CLOSED_SHELL ( 'NONE', ( #19950, #74164, #87845, #32759, #69298, #93386, #57848, #93490, #78669, #69395, #30161, #27337, #38431, #27914, #33066, #47135, #65288, #25798, #27116, #77737, #96508, #40818, #70975, #4960, #11158, #76291, #23190, #6345, #34024, #23817, #47680, #32934, #105888, #51070, #70542, #21210, #39919, #83037, #19730, #12828, #2228, #67722, #85386, #62766, #76505, #106687, #30614, #72666, #41554, #45074, #46730, #12512, #75713, #100252, #68552, #62444, #59337, #69099, #101920, #96260, #33641, #27260, #52538, #24876, #100763, #7550, #68281, #101388, #87591, #50189, #94497, #75757, #68626, #57542, #23751, #53283, #54693, #85465, #16884, #73129, #19013, #102995, #64682, #51131, #65343, #42818, #44467 ) ) ;
#42932=CARTESIAN_POINT ( 'NONE',  ( 7.500000000000005329, -3.000000000000000888, -52.94236561372726868 ) ) ;
#42937=( BOUNDED_CURVE ( )  B_SPLINE_CURVE ( 2, ( #19925, #36629, #46801 ),
 .UNSPECIFIED., .F., .F. ) 
 B_SPLINE_CURVE_WITH_KNOTS ( ( 3, 3 ),
 ( 0.000000000000000000, 1.000000000000000000 ),
 .UNSPECIFIED. ) 
 CURVE ( )  GEOMETRIC_REPRESENTATION_ITEM ( )  RATIONAL_B_SPLINE_CURVE ( ( 1.000000000000000000, 1.857142857142858317, 1.000000000000000000 ) ) 
 REPRESENTATION_ITEM ( '' )  );
#42938=FACE_OUTER_BOUND ( 'NONE', #85514, .T. ) ;
#42941=CARTESIAN_POINT ( 'NONE',  ( -5.393385909618478635, 41.67668960927788646, -58.73074311017365545 ) ) ;
#42953=CARTESIAN_POINT ( 'NONE',  ( -27.57459505077822470, 18.64284798593290660, -26.76870628202681246 ) ) ;
#42954=UNCERTAINTY_MEASURE_WITH_UNIT (LENGTH_MEASURE( 1.000000000000000082E-05 ), #82482, 'distance_accuracy_value', 'NONE');
#42958=CARTESIAN_POINT ( 'NONE',  ( 7.149999999999997691, 41.65000000000000568, -59.82695526683420439 ) ) ;
#42961=LINE ( 'NONE', #75853, #37948 ) ;
#42967=CARTESIAN_POINT ( 'NONE',  ( 27.61861779010158457, 41.31838093711942150, -69.45717397145128302 ) ) ;
#42986=CARTESIAN_POINT ( 'NONE',  ( -9.596002107494335576, 50.00000000000000000, -77.62543935900903591 ) ) ;
#43003=UNCERTAINTY_MEASURE_WITH_UNIT (LENGTH_MEASURE( 1.000000000000000082E-05 ), #26301, 'distance_accuracy_value', 'NONE');
#43060=MECHANICAL_DESIGN_GEOMETRIC_PRESENTATION_REPRESENTATION('',(#24151),#79002);
#43083=MECHANICAL_DESIGN_GEOMETRIC_PRESENTATION_REPRESENTATION('',(#96454),#101752);
#43091=FILL_AREA_STYLE ('',( #67371 ) ) ;
#43142=CARTESIAN_POINT ( 'NONE',  ( 13.73780227957887057, -3.000000000000002665, -78.37846873787221114 ) ) ;
#43163=EDGE_CURVE ( 'NONE', #80415, #37125, #3692, .T. ) ;
#43208=CARTESIAN_POINT ( 'NONE',  ( 14.33580415461469570, 42.00000000000010658, -89.41414988890622340 ) ) ;
#43210=CARTESIAN_POINT ( 'NONE',  ( 9.432319653620828248, -4.999999999999999112, -70.68463330170209247 ) ) ;
#43224=PRESENTATION_STYLE_ASSIGNMENT (( #10307 ) ) ;
#43238=CARTESIAN_POINT ( 'NONE',  ( -7.294238536526225225, 41.09454800505173466, -58.80184262229552417 ) ) ;
#43239=CARTESIAN_POINT ( 'NONE',  ( 7.036764705882358584, 40.00000000373366049, -71.06385277390856459 ) ) ;
#43294=CARTESIAN_POINT ( 'NONE',  ( -4.852941176470593199, 42.83333333333328596, -70.80672828634229177 ) ) ;
#43321=CARTESIAN_POINT ( 'NONE',  ( -45.60838156036751201, 42.00000000000000000, -79.13121736029046360 ) ) ;
#43328=ORIENTED_EDGE ( 'NONE', *, *, #59216, .T. ) ;
#43330=CARTESIAN_POINT ( 'NONE',  ( -52.56483885390522914, 40.83906611473334891, -38.23529411764704378 ) ) ;
#43339=CARTESIAN_POINT ( 'NONE',  ( -6.019162162301046060, 39.99999999999999289, -71.20548073448676973 ) ) ;
#43347=CARTESIAN_POINT ( 'NONE',  ( -8.737863884121393809, 49.99999999999999289, -90.03618980231146907 ) ) ;
#43366=EDGE_LOOP ( 'NONE', ( #51433, #72399 ) ) ;
#43421=CARTESIAN_POINT ( 'NONE',  ( -5.487124250504801459, 41.99999999999998579, -59.74242263126210162 ) ) ;
#43425=EDGE_CURVE ( 'NONE', #53678, #96838, #41691, .T. ) ;
#43438=CARTESIAN_POINT ( 'NONE',  ( 43.69716417794892749, 48.00000000000000000, 48.48761666242516100 ) ) ;
#43452=CARTESIAN_POINT ( 'NONE',  ( -6.795578989018840943, -5.000000000000069278, -15.32583302412394310 ) ) ;
#43473=CARTESIAN_POINT ( 'NONE',  ( 5.977870854928313271, 41.99823411354464753, -69.20734001019310710 ) ) ;
#43475=CARTESIAN_POINT ( 'NONE',  ( -63.25915952246064222, 50.00000000000000000, 0.7870165385200997843 ) ) ;
#43487=CARTESIAN_POINT ( 'NONE',  ( -37.46714894334873946, 18.64284798593131853, 8.551881563997355329 ) ) ;
#43488=UNCERTAINTY_MEASURE_WITH_UNIT (LENGTH_MEASURE( 1.000000000000000082E-05 ), #78700, 'distance_accuracy_value', 'NONE');
#43500=CARTESIAN_POINT ( 'NONE',  ( 41.43935051928187363, 39.62186541985202126, -51.04584900469333064 ) ) ;
#43503=FILL_AREA_STYLE ('',( #93655 ) ) ;
#43505=EDGE_CURVE ( 'NONE', #16973, #11528, #88502, .T. ) ;
#43517=CARTESIAN_POINT ( 'NONE',  ( -11.99999999999999467, 50.00000000000000000, -83.42920367502570400 ) ) ;
#43558=CARTESIAN_POINT ( 'NONE',  ( 14.81135246989093801, 41.99477691750401931, -87.54767829888531594 ) ) ;
#43604=CARTESIAN_POINT ( 'NONE',  ( 12.50000000000000000, 0.4010731690309218278, -18.19005076526336140 ) ) ;
#43614=CARTESIAN_POINT ( 'NONE',  ( -23.70422451879018055, 42.00000000000000000, 88.20421627933653497 ) ) ;
#43623=CARTESIAN_POINT ( 'NONE',  ( 6.873632531530262213, 41.52280089014492148, -58.77795419705466884 ) ) ;
#43624=CARTESIAN_POINT ( 'NONE',  ( -7.500000000000007994, 40.00000000000000000, -65.90297133633691828 ) ) ;
#43643=CARTESIAN_POINT ( 'NONE',  ( 7.445752247298699444, 40.55658335127025538, -70.17153608768727224 ) ) ;
#43652=CARTESIAN_POINT ( 'NONE',  ( 18.91781669292794987, 48.00000000000000000, 62.18610382930901892 ) ) ;
#43662=CARTESIAN_POINT ( 'NONE',  ( -10.19007819943550786, -3.000000000000002665, -96.34610920172687543 ) ) ;
#43681=CARTESIAN_POINT ( 'NONE',  ( -17.49999999999997158, 50.67917894244530430, 63.46126552128608722 ) ) ;
#43695=CARTESIAN_POINT ( 'NONE',  ( -6.690415133250795954, 41.73276121203647904, -59.04972748448755482 ) ) ;
#43702=CARTESIAN_POINT ( 'NONE',  ( 1.308996937483426715, -3.000000000000002665, -75.00000000000001421 ) ) ;
#43708=ORIENTED_EDGE ( 'NONE', *, *, #3797, .F. ) ;
#43710=CARTESIAN_POINT ( 'NONE',  ( 18.16578424162143079, -4.332661967058973218, -1.112710490967694810 ) ) ;
#43744=CARTESIAN_POINT ( 'NONE',  ( -11.36244727931663689, -4.957670368922723725, -12.57265801651846893 ) ) ;
#43758=CARTESIAN_POINT ( 'NONE',  ( -19.12563387234284562, 49.70270881371637017, 61.69659611208896877 ) ) ;
#43759=CARTESIAN_POINT ( 'NONE',  ( -7.311443696993588759, 40.96481804360126233, -58.73188616880665336 ) ) ;
#43760=CARTESIAN_POINT ( 'NONE',  ( 5.207236450897640090, 40.28819309316081387, -70.92786837021314739 ) ) ;
#43775=ORIENTED_EDGE ( 'NONE', *, *, #77534, .T. ) ;
#43799=CARTESIAN_POINT ( 'NONE',  ( 21.23076943213705903, 18.64284798592824899, 32.03398753740996341 ) ) ;
#43825=CARTESIAN_POINT ( 'NONE',  ( 17.50000000000003553, 49.99999999999769074, 59.56761335716116434 ) ) ;
#43838=MECHANICAL_DESIGN_GEOMETRIC_PRESENTATION_REPRESENTATION('',(#21473),#104124);
#43844=SURFACE_SIDE_STYLE ('',( #100483 ) ) ;
#43852=CARTESIAN_POINT ( 'NONE',  ( 20.52986868762305406, 40.83832388658744605, 61.74416104812828365 ) ) ;
#43862=CARTESIAN_POINT ( 'NONE',  ( 9.258863595255466095, 41.99999999999999289, -70.74260034492780846 ) ) ;
#43877=ORIENTED_EDGE ( 'NONE', *, *, #105401, .F. ) ;
#43898=CARTESIAN_POINT ( 'NONE',  ( -6.200186772461218965, 41.06054036581593891, -71.07396401990634160 ) ) ;
#43901=EDGE_CURVE ( 'NONE', #3104, #58075, #67851, .T. ) ;
#43932=CARTESIAN_POINT ( 'NONE',  ( -34.54697356181507217, 42.66571874608613513, -63.00576358640330454 ) ) ;
#43941=( NAMED_UNIT ( * ) PLANE_ANGLE_UNIT ( ) SI_UNIT ( $, .RADIAN. ) );
#43947=CARTESIAN_POINT ( 'NONE',  ( 11.66900197424181940, -4.900341487329494150, -12.56042530111529310 ) ) ;
#43965=CARTESIAN_POINT ( 'NONE',  ( 5.957442974701732119, 48.00000000000000000, 65.00000000000000000 ) ) ;
#43979=CARTESIAN_POINT ( 'NONE',  ( -9.572623054141676135, -4.999999999999671374, -20.18584606598301434 ) ) ;
#43981=CARTESIAN_POINT ( 'NONE',  ( 17.51664081523980698, 50.00000000000000000, 63.26386782005719311 ) ) ;
#43995=UNCERTAINTY_MEASURE_WITH_UNIT (LENGTH_MEASURE( 1.000000000000000082E-05 ), #79333, 'distance_accuracy_value', 'NONE');
#44004=CARTESIAN_POINT ( 'NONE',  ( 6.762666758904207320, 41.72338998057573178, -70.10115389619511461 ) ) ;
#44005=CARTESIAN_POINT ( 'NONE',  ( 22.66220480930525127, 50.00000000000000000, 59.06576954297840842 ) ) ;
#44025=ORIENTED_EDGE ( 'NONE', *, *, #40082, .F. ) ;
#44044=SURFACE_STYLE_USAGE ( .BOTH. , #35998 ) ;
#44047=CARTESIAN_POINT ( 'NONE',  ( -7.374560640988130800, 50.00000000000000000, -94.59600210748763516 ) ) ;
#44056=B_SPLINE_CURVE_WITH_KNOTS ( 'NONE', 3,
 ( #78374, #102660, #4494, #28818 ),
 .UNSPECIFIED., .F., .F.,
 ( 4, 4 ),
 ( 0.000000000000000000, 1.000000000000000000 ),
 .UNSPECIFIED. ) ;
#44095=CARTESIAN_POINT ( 'NONE',  ( 7.468836275491999466, -3.123212597914878152, -19.53079664952245409 ) ) ;
#44119=CARTESIAN_POINT ( 'NONE',  ( 1.469576158976823356E-15, 50.00000000000000000, -73.00000000000001421 ) ) ;
#44120=MECHANICAL_DESIGN_GEOMETRIC_PRESENTATION_REPRESENTATION('',(#57873),#94165);
#44136=CARTESIAN_POINT ( 'NONE',  ( -5.465597153059336577, 41.93635067907730019, -70.00903446595771129 ) ) ;
#44157=CARTESIAN_POINT ( 'NONE',  ( 30.67950393665801556, 18.64316884713159794, -23.57730434125293328 ) ) ;
#44166=CARTESIAN_POINT ( 'NONE',  ( -7.500000000000007105, 40.00000000000000000, -62.89165061483231511 ) ) ;
#44171=ORIENTED_EDGE ( 'NONE', *, *, #21996, .F. ) ;
#44187=CARTESIAN_POINT ( 'NONE',  ( 7.499935202740302564, 40.55407105531765666, -69.64903775193384661 ) ) ;
#44207=VECTOR ( 'NONE', #37347, 1000.000000000000000 ) ;
#44208=CARTESIAN_POINT ( 'NONE',  ( 8.831401106173728977, -5.000000000000002665, -94.83329464149440469 ) ) ;
#44225=CARTESIAN_POINT ( 'NONE',  ( -17.49999999999991473, 51.99987222567126111, 59.97465830877287374 ) ) ;
#44255=CARTESIAN_POINT ( 'NONE',  ( 12.76371622530481709, -5.000000000001442402, 12.10534828917873895 ) ) ;
#44263=VECTOR ( 'NONE', #38684, 1000.000000000000000 ) ;
#44278=CARTESIAN_POINT ( 'NONE',  ( 19.49275996658308685, 49.99917725797203616, 60.06179185754866268 ) ) ;
#44288=FACE_OUTER_BOUND ( 'NONE', #101234, .T. ) ;
#44300=CARTESIAN_POINT ( 'NONE',  ( -19.21945236286198266, 49.79349494036195267, 61.52156576933356291 ) ) ;
#44301=CARTESIAN_POINT ( 'NONE',  ( -7.495924014863156515, 40.46140149715811418, -59.65192205970540584 ) ) ;
#44302=CARTESIAN_POINT ( 'NONE',  ( 6.519736037359969316, 40.56016599668093647, -71.18560176916710702 ) ) ;
#44315=CARTESIAN_POINT ( 'NONE',  ( 5.328772475725927826, 26.78864416899411793, -45.33255757618040604 ) ) ;
#44317=CARTESIAN_POINT ( 'NONE',  ( -7.999999999999998224, -2.999999999999999556, -1.047197551196598964 ) ) ;
#44320=CARTESIAN_POINT ( 'NONE',  ( -7.374560640984191728, -5.000000000000002665, -75.40399789251388540 ) ) ;
#44345=EDGE_CURVE ( 'NONE', #84701, #60656, #9580, .T. ) ;
#44358=EDGE_LOOP ( 'NONE', ( #39865, #4724, #591, #94067 ) ) ;
#44369=CARTESIAN_POINT ( 'NONE',  ( 19.23735690889500916, 49.80931112121767512, 61.48632125443233321 ) ) ;
#44387=CARTESIAN_POINT ( 'NONE',  ( -11.85444436800005263, 42.00000000000000000, 90.56128410203886858 ) ) ;
#44395=CARTESIAN_POINT ( 'NONE',  ( -60.44710093648797056, 40.83768557982805447, 24.08449874113471623 ) ) ;
#44413=CARTESIAN_POINT ( 'NONE',  ( -11.99999999999999467, 50.00000000000000000, -86.57079632497432442 ) ) ;
#44417=CARTESIAN_POINT ( 'NONE',  ( -7.439122753854266357, 41.00341855746702180, -68.91429205792265122 ) ) ;
#44426=CARTESIAN_POINT ( 'NONE',  ( 7.004291983109769859, 40.56179000455576045, -71.01843131752761451 ) ) ;
#44431=CARTESIAN_POINT ( 'NONE',  ( -9.500000000000000000, -5.000000000000000000, -36.97043916959987087 ) ) ;
#44439=CARTESIAN_POINT ( 'NONE',  ( -7.036764705882398552, 40.00000000007573675, -71.06385277390853616 ) ) ;
#44467=ADVANCED_FACE ( 'NONE', ( #37104 ), #98382, .T. ) ;
#44485=CARTESIAN_POINT ( 'NONE',  ( 5.369174336198356379, 44.20122194677738037, -60.96850753999265748 ) ) ;
#44492=CARTESIAN_POINT ( 'NONE',  ( 10.87128754221327931, -4.996251208102432173, -12.57223391742547314 ) ) ;
#44507=SURFACE_STYLE_USAGE ( .BOTH. , #84957 ) ;
#44512=CARTESIAN_POINT ( 'NONE',  ( -7.150000055923752207, 41.64999994407625650, -59.82695526654634222 ) ) ;
#44524=EDGE_CURVE ( 'NONE', #27308, #56205, #2616, .T. ) ;
#44535=CARTESIAN_POINT ( 'NONE',  ( -5.688070444779528501, -4.337726323027712994, -16.91120255684542784 ) ) ;
#44546=CARTESIAN_POINT ( 'NONE',  ( 5.313748243244007519, 41.99394926078451107, -69.45901782876110531 ) ) ;
#44548=CARTESIAN_POINT ( 'NONE',  ( -55.22048556080422799, 49.99999999999999289, 34.80214219305234025 ) ) ;
#44550=B_SPLINE_CURVE_WITH_KNOTS ( 'NONE', 3,
 ( #54381, #96479, #4806, #104016, #37745, #14461, #30159, #13406, #86805, #70070, #79747, #86279, #22618, #55453, #46329, #95949, #12351, #38777 ),
 .UNSPECIFIED., .F., .F.,
 ( 4, 2, 2, 2, 2, 2, 2, 2, 4 ),
 ( 0.4999999999971661002, 0.5624999999975203169, 0.6249999999978745890, 0.6874999999982288612, 0.7499999999985831334, 0.8124999999989372945, 0.8749999999992915667, 0.9374999999996458389, 1.000000000000000000 ),
 .UNSPECIFIED. ) ;
#44573=CARTESIAN_POINT ( 'NONE',  ( 51.48757442383973881, 38.95383793068620548, -37.45149417477089315 ) ) ;
#44582=( NAMED_UNIT ( * ) SI_UNIT ( $, .STERADIAN. ) SOLID_ANGLE_UNIT ( ) );
#44589=CARTESIAN_POINT ( 'NONE',  ( 37.46929538836619855, 50.00000000000000000, -55.58823529426165067 ) ) ;
#44591=CARTESIAN_POINT ( 'NONE',  ( 11.68767211932491712, 50.00000000000000000, -81.85902538600508649 ) ) ;
#44614=( GEOMETRIC_REPRESENTATION_CONTEXT ( 3 ) GLOBAL_UNCERTAINTY_ASSIGNED_CONTEXT ( ( #83935 ) ) GLOBAL_UNIT_ASSIGNED_CONTEXT ( ( #104781, #78908, #62234 ) ) REPRESENTATION_CONTEXT ( 'NONE', 'WORKASPACE' ) );
#44625=CARTESIAN_POINT ( 'NONE',  ( -7.036764705882381676, 40.00000000007575807, -71.06385277390852195 ) ) ;
#44634=FILL_AREA_STYLE ('',( #51635 ) ) ;
#44674=CARTESIAN_POINT ( 'NONE',  ( -6.639654777812401321, 41.83126063031291864, -69.93930137318731965 ) ) ;
#44679=CARTESIAN_POINT ( 'NONE',  ( 1.663454779225379987, -5.000000000000000000, 16.34235115354128709 ) ) ;
#44680=CARTESIAN_POINT ( 'NONE',  ( -6.232496158895186156, 41.83455024993975968, -59.02481301687200244 ) ) ;
#44699=CARTESIAN_POINT ( 'NONE',  ( 47.37019975563026719, 41.99999999991776178, 36.40416150969240050 ) ) ;
#44707=CARTESIAN_POINT ( 'NONE',  ( 6.798788993459229602, 41.26122520824648632, -58.42041755854287999 ) ) ;
#44709=EDGE_LOOP ( 'NONE', ( #50422, #76492, #49870, #63734 ) ) ;
#44712=ORIENTED_EDGE ( 'NONE', *, *, #23275, .F. ) ;
#44733=CARTESIAN_POINT ( 'NONE',  ( -13.07034959214954384, 42.28767730836202787, -92.53124009454084842 ) ) ;
#44747=CARTESIAN_POINT ( 'NONE',  ( 9.290012601907397638, -5.000000000000002665, -75.85638632170150686 ) ) ;
#44748=CARTESIAN_POINT ( 'NONE',  ( 13.85425718576306053, -3.000000000000003109, -90.90560122695632117 ) ) ;
#44766=CARTESIAN_POINT ( 'NONE',  ( -17.49999999999998579, 51.01864103017746999, 63.17274301512910739 ) ) ;
#44787=CARTESIAN_POINT ( 'NONE',  ( 7.500000000000007105, 40.28750351091937176, -59.87155384411956760 ) ) ;
#44797=CARTESIAN_POINT ( 'NONE',  ( -14.92208856358372948, -5.000000000000000000, -7.448748508017043690 ) ) ;
#44820=VERTEX_POINT ( 'NONE', #11855 ) ;
#44821=CARTESIAN_POINT ( 'NONE',  ( 19.49162701228398831, 49.99890833186964301, 60.08453375891043891 ) ) ;
#44832=CARTESIAN_POINT ( 'NONE',  ( -7.500000000000001776, -7.939616441372559841, -16.39477006944641957 ) ) ;
#44845=CARTESIAN_POINT ( 'NONE',  ( -19.35113623624150847, 49.90206012729868235, 61.17429927557744662 ) ) ;
#44846=CARTESIAN_POINT ( 'NONE',  ( 4.881098022930994595, 41.14559726925936900, -70.72437870144329963 ) ) ;
#44859=( GEOMETRIC_REPRESENTATION_CONTEXT ( 3 ) GLOBAL_UNCERTAINTY_ASSIGNED_CONTEXT ( ( #18708 ) ) GLOBAL_UNIT_ASSIGNED_CONTEXT ( ( #90504, #73233, #33893 ) ) REPRESENTATION_CONTEXT ( 'NONE', 'WORKASPACE' ) );
#44860=CARTESIAN_POINT ( 'NONE',  ( 5.227629274769425294, 7.725904378977054066, -28.12787702362269471 ) ) ;
#44861=CARTESIAN_POINT ( 'NONE',  ( 12.40392177672334029, -4.188815825756464051, -12.99189655448344105 ) ) ;
#44920=CARTESIAN_POINT ( 'NONE',  ( 34.69770406740761359, 42.64551627458131833, -62.79854340097827503 ) ) ;
#44922=STYLED_ITEM ( 'NONE', ( #78521 ), #50189 ) ;
#44932=CARTESIAN_POINT ( 'NONE',  ( -37.36680950586716676, 18.64316884709021238, -10.04205104292877770 ) ) ;
#44941=CARTESIAN_POINT ( 'NONE',  ( 43.67033176680568118, 40.83721295465350920, 48.51745517052664525 ) ) ;
#44951=CARTESIAN_POINT ( 'NONE',  ( 6.019162162299725338, 41.99999999999999289, -71.20548073449060666 ) ) ;
#44958=CARTESIAN_POINT ( 'NONE',  ( 3.140974613991526887, 50.00000000000000000, -73.31232788067644890 ) ) ;
#44974=CARTESIAN_POINT ( 'NONE',  ( -7.500000000000000000, -4.999999999999999112, -20.99851272547259029 ) ) ;
#44983=CARTESIAN_POINT ( 'NONE',  ( -6.040960885908838840, 41.48433382036304096, -70.81801790822488840 ) ) ;
#44995=CARTESIAN_POINT ( 'NONE',  ( -17.59381741287697665, 45.00000000000001421, 63.12291724128729697 ) ) ;
#45024=CARTESIAN_POINT ( 'NONE',  ( 5.365535441410388628, 42.28877518162276772, -59.25308630239388208 ) ) ;
#45030=CARTESIAN_POINT ( 'NONE',  ( 11.62087833628057432, -4.912050167074662355, -12.56209946431235203 ) ) ;
#45044=CARTESIAN_POINT ( 'NONE',  ( 9.500000000000000000, -5.000000000000000000, -36.97043916959991350 ) ) ;
#45048=CARTESIAN_POINT ( 'NONE',  ( 39.04923757935661399, 48.00000000000000000, 52.30342408741256577 ) ) ;
#45052=CARTESIAN_POINT ( 'NONE',  ( -6.814345648127551947, 41.80574614977290793, -59.39410014841684671 ) ) ;
#45062=CARTESIAN_POINT ( 'NONE',  ( 17.50000000000000711, 50.00000000000000711, 63.71427545230567802 ) ) ;
#45068=ORIENTED_EDGE ( 'NONE', *, *, #80036, .F. ) ;
#45072=CARTESIAN_POINT ( 'NONE',  ( 50.94745919686198476, 50.00000000000000000, -37.05882352941176094 ) ) ;
#45074=ADVANCED_FACE ( 'NONE', ( #79779 ), #28832, .T. ) ;
#45085=CARTESIAN_POINT ( 'NONE',  ( 5.342383757966601365, 41.79455485342771226, -70.44171435326786934 ) ) ;
#45107=FILL_AREA_STYLE ('',( #103329 ) ) ;
#45109=CARTESIAN_POINT ( 'NONE',  ( 23.97042203813707673, 41.62162537289933084, -74.34607944144084968 ) ) ;
#45119=CARTESIAN_POINT ( 'NONE',  ( 37.55249893777119041, 42.26547227746785751, -58.87384932487446321 ) ) ;
#45127=CARTESIAN_POINT ( 'NONE',  ( -5.036189802311180408, 48.00000000000000000, -76.26213611587843388 ) ) ;
#45151=CARTESIAN_POINT ( 'NONE',  ( -5.221602127173184726, 7.006837110516260125, -27.47515623844168786 ) ) ;
#45156=CARTESIAN_POINT ( 'NONE',  ( -6.701893397842001221, 41.44328394191487774, -70.59544911652842814 ) ) ;
#45167=EDGE_CURVE ( 'NONE', #17802, #77528, #57432, .T. ) ;
#45173=EDGE_CURVE ( 'NONE', #21685, #70585, #24237, .T. ) ;
#45180=( BOUNDED_SURFACE ( )  B_SPLINE_SURFACE ( 2, 3, ( 
 ( #12113, #45044, #93043, #60175 ),
 ( #93582, #27826, #61218, #11574 ),
 ( #19207, #61766, #76850, #18651 ) ),
 .UNSPECIFIED., .F., .F., .F. ) 
 B_SPLINE_SURFACE_WITH_KNOTS ( ( 3, 3 ),
 ( 4, 4 ),
 ( 0.000000000000000000, 1.000000000000000000 ),
 ( 0.02099851272547260256, 0.06891429205785459811 ),
 .UNSPECIFIED. ) 
 GEOMETRIC_REPRESENTATION_ITEM ( )  RATIONAL_B_SPLINE_SURFACE ( (
 ( 1.000000000000000000, 1.000000000000000000, 1.000000000000000000, 1.000000000000000000),
 ( 1.857142857142858317, 1.857142857142858317, 1.857142857142858317, 1.857142857142858317),
 ( 1.000000000000000000, 1.000000000000000000, 1.000000000000000000, 1.000000000000000000) ) ) 
 REPRESENTATION_ITEM ( '' )  SURFACE ( )  );
#45209=CARTESIAN_POINT ( 'NONE',  ( -5.385153346518941397, 41.85687274187981188, -70.29203086348832130 ) ) ;
#45213=CARTESIAN_POINT ( 'NONE',  ( 16.21548335344357028, -5.000000000000000000, -2.627579377633686430 ) ) ;
#45214=CARTESIAN_POINT ( 'NONE',  ( -6.507454417189439511, 41.74144650497772346, -58.94379852000331965 ) ) ;
#45230=CARTESIAN_POINT ( 'NONE',  ( 6.847405647391515693, 41.77151288785266559, -59.31773432185592299 ) ) ;
#45231=CARTESIAN_POINT ( 'NONE',  ( -51.76085035121451483, 41.99999999999999289, -29.83308852628634966 ) ) ;
#45250=CARTESIAN_POINT ( 'NONE',  ( 1.517883041479706208E-15, -5.000000000000000888, -97.00000000000000000 ) ) ;
#45276=CARTESIAN_POINT ( 'NONE',  ( 9.891797161801495264, -5.000000000000002665, -73.72381496649794030 ) ) ;
#45304=SURFACE_STYLE_USAGE ( .BOTH. , #20552 ) ;
#45321=CARTESIAN_POINT ( 'NONE',  ( -9.117185603063706623, -4.332661967064742825, -15.39580070564181469 ) ) ;
#45359=CARTESIAN_POINT ( 'NONE',  ( -5.268008033849937100, 13.26688624804745587, -33.14867888032319598 ) ) ;
#45369=CARTESIAN_POINT ( 'NONE',  ( -19.01480799866954285, 49.53976911447221454, 61.88728409518844131 ) ) ;
#45371=CARTESIAN_POINT ( 'NONE',  ( 5.569582024719362146, 40.00000000167852932, -71.04463995182341307 ) ) ;
#45386=CARTESIAN_POINT ( 'NONE',  ( 5.134970455931373579, -1.158234108193381795, -20.02603949707692266 ) ) ;
#45392=CARTESIAN_POINT ( 'NONE',  ( -5.036189802309414709, -5.000000000000015099, -93.73786388411730286 ) ) ;
#45405=SURFACE_SIDE_STYLE ('',( #77763 ) ) ;
#45423=CARTESIAN_POINT ( 'NONE',  ( 10.00012749751951802, -5.000000000000000000, -1.308371270547806553 ) ) ;
#45446=CARTESIAN_POINT ( 'NONE',  ( 39.15195563986023330, 42.02328961493514470, -56.67495990243617143 ) ) ;
#45457=CARTESIAN_POINT ( 'NONE',  ( 23.57730434126663255, 18.64316884711714906, 30.67950393662606245 ) ) ;
#45466=CARTESIAN_POINT ( 'NONE',  ( 62.84406313655870946, 39.42568531683917143, -16.86755852376854037 ) ) ;
#45476=CARTESIAN_POINT ( 'NONE',  ( 8.087340429040205336, 41.99999999999999289, -69.98180430517568595 ) ) ;
#45488=CARTESIAN_POINT ( 'NONE',  ( 6.043427762770655853, 50.00000000000000000, -74.51456333905269958 ) ) ;
#45513=CARTESIAN_POINT ( 'NONE',  ( -6.035608738543801088, 41.34018720349636311, -70.92167698604198733 ) ) ;
#45525=CARTESIAN_POINT ( 'NONE',  ( -17.98225906059938239, 44.99999999999999289, 62.57939804496447067 ) ) ;
#45558=CARTESIAN_POINT ( 'NONE',  ( 11.71448656990683723, -4.888164313292308272, -12.55940474970822329 ) ) ;
#45563=FACE_OUTER_BOUND ( 'NONE', #104163, .T. ) ;
#45573=CARTESIAN_POINT ( 'NONE',  ( -5.774137037018697960, 50.00000000000000000, 63.00000000000000000 ) ) ;
#45578=CARTESIAN_POINT ( 'NONE',  ( -6.359250320826728142, 41.88719959362819623, -59.22188769180981893 ) ) ;
#45588=CARTESIAN_POINT ( 'NONE',  ( 19.06777080879943398, 50.00000000000000000, 60.49338507843820878 ) ) ;
#45590=EDGE_CURVE ( 'NONE', #90268, #712, #25398, .T. ) ;
#45600=CARTESIAN_POINT ( 'NONE',  ( 62.81518281356948563, 50.00000000000000711, -4.977348761394969401 ) ) ;
#45613=CARTESIAN_POINT ( 'NONE',  ( 6.214520401345230205, 41.72339003054456441, -70.49303489710376880 ) ) ;
#45623=VERTEX_POINT ( 'NONE', #75818 ) ;
#45630=CARTESIAN_POINT ( 'NONE',  ( 18.91791044776121211, 47.99999999999999289, 62.18611311450882795 ) ) ;
#45679=CARTESIAN_POINT ( 'NONE',  ( -6.924711584187146940, 40.92328497002484511, -70.90711766174086961 ) ) ;
#45686=CARTESIAN_POINT ( 'NONE',  ( -31.48004745648652758, 41.29390966982543176, -67.22208989512388655 ) ) ;
#45703=VERTEX_POINT ( 'NONE', #35399 ) ;
#45720=CARTESIAN_POINT ( 'NONE',  ( -6.746993971545061974, 41.86978750136238858, -69.53909815634938241 ) ) ;
#45724=CARTESIAN_POINT ( 'NONE',  ( -8.012318136523624901, -5.000000000000000000, 14.34023295164496403 ) ) ;
#45725=CARTESIAN_POINT ( 'NONE',  ( -6.315604073028507237, 41.49696650568338896, -58.51869299239607614 ) ) ;
#45745=CARTESIAN_POINT ( 'NONE',  ( 6.566498343660657433, 41.80386961834008730, -59.12741152495549102 ) ) ;
#45747=CARTESIAN_POINT ( 'NONE',  ( 15.50526908265481296, 41.99999999991779731, -57.69562748401063601 ) ) ;
#45752=ORIENTED_EDGE ( 'NONE', *, *, #61667, .F. ) ;
#45778=FACE_OUTER_BOUND ( 'NONE', #1066, .T. ) ;
#45835=CARTESIAN_POINT ( 'NONE',  ( -7.305752995881348966, 41.99999999999663913, -58.79284008965307606 ) ) ;
#45846=CARTESIAN_POINT ( 'NONE',  ( -16.28378713909053843, -4.332661967060385422, -8.128475758626676040 ) ) ;
#45860=ORIENTED_EDGE ( 'NONE', *, *, #7287, .F. ) ;
#45866=CARTESIAN_POINT ( 'NONE',  ( 19.36342679109174370, 49.91170501117324676, 61.12863474974990652 ) ) ;
#45877=UNCERTAINTY_MEASURE_WITH_UNIT (LENGTH_MEASURE( 1.000000000000000082E-05 ), #60632, 'distance_accuracy_value', 'NONE');
#45892=CARTESIAN_POINT ( 'NONE',  ( -18.93028278895031136, 49.10155414044731970, 62.09492669842853729 ) ) ;
#45895=AXIS2_PLACEMENT_3D ( 'NONE', #106135, #83472, #48961 ) ;
#45896=CARTESIAN_POINT ( 'NONE',  ( 6.060122754898491948, 40.55658532241655223, -71.16215414250133620 ) ) ;
#45899=FILL_AREA_STYLE_COLOUR ( '', #53836 ) ;
#45911=CARTESIAN_POINT ( 'NONE',  ( 5.223130590452879751, 7.187516661514774974, -27.63920076787009350 ) ) ;
#45912=CARTESIAN_POINT ( 'NONE',  ( 12.34835181856063002, -4.332967528434596538, -12.86601580078908214 ) ) ;
#45913=CARTESIAN_POINT ( 'NONE',  ( -4.028951842967194885, -3.000000000000000444, -6.990291106834064294 ) ) ;
#45915=CARTESIAN_POINT ( 'NONE',  ( 0.000000000000000000, -5.000000000000002665, -75.00000000000001421 ) ) ;
#45942=CARTESIAN_POINT ( 'NONE',  ( 5.062179317057940331, -5.000000000000000000, -8.716351559230457013 ) ) ;
#45959=CARTESIAN_POINT ( 'NONE',  ( -42.34743190980356076, 39.51742533357018772, -49.83185399579645036 ) ) ;
#45971=CARTESIAN_POINT ( 'NONE',  ( 34.62244506083275297, 42.65563576728210649, -62.90200742928525557 ) ) ;
#45982=CARTESIAN_POINT ( 'NONE',  ( 36.40416150948652785, 42.00000000008225953, 47.37019975542485639 ) ) ;
#45989=CARTESIAN_POINT ( 'NONE',  ( 61.99214259692967488, 39.42505830967482439, -19.76944376150414939 ) ) ;
#46008=CARTESIAN_POINT ( 'NONE',  ( 2.617478844992369158, 49.99999999999999289, -75.26027323389158141 ) ) ;
#46020=CARTESIAN_POINT ( 'NONE',  ( 9.455047728417365960, -5.000000000000000000, -19.27141366270301504 ) ) ;
#46024=FILL_AREA_STYLE ('',( #5033 ) ) ;
#46034=CARTESIAN_POINT ( 'NONE',  ( -6.654387163495472990, 41.27136526523243987, -70.82047234851677331 ) ) ;
#46056=CARTESIAN_POINT ( 'NONE',  ( -12.50000000000000533, 27.18014154145715011, -44.71980230305747028 ) ) ;
#46066=CARTESIAN_POINT ( 'NONE',  ( 7.302671812080789415, 41.33023047990123899, -59.14964464841043679 ) ) ;
#46074=CARTESIAN_POINT ( 'NONE',  ( 5.168696396656956793, 1.295298111819218168, -22.28139744604624184 ) ) ;
#46085=CARTESIAN_POINT ( 'NONE',  ( 5.500000000000007105, 42.00000000000000000, -65.90297133634214788 ) ) ;
#46088=CARTESIAN_POINT ( 'NONE',  ( -17.59386865947600143, -4.333298119783918878, 3.400962272289256294 ) ) ;
#46098=CARTESIAN_POINT ( 'NONE',  ( -52.56483885390515809, 48.00000000000000000, -38.23529411764715036 ) ) ;
#46104=CARTESIAN_POINT ( 'NONE',  ( -6.777274421432666784, 41.87254869799794932, -59.70743268153353256 ) ) ;
#46106=( BOUNDED_CURVE ( )  B_SPLINE_CURVE ( 2, ( #48484, #82461, #33403 ),
 .UNSPECIFIED., .F., .F. ) 
 B_SPLINE_CURVE_WITH_KNOTS ( ( 3, 3 ),
 ( 0.000000000000000000, 1.000000000000000000 ),
 .UNSPECIFIED. ) 
 CURVE ( )  GEOMETRIC_REPRESENTATION_ITEM ( )  RATIONAL_B_SPLINE_CURVE ( ( 1.000000000000000000, 1.857142857142858317, 1.000000000000000000 ) ) 
 REPRESENTATION_ITEM ( '' )  );
#46176=CARTESIAN_POINT ( 'NONE',  ( 1.224646799147352665E-15, 48.00000000000000000, -75.00000000000001421 ) ) ;
#46210=EDGE_CURVE ( 'NONE', #14419, #55315, #69482, .T. ) ;
#46254=CARTESIAN_POINT ( 'NONE',  ( 1.724765290415787300, -3.000000000000002665, -69.73714729959421277 ) ) ;
#46255=CARTESIAN_POINT ( 'NONE',  ( -5.308064226573042887, 41.67430808342687243, -70.56675994572434263 ) ) ;
#46261=CARTESIAN_POINT ( 'NONE',  ( -5.896196268914855487, 41.78011476317043815, -58.83937604779054453 ) ) ;
#46280=CARTESIAN_POINT ( 'NONE',  ( 5.767822811355441281, 42.00032026584280231, -59.73203674101891636 ) ) ;
#46281=CARTESIAN_POINT ( 'NONE',  ( -37.36680950586716676, 18.64316884709021238, -10.04205104292877770 ) ) ;
#46295=PLANE ( 'NONE',  #81043 ) ;
#46308=CARTESIAN_POINT ( 'NONE',  ( 14.75116209840774495, 43.55504285524111907, -90.22050492864485705 ) ) ;
#46328=CARTESIAN_POINT ( 'NONE',  ( 2.384812152908761806, -5.000000000000002665, -98.00000000000000000 ) ) ;
#46329=CARTESIAN_POINT ( 'NONE',  ( 16.50306599534081187, -4.333298119783718150, -6.982805420311324340 ) ) ;
#46352=VECTOR ( 'NONE', #97539, 1000.000000000000114 ) ;
#46412=ORIENTED_EDGE ( 'NONE', *, *, #69720, .T. ) ;
#46422=CARTESIAN_POINT ( 'NONE',  ( -19.50010530980351220, 50.00000000000000000, 59.90637122617393828 ) ) ;
#46428=CARTESIAN_POINT ( 'NONE',  ( 12.50000000000000000, -3.000000000000000000, -8.595933841506987250 ) ) ;
#46431=VERTEX_POINT ( 'NONE', #34361 ) ;
#46437=CARTESIAN_POINT ( 'NONE',  ( 5.293610867670049736, 18.51054415109676654, -37.87873510570408087 ) ) ;
#46439=CARTESIAN_POINT ( 'NONE',  ( -50.94745919686192082, 50.00000000000000000, -37.05882352941185331 ) ) ;
#46442=CARTESIAN_POINT ( 'NONE',  ( 2.617478844990903664, -3.000000000000002665, -94.73972676610405586 ) ) ;
#46456=CARTESIAN_POINT ( 'NONE',  ( -34.37606913705030820, 42.68840706779676708, -63.24071832532951731 ) ) ;
#46476=CARTESIAN_POINT ( 'NONE',  ( -7.230783165911326194, -2.999999999999882760, -70.90935356276069967 ) ) ;
#46485=CARTESIAN_POINT ( 'NONE',  ( -45.44351312664282716, 39.21094759328430257, -45.67963897325379463 ) ) ;
#46493=CARTESIAN_POINT ( 'NONE',  ( 46.38169941325361378, 41.13208785335375239, -46.73570547342293935 ) ) ;
#46502=CARTESIAN_POINT ( 'NONE',  ( -1.233923992984923027E-14, 18.64316884711714195, -38.36535705883633085 ) ) ;
#46507=CARTESIAN_POINT ( 'NONE',  ( -14.79725422420208858, 39.42585232341617996, 63.36302458054748854 ) ) ;
#46526=CARTESIAN_POINT ( 'NONE',  ( -6.145467200824003662, 48.00000000000000000, -77.00333157709306420 ) ) ;
#46532=ORIENTED_EDGE ( 'NONE', *, *, #24131, .F. ) ;
#46534=FILL_AREA_STYLE_COLOUR ( '', #5917 ) ;
#46542=CARTESIAN_POINT ( 'NONE',  ( 8.743816783185534902, -5.000000000000000888, -16.78777973705476612 ) ) ;
#46558=ORIENTED_EDGE ( 'NONE', *, *, #43901, .F. ) ;
#46581=COLOUR_RGB ( '', 0.31764706, 0.68627451, 0.89019608) ;
#46584=CARTESIAN_POINT ( 'NONE',  ( 7.217786572945549040, 41.17942765912351177, -58.69595075570492071 ) ) ;
#46591=CARTESIAN_POINT ( 'NONE',  ( 7.500000000000001776, 9.462792962020666110, -29.31754814678773968 ) ) ;
#46617=CARTESIAN_POINT ( 'NONE',  ( -65.26738680893376454, 49.99999999999999289, 0.8120011905356555593 ) ) ;
#46629=CARTESIAN_POINT ( 'NONE',  ( 18.47404693474707571, 50.00000000000000711, 61.29115758976740835 ) ) ;
#46637=CARTESIAN_POINT ( 'NONE',  ( 1.899844911462918340, 42.00000000000000000, -68.00818075325166490 ) ) ;
#46639=CARTESIAN_POINT ( 'NONE',  ( 58.66297648405128484, 49.99999999999999289, -23.00451178233782557 ) ) ;
#46649=CARTESIAN_POINT ( 'NONE',  ( 7.150000000000015454, 41.65000000000000568, -68.91429206202192859 ) ) ;
#46652=LINE ( 'NONE', #79552, #42185 ) ;
#46667=CARTESIAN_POINT ( 'NONE',  ( 7.491624566500244775, 40.33173439531471161, -59.48415712631144459 ) ) ;
#46692=ORIENTED_EDGE ( 'NONE', *, *, #85794, .T. ) ;
#46699=B_SPLINE_CURVE_WITH_KNOTS ( 'NONE', 3,
 ( #62381, #30019, #22988, #5195, #73075, #88238, #96861, #95274 ),
 .UNSPECIFIED., .F., .F.,
 ( 4, 2, 2, 4 ),
 ( 0.000000000000000000, 0.2500000000000000000, 0.5000000000000000000, 1.000000000000000000 ),
 .UNSPECIFIED. ) ;
#46702=EDGE_LOOP ( 'NONE', ( #77207, #28121, #50577, #97798 ) ) ;
#46710=( LENGTH_UNIT ( ) NAMED_UNIT ( * ) SI_UNIT ( .MILLI., .METRE. ) );
#46717=CARTESIAN_POINT ( 'NONE',  ( 7.137815226409024660, -5.000000000001136868, -4.175893272573466319 ) ) ;
#46720=CARTESIAN_POINT ( 'NONE',  ( -5.220566466144580531, 6.884671715754390853, -27.36422395346735215 ) ) ;
#46722=SURFACE_STYLE_FILL_AREA ( #80142 ) ;
#46730=ADVANCED_FACE ( 'NONE', ( #44288 ), #24076, .T. ) ;
#46736=EDGE_CURVE ( 'NONE', #32960, #11528, #31680, .T. ) ;
#46737=CARTESIAN_POINT ( 'NONE',  ( -20.94717588032531452, 41.83711825373250548, -78.41832805012246865 ) ) ;
#46738=CARTESIAN_POINT ( 'NONE',  ( -17.60890209088405456, 50.00000000000000000, 62.65190115956760764 ) ) ;
#46746=CARTESIAN_POINT ( 'NONE',  ( 17.50000000000023803, 50.00318699355108976, 59.98279283212327329 ) ) ;
#46764=CARTESIAN_POINT ( 'NONE',  ( 6.921856739985489781, 41.59435684990518922, -70.13580383465753698 ) ) ;
#46801=CARTESIAN_POINT ( 'NONE',  ( -50.94745919686192082, 50.00000000000000000, -37.05882352941185331 ) ) ;
#46823=CARTESIAN_POINT ( 'NONE',  ( 0.000000000000000000, 0.000000000000000000, 0.000000000000000000 ) ) ;
#46834=CARTESIAN_POINT ( 'NONE',  ( -13.87686815719945166, 43.16530573668475057, -91.42246037821334426 ) ) ;
#46849=EDGE_CURVE ( 'NONE', #84646, #82792, #105169, .T. ) ;
#46856=FILL_AREA_STYLE ('',( #104025 ) ) ;
#46914=CARTESIAN_POINT ( 'NONE',  ( -9.797174393178825657E-16, -3.000000000000000000, 8.000000000000000000 ) ) ;
#46935=FILL_AREA_STYLE ('',( #85843 ) ) ;
#46940=( LENGTH_UNIT ( ) NAMED_UNIT ( * ) SI_UNIT ( .MILLI., .METRE. ) );
#46956=CARTESIAN_POINT ( 'NONE',  ( 8.737863884125493641, -3.000000000000002665, -79.96381019769830800 ) ) ;
#46960=ORIENTED_EDGE ( 'NONE', *, *, #60902, .T. ) ;
#46967=CARTESIAN_POINT ( 'NONE',  ( 7.597212443344973032, -5.000000000004688694, -19.53267873632396956 ) ) ;
#46969=CARTESIAN_POINT ( 'NONE',  ( -11.69538631874992340, 50.00000000000001421, -81.87730495799611674 ) ) ;
#46984=CARTESIAN_POINT ( 'NONE',  ( -6.784953749642196996, 41.67963440881483450, -59.00226708758491156 ) ) ;
#46995=MECHANICAL_DESIGN_GEOMETRIC_PRESENTATION_REPRESENTATION('',(#22871),#105519);
#46999=CARTESIAN_POINT ( 'NONE',  ( -43.29564266603537703, 39.41494058703111847, -48.56300739893791985 ) ) ;
#47009=CARTESIAN_POINT ( 'NONE',  ( 44.27062040774965368, 41.35340516790330412, -49.63795927564910926 ) ) ;
#47023=CARTESIAN_POINT ( 'NONE',  ( -51.64426891978533973, 39.42569251748471260, 39.58139286548590263 ) ) ;
#47031=B_SPLINE_CURVE_WITH_KNOTS ( 'NONE', 3,
 ( #34344, #42932, #34871, #41326 ),
 .UNSPECIFIED., .F., .F.,
 ( 4, 4 ),
 ( 0.000000000000000000, 1.000000000000000000 ),
 .UNSPECIFIED. ) ;
#47043=CARTESIAN_POINT ( 'NONE',  ( -2.617478844990583031, 48.00000000000000000, -75.26027323389584467 ) ) ;
#47045=CARTESIAN_POINT ( 'NONE',  ( 0.000000000000000000, 42.00000000000000000, -56.99999999999999289 ) ) ;
#47057=CARTESIAN_POINT ( 'NONE',  ( 5.933868275853403595, -5.000000000000000000, -15.37667404185483910 ) ) ;
#47060=CARTESIAN_POINT ( 'NONE',  ( -4.852941176470586093, 40.00000000000132871, -70.80672828634229177 ) ) ;
#47075=CARTESIAN_POINT ( 'NONE',  ( 1.262844703064978993E-15, -3.000000000000002665, -95.00000000000000000 ) ) ;
#47092=CARTESIAN_POINT ( 'NONE',  ( -12.50000000000001066, 39.67068617188025570, -64.72045672135165262 ) ) ;
#47098=EDGE_LOOP ( 'NONE', ( #26410, #20996, #25617, #22563, #31533 ) ) ;
#47135=ADVANCED_FACE ( 'NONE', ( #25342, #91130, #65773 ), #17240, .F. ) ;
#47138=CARTESIAN_POINT ( 'NONE',  ( 54.34415824577756382, 50.00000000000000000, -32.38913437803500983 ) ) ;
#47163=ORIENTED_EDGE ( 'NONE', *, *, #86147, .T. ) ;
#47170=CARTESIAN_POINT ( 'NONE',  ( 6.075691126275640563, 41.99394904787047977, -68.91429206828460963 ) ) ;
#47187=CARTESIAN_POINT ( 'NONE',  ( 7.500000000000009770, 40.18760374782148403, -59.65697284672557998 ) ) ;
#47188=( GEOMETRIC_REPRESENTATION_CONTEXT ( 3 ) GLOBAL_UNCERTAINTY_ASSIGNED_CONTEXT ( ( #55604 ) ) GLOBAL_UNIT_ASSIGNED_CONTEXT ( ( #29536, #39194, #80681 ) ) REPRESENTATION_CONTEXT ( 'NONE', 'WORKASPACE' ) );
#47189=CARTESIAN_POINT ( 'NONE',  ( -4.651132217449170270, -5.000000000000000000, -15.66661053588738106 ) ) ;
#47216=CARTESIAN_POINT ( 'NONE',  ( -10.51296777078104050, 50.00000000000000000, -92.64705882352942012 ) ) ;
#47236=CARTESIAN_POINT ( 'NONE',  ( 0.000000000000000000, -3.000000000000000000, 8.000000000000000000 ) ) ;
#47239=B_SPLINE_CURVE_WITH_KNOTS ( 'NONE', 3,
 ( #84868, #27199, #84336, #58468, #60089, #35281, #11488, #92955, #83788, #99978, #93505, #34220, #91375, #10432, #35825, #83265 ),
 .UNSPECIFIED., .F., .F.,
 ( 4, 2, 2, 1, 2, 2, 1, 2, 4 ),
 ( 0.000000000000000000, 0.2499999999999694134, 0.3749999999999552025, 0.3906249999999557576, 0.3984374999999557576, 0.4062499999999557576, 0.4374999999999586997, 0.4999999999999641398, 1.000000000000000000 ),
 .UNSPECIFIED. ) ;
#47255=CARTESIAN_POINT ( 'NONE',  ( -31.55411806780566408, 43.06427826655156110, -67.12025964001210809 ) ) ;
#47256=CARTESIAN_POINT ( 'NONE',  ( -17.52057716778178786, 49.99999999999999289, 63.21064094274808554 ) ) ;
#47273=PRESENTATION_STYLE_ASSIGNMENT (( #20947 ) ) ;
#47296=CARTESIAN_POINT ( 'NONE',  ( -1.724765290415802621, -3.000000000000002665, -69.73714729959421277 ) ) ;
#47322=CARTESIAN_POINT ( 'NONE',  ( 6.275175096193794211, 41.94081482539142058, -59.38054156036670861 ) ) ;
#47329=ORIENTED_EDGE ( 'NONE', *, *, #15608, .F. ) ;
#47347=CARTESIAN_POINT ( 'NONE',  ( -52.56483885390523625, 40.83906611473335602, -38.23529411764706509 ) ) ;
#47379=CARTESIAN_POINT ( 'NONE',  ( -7.137815226409945701, -4.999999999999998224, 4.175893272574815462 ) ) ;
#47424=CARTESIAN_POINT ( 'NONE',  ( -62.06337123375774212, 48.00000000000000711, -19.99347512944444816 ) ) ;
#47432=ORIENTED_EDGE ( 'NONE', *, *, #8767, .F. ) ;
#47438=CARTESIAN_POINT ( 'NONE',  ( 19.06872869572427120, 49.63275118039182843, 61.79276190149701620 ) ) ;
#47467=CARTESIAN_POINT ( 'NONE',  ( 10.50000000000000000, -5.000000000000000000, -9.904958390907863119 ) ) ;
#47484=CARTESIAN_POINT ( 'NONE',  ( 8.737863884121400915, -4.999999999998638422, -90.03618980231146907 ) ) ;
#47497=CARTESIAN_POINT ( 'NONE',  ( 7.347171990167045585, -3.439186728100360302, -18.43985286355972875 ) ) ;
#47514=CARTESIAN_POINT ( 'NONE',  ( -6.943035977205679110, 41.50417750172036335, -58.81491712266881677 ) ) ;
#47522=CARTESIAN_POINT ( 'NONE',  ( -5.902907888919634694, -5.000000000000001776, -73.20788160634965891 ) ) ;
#47530=CARTESIAN_POINT ( 'NONE',  ( 6.738100180926640093, 41.71798714554645215, -59.05424661244425266 ) ) ;
#47537=CARTESIAN_POINT ( 'NONE',  ( -9.739726766101606259, -5.000000000000002665, -82.38252115500968387 ) ) ;
#47555=CARTESIAN_POINT ( 'NONE',  ( -39.07677920758315793, 39.42618461990478096, 52.28553321386016250 ) ) ;
#47574=CARTESIAN_POINT ( 'NONE',  ( -9.999999999999992895, 48.00000000000000000, -86.30899693747680601 ) ) ;
#47583=DIRECTION ( 'NONE',  ( 0.000000000000000000, 1.000000000000000000, 0.000000000000000000 ) ) ;
#47586=CARTESIAN_POINT ( 'NONE',  ( 7.424909431085690237, -5.000000000000000888, -15.55223105906578240 ) ) ;
#47599=CARTESIAN_POINT ( 'NONE',  ( -5.209797429415269576, 40.00000000002213341, -70.92874401597350698 ) ) ;
#47601=ORIENTED_EDGE ( 'NONE', *, *, #166, .F. ) ;
#47629=CARTESIAN_POINT ( 'NONE',  ( 22.47385306464369492, 18.64284798592518655, -31.17447444073591356 ) ) ;
#47665=CARTESIAN_POINT ( 'NONE',  ( 50.18984356158254201, 50.00000000000000000, 38.51389699555568313 ) ) ;
#47676=CARTESIAN_POINT ( 'NONE',  ( 19.47229003637610489, 49.99999999999998579, 59.94434553428096990 ) ) ;
#47680=ADVANCED_FACE ( 'NONE', ( #100663 ), #51579, .T. ) ;
#47704=CARTESIAN_POINT ( 'NONE',  ( -7.149999999999890221, 41.65000000000012648, -59.82695526680724640 ) ) ;
#47705=MECHANICAL_DESIGN_GEOMETRIC_PRESENTATION_REPRESENTATION('',(#52878),#39119);
#47743=CARTESIAN_POINT ( 'NONE',  ( -39.08667504540946425, 49.99999999999999289, -56.76470588249692639 ) ) ;
#47758=CARTESIAN_POINT ( 'NONE',  ( 2.094395098902538166, -3.000000000000000000, -8.000000000000000000 ) ) ;
#47775=CARTESIAN_POINT ( 'NONE',  ( 6.641837668257387861, 41.74662779905570176, -59.04567176600482981 ) ) ;
#47786=CARTESIAN_POINT ( 'NONE',  ( 17.49999999999901235, 48.51938947814463177, 62.60970113050974817 ) ) ;
#47795=CARTESIAN_POINT ( 'NONE',  ( -5.538604458984424994, -4.999999999982783550, -16.33373421806852122 ) ) ;
#47796=CARTESIAN_POINT ( 'NONE',  ( -13.93041290236829965, 43.14806440719855374, -91.34884852387233423 ) ) ;
#47797=CARTESIAN_POINT ( 'NONE',  ( 7.320805580757752118, 41.41776788117373798, -59.82972163162600054 ) ) ;
#47817=CARTESIAN_POINT ( 'NONE',  ( -4.852941176470598528, -3.000000000000002665, -70.80672828634229177 ) ) ;
#47844=CARTESIAN_POINT ( 'NONE',  ( 5.711454417755754243, 41.98245396441496524, -59.41190390763706830 ) ) ;
#47874=CARTESIAN_POINT ( 'NONE',  ( 7.500000000000007105, -4.999999999999999112, -68.91429205785459544 ) ) ;
#47878=DIRECTION ( 'NONE',  ( 1.000000000000000000, 0.000000000000000000, 0.000000000000000000 ) ) ;
#47899=CARTESIAN_POINT ( 'NONE',  ( 4.175893272575727622, -4.999999999998865796, -7.137815226411304614 ) ) ;
#47903=CARTESIAN_POINT ( 'NONE',  ( 7.500000000000000888, -3.000671055698259870, -20.99923901233272971 ) ) ;
#47927=CARTESIAN_POINT ( 'NONE',  ( -8.162336134653097375, 41.33266196706049556, -58.07023218170494516 ) ) ;
#47947=CARTESIAN_POINT ( 'NONE',  ( -28.60676286294164328, 48.00000000000000711, 58.59397763554174077 ) ) ;
#47961=CARTESIAN_POINT ( 'NONE',  ( 19.17148997711927905, 49.74984135236479688, 61.61528624114195196 ) ) ;
#47967=( BOUNDED_CURVE ( )  B_SPLINE_CURVE ( 2, ( #88328, #105554, #41351 ),
 .UNSPECIFIED., .F., .F. ) 
 B_SPLINE_CURVE_WITH_KNOTS ( ( 3, 3 ),
 ( 0.000000000000000000, 1.000000000000000000 ),
 .UNSPECIFIED. ) 
 CURVE ( )  GEOMETRIC_REPRESENTATION_ITEM ( )  RATIONAL_B_SPLINE_CURVE ( ( 1.000000000000000000, 1.857142857142858317, 1.000000000000000000 ) ) 
 REPRESENTATION_ITEM ( '' )  );
#47978=CARTESIAN_POINT ( 'NONE',  ( 6.348226085585078948, 41.72645248587730293, -58.84140401153305788 ) ) ;
#47982=EDGE_LOOP ( 'NONE', ( #68397, #16869, #16187, #1419 ) ) ;
#47992=CARTESIAN_POINT ( 'NONE',  ( 12.49999999999999822, -4.999999999999999112, -34.12705337364891278 ) ) ;
#48009=FILL_AREA_STYLE_COLOUR ( '', #12327 ) ;
#48018=CARTESIAN_POINT ( 'NONE',  ( 8.044970079964597787, -4.999999999999987566, -15.82739658861712151 ) ) ;
#48021=CARTESIAN_POINT ( 'NONE',  ( -39.04193823264170504, 42.03880034757720097, -56.82620883133870393 ) ) ;
#48042=CARTESIAN_POINT ( 'NONE',  ( -8.990409435379676850, -5.000000000000000888, -71.93151781322266913 ) ) ;
#48049=AXIS2_PLACEMENT_3D ( 'NONE', #36856, #28774, #20695 ) ;
#48053=CARTESIAN_POINT ( 'NONE',  ( -42.99950361083188000, 39.44597763921156997, -48.95955523496266437 ) ) ;
#48062=CARTESIAN_POINT ( 'NONE',  ( 9.999999999999996447, -5.000000000000002665, -83.69100306251233690 ) ) ;
#48073=CARTESIAN_POINT ( 'NONE',  ( -12.51707952085838471, -5.000000000000000000, -88.70144047758928707 ) ) ;
#48115=CARTESIAN_POINT ( 'NONE',  ( 7.441633456671346458, -4.999999999999998224, -15.55954248125250139 ) ) ;
#48141=CARTESIAN_POINT ( 'NONE',  ( 7.442703790580194934, 40.98154234363288140, -69.28862639872464513 ) ) ;
#48150=CARTESIAN_POINT ( 'NONE',  ( -60.68810323480906987, 50.00000000000000711, 17.09759988054065261 ) ) ;
#48182=B_SPLINE_CURVE_WITH_KNOTS ( 'NONE', 3,
 ( #70717, #13519, #35729, #20632, #37321, #101492, #60521, #61582, #19556, #44317, #36270, #86392, #53472, #12459, #45913, #78269, #4381, #103089 ),
 .UNSPECIFIED., .F., .F.,
 ( 4, 2, 2, 2, 2, 2, 2, 2, 4 ),
 ( 0.000000000000000000, 0.06250000000000000000, 0.1250000000000000000, 0.1875000000000000000, 0.2500000000000000000, 0.3125000000000000000, 0.3750000000000000000, 0.4375000000000000000, 0.5000000000000000000 ),
 .UNSPECIFIED. ) ;
#48195=CARTESIAN_POINT ( 'NONE',  ( -57.09426686934756390, 50.00000000000000000, -27.25041924766811618 ) ) ;
#48241=SURFACE_STYLE_FILL_AREA ( #64971 ) ;
#48245=CARTESIAN_POINT ( 'NONE',  ( 5.500000036871884213, 42.00000000000000000, -68.91429207046176941 ) ) ;
#48261=SURFACE_STYLE_USAGE ( .BOTH. , #106501 ) ;
#48273=CARTESIAN_POINT ( 'NONE',  ( -12.13034742782427955, 48.00000000000000000, -93.82352941176471006 ) ) ;
#48281=( BOUNDED_SURFACE ( )  B_SPLINE_SURFACE ( 2, 3, ( 
 ( #55357, #72088, #39214, #104995, #106030, #48330, #89870, #73669, #277, #66119, #80699, #55872 ),
 ( #81222, #48855, #64541, #73125, #6817, #7870, #74200, #57477, #90403, #25163, #58015, #23568 ),
 ( #72614, #33247, #32722, #98997, #31658, #90943, #15439, #65059, #56950, #40775, #16505, #31139 ),
 ( #15976, #17053, #65592, #7341, #49391, #82300, #89349, #49930, #40250, #32175, #47795, #56415 ),
 ( #97956, #24105, #106572, #98478, #6274, #41311, #24630, #39736, #105517, #81747, #8410, #64026 ),
 ( #96903, #23037, #97408, #88809, #14900, #51525, #10008, #26245, #43452, #83363, #9462, #27312 ),
 ( #19227, #43979, #25717, #50452, #42373, #91476, #59109, #58576, #812, #76329, #68258, #76866 ) ),
 .UNSPECIFIED., .F., .F., .F. ) 
 B_SPLINE_SURFACE_WITH_KNOTS ( ( 3, 2, 2, 3 ),
 ( 4, 2, 2, 2, 2, 4 ),
 ( -0.01000000000000000021, 0.000000000000000000, 1.000000000000000000, 1.010000000000000009 ),
 ( 0.000000000000000000, 0.001801747411056191499, 0.003603494822112382999, 0.005405242233168574065, 0.006306115938696670031, 0.007206989644224765998 ),
 .UNSPECIFIED. ) 
 GEOMETRIC_REPRESENTATION_ITEM ( )  RATIONAL_B_SPLINE_SURFACE ( (
 ( 1.000000000000000000, 1.000000000000000000, 1.000000000000000000, 1.000000000000000000, 1.000000000000000000, 1.000000000000000000, 1.000000000000000000, 1.000000000000000000, 1.000000000000000000, 1.000000000000000000, 1.000000000000000000, 1.000000000000000000),
 ( 1.000000000000000000, 1.000000000000000000, 1.000000000000000000, 1.000000000000000000, 1.000000000000000000, 1.000000000000000000, 1.000000000000000000, 1.000000000000000000, 1.000000000000000000, 1.000000000000000000, 1.000000000000000000, 1.000000000000000000),
 ( 1.000000000000000000, 1.000000000000000000, 1.000000000000000000, 1.000000000000000000, 1.000000000000000000, 1.000000000000000000, 1.000000000000000000, 1.000000000000000000, 1.000000000000000000, 1.000000000000000000, 1.000000000000000000, 1.000000000000000000),
 ( 1.857142857142858317, 1.857142857142858317, 1.857142857142858317, 1.857142857142858317, 1.857142857142858317, 1.857142857142858317, 1.857142857142858317, 1.857142857142858317, 1.857142857142858317, 1.857142857142858317, 1.857142857142858317, 1.857142857142858317),
 ( 1.000000000000000000, 1.000000000000000000, 1.000000000000000000, 1.000000000000000000, 1.000000000000000000, 1.000000000000000000, 1.000000000000000000, 1.000000000000000000, 1.000000000000000000, 1.000000000000000000, 1.000000000000000000, 1.000000000000000000),
 ( 1.000000000000000000, 1.000000000000000000, 1.000000000000000000, 1.000000000000000000, 1.000000000000000000, 1.000000000000000000, 1.000000000000000000, 1.000000000000000000, 1.000000000000000000, 1.000000000000000000, 1.000000000000000000, 1.000000000000000000),
 ( 1.000000000000000000, 1.000000000000000000, 1.000000000000000000, 1.000000000000000000, 1.000000000000000000, 1.000000000000000000, 1.000000000000000000, 1.000000000000000000, 1.000000000000000000, 1.000000000000000000, 1.000000000000000000, 1.000000000000000000) ) ) 
 REPRESENTATION_ITEM ( '' )  SURFACE ( )  );
#48291=CARTESIAN_POINT ( 'NONE',  ( 0.000000000000000000, -5.000000000000000000, 10.00000000000000000 ) ) ;
#48298=VERTEX_POINT ( 'NONE', #5560 ) ;
#48318=ORIENTED_EDGE ( 'NONE', *, *, #20675, .T. ) ;
#48319=CARTESIAN_POINT ( 'NONE',  ( 17.49999999999998934, 49.46308821774509568, 63.99046601234773135 ) ) ;
#48327=STYLED_ITEM ( 'NONE', ( #16687 ), #47135 ) ;
#48330=CARTESIAN_POINT ( 'NONE',  ( -7.084012698788995976, -4.012402067415701268, -17.39015006382141237 ) ) ;
#48355=CARTESIAN_POINT ( 'NONE',  ( -64.91565662648044110, 48.00000000000000000, 6.815324757466639127 ) ) ;
#48381=CARTESIAN_POINT ( 'NONE',  ( 5.668940197363838251, 41.88723871811491506, -59.02759513106027356 ) ) ;
#48391=CARTESIAN_POINT ( 'NONE',  ( -1.833333333403031284, 42.00000000000000000, -60.21711271837360613 ) ) ;
#48392=CARTESIAN_POINT ( 'NONE',  ( -5.625019081819782052, 41.66287055468434630, -70.61600276915974916 ) ) ;
#48432=EDGE_CURVE ( 'NONE', #80162, #100984, #103480, .T. ) ;
#48436=CARTESIAN_POINT ( 'NONE',  ( 2.094395098902661179, -4.999999999999998224, 8.000000000000000000 ) ) ;
#48454=COLOUR_RGB ( '', 0.08235294, 0.09019608, 0.10196078) ;
#48483=DIRECTION ( 'NONE',  ( 0.000000000000000000, 0.7456561006171790185, 0.6663309835302448914 ) ) ;
#48484=CARTESIAN_POINT ( 'NONE',  ( 1.469576158976823356E-15, 50.00000000000000000, -73.00000000000001421 ) ) ;
#48510=CARTESIAN_POINT ( 'NONE',  ( 6.828042838857774299, 41.63841260098274688, -58.95291818684747653 ) ) ;
#48514=COLOUR_RGB ( '', 0.08235294, 0.09019608, 0.10196078) ;
#48535=CARTESIAN_POINT ( 'NONE',  ( -5.909135300144294334, -5.000000000000000000, -15.35560945501324248 ) ) ;
#48539=CARTESIAN_POINT ( 'NONE',  ( 8.000000000000001776, -3.000000000000000444, -1.047197551196596965 ) ) ;
#48554=CARTESIAN_POINT ( 'NONE',  ( 7.464071982068412936, -3.053493056030892383, -19.53076229013005261 ) ) ;
#48570=CARTESIAN_POINT ( 'NONE',  ( -17.49999999999997513, 49.99999999999970157, 59.56761335716139882 ) ) ;
#48583=CARTESIAN_POINT ( 'NONE',  ( 25.60851123651792705, 48.00000000000000000, -75.29411764705884025 ) ) ;
#48584=CARTESIAN_POINT ( 'NONE',  ( -24.00311689919816160, 41.61929283342283981, -74.30204191058474805 ) ) ;
#48590=CARTESIAN_POINT ( 'NONE',  ( 0.000000000000000000, -5.000000000000002665, -75.00000000000001421 ) ) ;
#48594=CARTESIAN_POINT ( 'NONE',  ( 4.852941176470593199, -5.250000000000004441, -70.80672828634229177 ) ) ;
#48599=( BOUNDED_CURVE ( )  B_SPLINE_CURVE ( 2, ( #70868, #30426, #62268 ),
 .UNSPECIFIED., .F., .F. ) 
 B_SPLINE_CURVE_WITH_KNOTS ( ( 3, 3 ),
 ( 0.000000000000000000, 1.000000000000000000 ),
 .UNSPECIFIED. ) 
 CURVE ( )  GEOMETRIC_REPRESENTATION_ITEM ( )  RATIONAL_B_SPLINE_CURVE ( ( 1.000000000000000000, 1.857142857142858317, 1.000000000000000000 ) ) 
 REPRESENTATION_ITEM ( '' )  );
#48605=CARTESIAN_POINT ( 'NONE',  ( 5.782876476886952055, -5.000000000000000000, -96.70368651365731694 ) ) ;
#48611=ORIENTED_EDGE ( 'NONE', *, *, #37577, .F. ) ;
#48612=CARTESIAN_POINT ( 'NONE',  ( 2.911225856420454949, 38.95261502387059238, 63.66761955064095702 ) ) ;
#48628=CARTESIAN_POINT ( 'NONE',  ( -11.02516228146338229, -4.987106852743500518, -12.57633211456099787 ) ) ;
#48641=ORIENTED_EDGE ( 'NONE', *, *, #80036, .T. ) ;
#48645=CARTESIAN_POINT ( 'NONE',  ( -7.229692795438678488, 41.58551687973270816, -59.68506457723876935 ) ) ;
#48648=MECHANICAL_DESIGN_GEOMETRIC_PRESENTATION_REPRESENTATION('',(#100560),#2137);
#48653=CARTESIAN_POINT ( 'NONE',  ( -5.363597346089342466, 41.33266196706077267, -58.39526881795508473 ) ) ;
#48656=CARTESIAN_POINT ( 'NONE',  ( 9.432319653620828248, -4.999999999999999112, -70.68463330170209247 ) ) ;
#48674=CARTESIAN_POINT ( 'NONE',  ( -32.06611684416825625, 38.95383793066319100, 55.63518754859966720 ) ) ;
#48677=CARTESIAN_POINT ( 'NONE',  ( -56.29028211295952389, 50.00000000000000711, -28.72872561009205938 ) ) ;
#48681=MECHANICAL_DESIGN_GEOMETRIC_PRESENTATION_REPRESENTATION('',(#34954),#19423);
#48685=COLOUR_RGB ( '', 0.09019608, 0.27058824, 0.51372549) ;
#48688=CARTESIAN_POINT ( 'NONE',  ( 7.493944697689368439, 40.57567825174881904, -59.86116849737391021 ) ) ;
#48703=CARTESIAN_POINT ( 'NONE',  ( 12.13034742782427955, 41.99999999999999289, -93.82352941176471006 ) ) ;
#48706=CARTESIAN_POINT ( 'NONE',  ( 13.88435755492751511, 42.00000000000000000, -90.88030988993200765 ) ) ;
#48715=CARTESIAN_POINT ( 'NONE',  ( 6.516354785991091835E-11, 40.83842593836580903, 65.00000000086684793 ) ) ;
#48721=ORIENTED_EDGE ( 'NONE', *, *, #22608, .F. ) ;
#48726=CARTESIAN_POINT ( 'NONE',  ( -6.701893397842001221, 41.44328394191487774, -70.59544911652842814 ) ) ;
#48752=FILL_AREA_STYLE ('',( #15878 ) ) ;
#48757=CARTESIAN_POINT ( 'NONE',  ( -7.255115699379916627, 41.55406131346213527, -69.27528309631122738 ) ) ;
#48792=CARTESIAN_POINT ( 'NONE',  ( 12.50000000000000355, 27.29089671806294248, -44.83733606656386428 ) ) ;
#48806=CARTESIAN_POINT ( 'NONE',  ( 17.50000000000002842, 48.19572006404330722, 64.09945636913033695 ) ) ;
#48815=CARTESIAN_POINT ( 'NONE',  ( -4.175893272574848325, -4.999999999999998224, 7.137815226409911951 ) ) ;
#48845=CARTESIAN_POINT ( 'NONE',  ( 17.50000000000004974, 49.76444793455075200, 62.19248936617555046 ) ) ;
#48848=EDGE_CURVE ( 'NONE', #44820, #9732, #42961, .T. ) ;
#48855=CARTESIAN_POINT ( 'NONE',  ( -7.499143977330837707, -3.006661276316075604, -20.23006715386054566 ) ) ;
#48899=ORIENTED_EDGE ( 'NONE', *, *, #43163, .T. ) ;
#48903=CARTESIAN_POINT ( 'NONE',  ( 18.89111011270470541, 41.89281849971280280, -81.21350009779806101 ) ) ;
#48906=CARTESIAN_POINT ( 'NONE',  ( 19.32152200343512760, 18.64316884711617561, -33.52312678240317467 ) ) ;
#48914=CARTESIAN_POINT ( 'NONE',  ( 5.500000000000641265, 42.00000000000000000, -59.88032989331720302 ) ) ;
#48915=CARTESIAN_POINT ( 'NONE',  ( -6.757705282517541434, 41.35007050579768162, -70.67351639275690900 ) ) ;
#48957=CARTESIAN_POINT ( 'NONE',  ( -2.094395098902661179, -4.999999999999998224, 8.000000000000000000 ) ) ;
#48961=DIRECTION ( 'NONE',  ( 0.000000000000000000, 0.000000000000000000, 1.000000000000000000 ) ) ;
#48987=ORIENTED_EDGE ( 'NONE', *, *, #54026, .T. ) ;
#49040=CARTESIAN_POINT ( 'NONE',  ( 6.839476587632750793, 41.56703181668088831, -58.82533975359289968 ) ) ;
#49064=CARTESIAN_POINT ( 'NONE',  ( -7.279541227045297269, -4.999999999999999112, -15.48747486643692106 ) ) ;
#49079=CARTESIAN_POINT ( 'NONE',  ( 12.34835181856063002, -4.332967528434596538, -12.86601580078908214 ) ) ;
#49081=( NAMED_UNIT ( * ) SI_UNIT ( $, .STERADIAN. ) SOLID_ANGLE_UNIT ( ) );
#49090=COLOUR_RGB ( '', 0.66274510, 0.83137255, 0.94901961) ;
#49098=CARTESIAN_POINT ( 'NONE',  ( -17.49999999999490896, 48.96861188085171079, 62.56461476143485356 ) ) ;
#49102=CARTESIAN_POINT ( 'NONE',  ( -6.827804075699749120, -4.999999999995546673, -71.19745154229521233 ) ) ;
#49108=ORIENTED_EDGE ( 'NONE', *, *, #9403, .T. ) ;
#49117=CARTESIAN_POINT ( 'NONE',  ( 0.000000000000000000, -5.000000000000002665, -73.00000000000001421 ) ) ;
#49121=CARTESIAN_POINT ( 'NONE',  ( 4.852941176470593199, 9.833333333333344584, -70.80672828634229177 ) ) ;
#49129=B_SPLINE_CURVE_WITH_KNOTS ( 'NONE', 3,
 ( #66269, #9611, #99156, #58173 ),
 .UNSPECIFIED., .F., .F.,
 ( 4, 4 ),
 ( 0.000000000000000000, 1.000000000000000000 ),
 .UNSPECIFIED. ) ;
#49134=CARTESIAN_POINT ( 'NONE',  ( 8.732981572811874926, -5.000000000000000000, -94.70094745737053188 ) ) ;
#49150=SURFACE_SIDE_STYLE ('',( #16265 ) ) ;
#49177=CARTESIAN_POINT ( 'NONE',  ( -7.043655074372488833, 41.66078712639146175, -59.26733995391339249 ) ) ;
#49202=FACE_OUTER_BOUND ( 'NONE', #33016, .T. ) ;
#49205=B_SPLINE_CURVE_WITH_KNOTS ( 'NONE', 3,
 ( #75527, #18384, #60964, #1071, #10776, #101413, #10259, #34046, #43695, #27025 ),
 .UNSPECIFIED., .F., .F.,
 ( 4, 2, 2, 2, 4 ),
 ( 0.000000000000000000, 0.5000000000000000000, 0.7500000000000000000, 0.8750000000000000000, 1.000000000000000000 ),
 .UNSPECIFIED. ) ;
#49213=CARTESIAN_POINT ( 'NONE',  ( -62.81518964951828110, 49.99999999999998579, -4.977225890182330303 ) ) ;
#49227=CARTESIAN_POINT ( 'NONE',  ( -6.701893397842001221, 41.44328394191487774, -70.59544911652842814 ) ) ;
#49240=CARTESIAN_POINT ( 'NONE',  ( -4.852941176470593199, -5.250000000000004441, -70.80672828634229177 ) ) ;
#49243=CARTESIAN_POINT ( 'NONE',  ( 14.91270732344407257, 41.98564553269472555, -86.62216337287246404 ) ) ;
#49254=CARTESIAN_POINT ( 'NONE',  ( -62.34828826644581312, 50.00000000000000000, -10.72527895994686986 ) ) ;
#49287=FACE_OUTER_BOUND ( 'NONE', #17728, .T. ) ;
#49290=CARTESIAN_POINT ( 'NONE',  ( -7.286132170098562177, 40.29425722237677832, -70.75304762475369103 ) ) ;
#49310=CARTESIAN_POINT ( 'NONE',  ( -10.47772246152234565, -5.000000000000000000, -91.06170733474810675 ) ) ;
#49315=B_SPLINE_CURVE_WITH_KNOTS ( 'NONE', 3,
 ( #106255, #65816, #64243, #23257, #105734, #22737, #6503, #46969, #5974, #39440, #22203, #14589, #41012, #55576, #57178, #38906, #71768, #90092 ),
 .UNSPECIFIED., .F., .F.,
 ( 4, 2, 2, 2, 2, 2, 2, 2, 4 ),
 ( 0.000000000000000000, 0.06250000000000000000, 0.1250000000000000000, 0.1875000000000000000, 0.2500000000000000000, 0.3125000000000000000, 0.3750000000000000000, 0.4375000000000000000, 0.5000000000000000000 ),
 .UNSPECIFIED. ) ;
#49326=CARTESIAN_POINT ( 'NONE',  ( 12.50000000000000355, 34.83311936966315869, -54.12527282038643506 ) ) ;
#49391=CARTESIAN_POINT ( 'NONE',  ( -7.731157688197621169, -5.000000000014319212, -17.87147387707815582 ) ) ;
#49397=DIRECTION ( 'NONE',  ( 0.000000000000000000, 0.000000000000000000, 1.000000000000000000 ) ) ;
#49421=CARTESIAN_POINT ( 'NONE',  ( 58.90678327789231616, 48.00000000000000000, -28.11551192221969941 ) ) ;
#49455=CARTESIAN_POINT ( 'NONE',  ( -6.057904167604424295, 41.61856606222242760, -70.65344123333893833 ) ) ;
#49523=B_SPLINE_CURVE_WITH_KNOTS ( 'NONE', 3,
 ( #12336, #86791, #12862, #78140, #37190, #37732, #78654, #70052, #4792, #102958, #29122, #70591, #103483, #84649, #10733, #97490, #31223, #87308, #71112, #32263, #80787, #73216, #96985, #63575, #88373, #55961, #104533 ),
 .UNSPECIFIED., .F., .F.,
 ( 4, 2, 2, 2, 2, 2, 1, 2, 2, 2, 2, 2, 2, 4 ),
 ( 0.000000000000000000, 0.1250000000000165701, 0.2500000000000331402, 0.3750000000000497380, 0.4375000000000578426, 0.4687500000000607847, 0.4843750000000630607, 0.4921875000000641154, 0.5000000000000651701, 0.6250000000000489608, 0.7500000000000326406, 0.8750000000000164313, 0.9375000000000082157, 1.000000000000000000 ),
 .UNSPECIFIED. ) ;
#49573=CARTESIAN_POINT ( 'NONE',  ( -45.60838156036751201, 42.00000000000000000, -79.13121736029046360 ) ) ;
#49582=CARTESIAN_POINT ( 'NONE',  ( 6.635365873752379962, 41.60399788275461219, -58.75656668935356919 ) ) ;
#49599=CARTESIAN_POINT ( 'NONE',  ( 18.06487379447606756, 45.00000000000000711, 62.52595132501897979 ) ) ;
#49605=CARTESIAN_POINT ( 'NONE',  ( -8.292751449259418095, -5.000000000000000888, -16.13133567586304906 ) ) ;
#49609=CARTESIAN_POINT ( 'NONE',  ( 12.34835181856063002, -4.332967528434596538, -12.86601580078908214 ) ) ;
#49612=CARTESIAN_POINT ( 'NONE',  ( -18.91791044776116237, 47.99999999999999289, 62.18611311450883505 ) ) ;
#49626=CARTESIAN_POINT ( 'NONE',  ( -49.86794645319100994, 40.83866221574536581, -41.94290818787430908 ) ) ;
#49641=CARTESIAN_POINT ( 'NONE',  ( -19.49880643229725408, 49.99998348590659702, 59.93398820730007515 ) ) ;
#49655=CARTESIAN_POINT ( 'NONE',  ( -21.89416662624832099, 41.75480087786124272, -77.14963689140114411 ) ) ;
#49660=CARTESIAN_POINT ( 'NONE',  ( -3.140974613990812792, -5.000000000000002665, -96.68767211932356531 ) ) ;
#49666=( LENGTH_UNIT ( ) NAMED_UNIT ( * ) SI_UNIT ( .MILLI., .METRE. ) );
#49678=CARTESIAN_POINT ( 'NONE',  ( 12.12965108312117479, -5.000000000000000000, -89.82640756711197128 ) ) ;
#49679=CARTESIAN_POINT ( 'NONE',  ( -17.49999999999997513, 50.00000000000000000, 100.0000000000000000 ) ) ;
#49685=CARTESIAN_POINT ( 'NONE',  ( -5.800528474434197612, 38.95336917065268523, 63.47065297900079628 ) ) ;
#49724=CARTESIAN_POINT ( 'NONE',  ( 6.890281281981907924, 41.03680257675737408, -70.85895802599645776 ) ) ;
#49736=CARTESIAN_POINT ( 'NONE',  ( 5.354260712552314949, 36.72665595308956199, -54.26279534929282278 ) ) ;
#49743=CARTESIAN_POINT ( 'NONE',  ( 6.941422757283499223, 41.41225026875491722, -70.44081393238894861 ) ) ;
#49765=CARTESIAN_POINT ( 'NONE',  ( 38.12216208879490864, 18.64284798592648329, -4.860317469366568055 ) ) ;
#49788=CARTESIAN_POINT ( 'NONE',  ( -2.850063997753378597, -5.000000000000000000, -72.23558523188754066 ) ) ;
#49794=CARTESIAN_POINT ( 'NONE',  ( -62.91825180719953892, 50.00000000000000000, 6.605622457240398759 ) ) ;
#49808=CARTESIAN_POINT ( 'NONE',  ( 6.991644890290505288, 41.20407774039003357, -58.47941669199799009 ) ) ;
#49825=CARTESIAN_POINT ( 'NONE',  ( -12.50000000000000000, -3.000000000000003109, -14.34180675897363599 ) ) ;
#49834=CARTESIAN_POINT ( 'NONE',  ( -7.278899862585794800, 40.56071481047660399, -70.70219261697603486 ) ) ;
#49843=CARTESIAN_POINT ( 'NONE',  ( 0.000000000000000000, -5.000000000000000000, 10.00000000000000000 ) ) ;
#49854=SURFACE_STYLE_FILL_AREA ( #97339 ) ;
#49868=CARTESIAN_POINT ( 'NONE',  ( 12.50000000000000355, 27.89883036488820167, -45.48774139817316353 ) ) ;
#49870=ORIENTED_EDGE ( 'NONE', *, *, #81900, .T. ) ;
#49881=CARTESIAN_POINT ( 'NONE',  ( -16.51907061138353683, 42.00139744608745218, -87.79003255390433935 ) ) ;
#49883=( BOUNDED_SURFACE ( )  B_SPLINE_SURFACE ( 2, 3, ( 
 ( #87841, #52803, #46834, #85729 ),
 ( #11801, #44733, #102425, #94345 ),
 ( #20507, #24713, #82387, #16593 ) ),
 .UNSPECIFIED., .F., .F., .F. ) 
 B_SPLINE_SURFACE_WITH_KNOTS ( ( 3, 3 ),
 ( 4, 4 ),
 ( 0.000000000000000000, 1.000000000000000000 ),
 ( -0.02264331519860533423, -0.01818793032683159450 ),
 .UNSPECIFIED. ) 
 GEOMETRIC_REPRESENTATION_ITEM ( )  RATIONAL_B_SPLINE_SURFACE ( (
 ( 1.000000000000000000, 1.000000000000000000, 1.000000000000000000, 1.000000000000000000),
 ( 1.857142857142858317, 1.857142857142858317, 1.857142857142858317, 1.857142857142858317),
 ( 1.000000000000000000, 1.000000000000000000, 1.000000000000000000, 1.000000000000000000) ) ) 
 REPRESENTATION_ITEM ( '' )  SURFACE ( )  );
#49894=CARTESIAN_POINT ( 'NONE',  ( -7.493944919676032157, 40.57567429012536309, -59.86116873889386625 ) ) ;
#49920=CARTESIAN_POINT ( 'NONE',  ( 19.31075363035184012, 49.87050359945839517, 61.31541196677274996 ) ) ;
#49928=ORIENTED_EDGE ( 'NONE', *, *, #58682, .T. ) ;
#49930=CARTESIAN_POINT ( 'NONE',  ( -6.904524730080175310, -4.999999999998975930, -16.27804637755029304 ) ) ;
#49953=CARTESIAN_POINT ( 'NONE',  ( -51.78317192862404994, 48.00000000000000000, 39.73656039225668479 ) ) ;
#49957=B_SPLINE_CURVE_WITH_KNOTS ( 'NONE', 3,
 ( #75259, #98477, #41840, #7869, #106029, #67200, #24629, #8408 ),
 .UNSPECIFIED., .F., .F.,
 ( 4, 2, 2, 4 ),
 ( 0.000000000000000000, 0.5000000000000000000, 0.7500000000000000000, 1.000000000000000000 ),
 .UNSPECIFIED. ) ;
#49980=CARTESIAN_POINT ( 'NONE',  ( 19.39114753129161173, 41.87392969580012902, -80.53546452172405168 ) ) ;
#49993=CARTESIAN_POINT ( 'NONE',  ( -19.45221650979668837, 49.97868703238423649, 60.60569223047880172 ) ) ;
#50039=CARTESIAN_POINT ( 'NONE',  ( -17.49999999999997513, 49.17184032807011107, 64.03033582390544609 ) ) ;
#50046=ORIENTED_EDGE ( 'NONE', *, *, #38218, .T. ) ;
#50072=ORIENTED_EDGE ( 'NONE', *, *, #104867, .T. ) ;
#50079=ORIENTED_EDGE ( 'NONE', *, *, #44524, .T. ) ;
#50106=SURFACE_SIDE_STYLE ('',( #90572 ) ) ;
#50110=FILL_AREA_STYLE_COLOUR ( '', #94877 ) ;
#50113=ORIENTED_EDGE ( 'NONE', *, *, #4682, .T. ) ;
#50126=CARTESIAN_POINT ( 'NONE',  ( -1.630169624183789523, -5.000000000000000000, -16.56347947976414403 ) ) ;
#50131=CARTESIAN_POINT ( 'NONE',  ( 17.58497575071690022, 45.00000000000000711, 63.15110831394576962 ) ) ;
#50144=CARTESIAN_POINT ( 'NONE',  ( -5.036189802311206165, -3.000000000000002665, -76.26213611587844809 ) ) ;
#50149=B_SPLINE_CURVE_WITH_KNOTS ( 'NONE', 3,
 ( #48914, #56480, #48391, #99057 ),
 .UNSPECIFIED., .F., .F.,
 ( 4, 4 ),
 ( 0.000000000000000000, 1.000000000000000000 ),
 .UNSPECIFIED. ) ;
#50175=CARTESIAN_POINT ( 'NONE',  ( -19.09326099321248549, 49.66527553187732025, 61.75128748409861856 ) ) ;
#50189=ADVANCED_FACE ( 'NONE', ( #3590 ), #72845, .T. ) ;
#50191=CARTESIAN_POINT ( 'NONE',  ( -20.77102041147630729, 41.81346959299248311, -78.66739485428914236 ) ) ;
#50197=CARTESIAN_POINT ( 'NONE',  ( -6.315918965248128458, 41.33387153033192618, -58.37026290468334366 ) ) ;
#50199=ORIENTED_EDGE ( 'NONE', *, *, #23380, .T. ) ;
#50207=ORIENTED_EDGE ( 'NONE', *, *, #52997, .T. ) ;
#50221=CARTESIAN_POINT ( 'NONE',  ( 60.72168482585779259, 38.95312673567827488, -19.36417048051057677 ) ) ;
#50246=AXIS2_PLACEMENT_3D ( 'NONE', #20467, #105436, #55788 ) ;
#50256=CARTESIAN_POINT ( 'NONE',  ( 0.000000000000000000, -79.93083296558610584, -85.00000000000000000 ) ) ;
#50309=CARTESIAN_POINT ( 'NONE',  ( -7.500000000000005329, 41.41666666666666430, -68.91429205785459544 ) ) ;
#50332=CARTESIAN_POINT ( 'NONE',  ( -90.56128410203886858, 42.00000000000000000, -11.85444436786843703 ) ) ;
#50356=CARTESIAN_POINT ( 'NONE',  ( -7.121430446200055719, 40.29466789218744083, -71.00332351295398325 ) ) ;
#50363=B_SPLINE_CURVE_WITH_KNOTS ( 'NONE', 3,
 ( #16855, #49736, #13517, #44315, #94471, #60519, #36268, #95008, #69135, #102008, #52932, #28167, #46437, #12457, #103087, #12983, #3321, #86913, #61043, #103605, #85858, #20087, #93930, #68604, #44860, #21143, #45911, #70181, #62630, #78267, #79327, #61580, #87440, #29756, #77748, #45386, #69657, #4379 ),
 .UNSPECIFIED., .F., .F.,
 ( 4, 2, 2, 2, 1, 1, 1, 1, 1, 1, 1, 2, 2, 2, 2, 1, 1, 1, 1, 1, 1, 1, 2, 2, 2, 4 ),
 ( 0.000000000000000000, 0.2499999999998910316, 0.3749999999998364086, 0.4374999999998089306, 0.4687499999997950528, 0.4843749999997879474, 0.4921874999997842837, 0.4960937499997825628, 0.4980468749997818967, 0.4990234374997816746, 0.4995117187497816746, 0.4997558593747817302, 0.4999999999997817857, 0.6249999999998058220, 0.6874999999998179234, 0.7187499999998239186, 0.7343749999998269162, 0.7421874999998283595, 0.7460937499998292477, 0.7480468749998296918, 0.7490234374998299138, 0.7495117187498299138, 0.7497558593748300249, 0.7499999999998301359, 0.8749999999999150679, 1.000000000000000000 ),
 .UNSPECIFIED. ) ;
#50372=ORIENTED_EDGE ( 'NONE', *, *, #43901, .T. ) ;
#50390=CARTESIAN_POINT ( 'NONE',  ( 12.49989493515518646, 18.64301898209307140, -36.27145154709465658 ) ) ;
#50401=CARTESIAN_POINT ( 'NONE',  ( 17.50000000000002842, 50.00000000000000000, 63.82142195508322402 ) ) ;
#50413=CARTESIAN_POINT ( 'NONE',  ( -2.094395098902661623, -3.000000000000000000, 8.000000000000000000 ) ) ;
#50416=CARTESIAN_POINT ( 'NONE',  ( -7.500000000000006217, 39.99999999999122480, -59.88032989330939415 ) ) ;
#50422=ORIENTED_EDGE ( 'NONE', *, *, #35288, .T. ) ;
#50452=CARTESIAN_POINT ( 'NONE',  ( -9.313960278265176029, -5.000000000000103029, -17.95852857499287225 ) ) ;
#50476=CARTESIAN_POINT ( 'NONE',  ( -52.56483885390515809, 48.00000000000000000, -38.23529411764715036 ) ) ;
#50497=EDGE_CURVE ( 'NONE', #60656, #24664, #67175, .T. ) ;
#50500=CARTESIAN_POINT ( 'NONE',  ( 18.56873304867848162, 41.90421603127634853, -81.65074648123847112 ) ) ;
#50506=SURFACE_SIDE_STYLE ('',( #76382 ) ) ;
#50554=CARTESIAN_POINT ( 'NONE',  ( -17.49999999999996803, 47.99999999999997868, 64.09949417230998847 ) ) ;
#50569=EDGE_CURVE ( 'NONE', #33011, #288, #103280, .T. ) ;
#50571=CARTESIAN_POINT ( 'NONE',  ( -14.62196857730996946, 42.00000000000000711, -88.48477568205504440 ) ) ;
#50577=ORIENTED_EDGE ( 'NONE', *, *, #37314, .T. ) ;
#50586=ORIENTED_EDGE ( 'NONE', *, *, #76568, .F. ) ;
#50591=EDGE_LOOP ( 'NONE', ( #72662, #97293, #89883, #5127 ) ) ;
#50601=CARTESIAN_POINT ( 'NONE',  ( -6.955654383127702012, 41.30888465058240655, -58.54627983348873244 ) ) ;
#50615=CARTESIAN_POINT ( 'NONE',  ( -23.70422451874885184, 42.00000000000000000, -88.20421627933662023 ) ) ;
#50625=CARTESIAN_POINT ( 'NONE',  ( 7.126148245860624009, 41.12758397993106030, -58.55282951229288102 ) ) ;
#50637=CARTESIAN_POINT ( 'NONE',  ( 5.902907888931476776, -4.999999999999999112, -73.20788160635341058 ) ) ;
#50643=CARTESIAN_POINT ( 'NONE',  ( -8.584127441494805666, -5.000000000000000000, -16.50953036925850981 ) ) ;
#50663=CARTESIAN_POINT ( 'NONE',  ( -6.544091414552472230, -3.000000000000003109, -98.56434427383338459 ) ) ;
#50677=B_SPLINE_CURVE_WITH_KNOTS ( 'NONE', 3,
 ( #60860, #70001, #53806, #53290, #86735, #45213, #3681, #38197, #85668, #95879, #13869, #12810, #103429, #77566, #71057, #95341, #44679, #30094, #62450, #4206, #45724, #79677, #36086, #93750, #19902, #37135, #102902, #52745, #69478, #61936, #21477, #102363, #29066, #20972 ),
 .UNSPECIFIED., .F., .F.,
 ( 4, 2, 2, 2, 2, 2, 2, 2, 2, 2, 2, 2, 2, 2, 2, 2, 4 ),
 ( 0.000000000000000000, 0.06250000000000002776, 0.1250000000000000555, 0.1875000000000000555, 0.2500000000000000555, 0.3125000000000000000, 0.3750000000000000000, 0.4374999999999999445, 0.4999999999999999445, 0.5624999999999998890, 0.6249999999999997780, 0.6874999999999998890, 0.7499999999999998890, 0.8124999999999998890, 0.8749999999999998890, 0.9375000000000000000, 1.000000000000000000 ),
 .UNSPECIFIED. ) ;
#50683=CARTESIAN_POINT ( 'NONE',  ( -19.49662282918389877, 49.99981527065391873, 59.98277621002914373 ) ) ;
#50697=CARTESIAN_POINT ( 'NONE',  ( -19.44876292489749758, 41.87164991014802951, -80.45734961732209456 ) ) ;
#50706=CARTESIAN_POINT ( 'NONE',  ( -2.617478844990611897, -3.000000000000002665, -75.26027323389583046 ) ) ;
#50729=EDGE_LOOP ( 'NONE', ( #1614, #84281, #47163, #83955 ) ) ;
#50766=CARTESIAN_POINT ( 'NONE',  ( -7.302672345405872179, 41.33022796407946942, -59.14964389299829151 ) ) ;
#50828=CARTESIAN_POINT ( 'NONE',  ( -7.500000000000004441, 41.41666666666666430, -71.71180648257555390 ) ) ;
#50856=CARTESIAN_POINT ( 'NONE',  ( -79.13121736037271603, 42.00000000000000000, 45.60838156032633606 ) ) ;
#50862=COLOUR_RGB ( '', 0.72549020, 0.75294118, 0.79215686) ;
#50865=CARTESIAN_POINT ( 'NONE',  ( -63.17580323280985510, 40.83918043368394990, 15.57597231978257213 ) ) ;
#50887=CARTESIAN_POINT ( 'NONE',  ( -6.965116046117190152, 41.61856606226410094, -70.00485699691064667 ) ) ;
#50919=CARTESIAN_POINT ( 'NONE',  ( 12.50000000000001421, 34.82001026956950085, -54.10527893612417216 ) ) ;
#50924=CARTESIAN_POINT ( 'NONE',  ( -6.256238905932293370, -3.000000000000353495, -71.20382035666706599 ) ) ;
#50943=CARTESIAN_POINT ( 'NONE',  ( -7.999999999999996447, -3.000000000000000000, 2.094395098902548824 ) ) ;
#50952=CARTESIAN_POINT ( 'NONE',  ( -5.500000000000006217, 42.00000000000000000, -59.88032989329961708 ) ) ;
#50953=FACE_OUTER_BOUND ( 'NONE', #51272, .T. ) ;
#50984=CARTESIAN_POINT ( 'NONE',  ( 17.82557447769810821, 50.00000000000000000, 62.13990790720372104 ) ) ;
#50994=CARTESIAN_POINT ( 'NONE',  ( -6.618366600633001084, -4.380080200176828420, -16.79229307443615582 ) ) ;
#51006=CARTESIAN_POINT ( 'NONE',  ( -11.91432047182436094, 49.99999999999999289, 64.17585289259305625 ) ) ;
#51049=CARTESIAN_POINT ( 'NONE',  ( 6.145467200814584530, 50.00000000000543565, -92.99666842292452884 ) ) ;
#51070=ADVANCED_FACE ( 'NONE', ( #10341 ), #83890, .T. ) ;
#51107=CARTESIAN_POINT ( 'NONE',  ( 7.500000000000006217, 39.99999999999942446, -59.88032989331673406 ) ) ;
#51109=( BOUNDED_SURFACE ( )  B_SPLINE_SURFACE ( 2, 3, ( 
 ( #48291, #95814, #88250, #7832, #71513, #63457, #96351, #104414, #81189, #40742, #23001, #73627, #7299, #89836, #22482, #81709, #55837, #21941 ),
 ( #56374, #15937, #87724, #15404, #13805, #54793, #46717, #30559, #79609, #39702, #24066, #5724, #105995, #55323, #32143, #48815, #97915, #14330 ),
 ( #47236, #80135, #6238, #56911, #88774, #39174, #31104, #63988, #47758, #80661, #72578, #105480, #41274, #50943, #74165, #245, #50413, #34822 ) ),
 .UNSPECIFIED., .F., .T., .T. ) 
 B_SPLINE_SURFACE_WITH_KNOTS ( ( 3, 3 ),
 ( 4, 2, 2, 2, 2, 2, 2, 2, 4 ),
 ( 0.000000000000000000, 1.000000000000000000 ),
 ( 0.000000000000000000, 0.7853981633974482790, 1.570796326794896558, 2.356194490192344837, 3.141592653589793116, 3.926990816987241395, 4.712388980384689674, 5.497787143782137953, 6.283185307179586232 ),
 .UNSPECIFIED. ) 
 GEOMETRIC_REPRESENTATION_ITEM ( )  RATIONAL_B_SPLINE_SURFACE ( (
 ( 1.000000000000000000, 1.000000000000000000, 1.000000000000000000, 1.000000000000000000, 1.000000000000000000, 1.000000000000000000, 1.000000000000000000, 1.000000000000000000, 1.000000000000000000, 1.000000000000000000, 1.000000000000000000, 1.000000000000000000, 1.000000000000000000, 1.000000000000000000, 1.000000000000000000, 1.000000000000000000, 1.000000000000000000, 1.000000000000000000),
 ( 1.857142857142858317, 1.857142857142858317, 1.857142857142858317, 1.857142857142858317, 1.857142857142858317, 1.857142857142858317, 1.857142857142858317, 1.857142857142858317, 1.857142857142858317, 1.857142857142858317, 1.857142857142858317, 1.857142857142858317, 1.857142857142858317, 1.857142857142858317, 1.857142857142858317, 1.857142857142858317, 1.857142857142858317, 1.857142857142858317),
 ( 1.000000000000000000, 1.000000000000000000, 1.000000000000000000, 1.000000000000000000, 1.000000000000000000, 1.000000000000000000, 1.000000000000000000, 1.000000000000000000, 1.000000000000000000, 1.000000000000000000, 1.000000000000000000, 1.000000000000000000, 1.000000000000000000, 1.000000000000000000, 1.000000000000000000, 1.000000000000000000, 1.000000000000000000, 1.000000000000000000) ) ) 
 REPRESENTATION_ITEM ( '' )  SURFACE ( )  );
#51131=ADVANCED_FACE ( 'NONE', ( #72816 ), #23440, .T. ) ;
#51165=CARTESIAN_POINT ( 'NONE',  ( 6.894536717076869436, 41.40765062553401776, -58.61755662071193029 ) ) ;
#51166=CARTESIAN_POINT ( 'NONE',  ( -7.500000000000007994, 40.00000000000000000, -70.16688272716517361 ) ) ;
#51177=CARTESIAN_POINT ( 'NONE',  ( -8.737863883542573262, -3.000000000000003109, -79.96381019629100706 ) ) ;
#51202=ORIENTED_EDGE ( 'NONE', *, *, #61215, .T. ) ;
#51204=CARTESIAN_POINT ( 'NONE',  ( 8.447961717367675760, -4.999999999999968914, -16.27270454675222666 ) ) ;
#51206=CARTESIAN_POINT ( 'NONE',  ( 10.71924530989373103, -3.000000000000002665, -74.44967652504091404 ) ) ;
#51207=CARTESIAN_POINT ( 'NONE',  ( -15.04647843581905420, -3.000000000000003109, -85.64811627161152785 ) ) ;
#51223=CARTESIAN_POINT ( 'NONE',  ( -17.49999999999995737, 51.99999999999994316, 59.71562975593252531 ) ) ;
#51244=CARTESIAN_POINT ( 'NONE',  ( 5.036189802311931807, -3.000000000000002665, -76.26213611587876073 ) ) ;
#51264=LINE ( 'NONE', #19500, #4543 ) ;
#51272=EDGE_LOOP ( 'NONE', ( #26076, #17327, #43328, #37555, #30315, #48318, #15888 ) ) ;
#51276=DIRECTION ( 'NONE',  ( -0.000000000000000000, 1.000000000000000000, -0.000000000000000000 ) ) ;
#51278=FILL_AREA_STYLE ('',( #93361 ) ) ;
#51280=CARTESIAN_POINT ( 'NONE',  ( 8.641101172573151246, -5.000000000000001776, -72.37542516944607485 ) ) ;
#51305=CARTESIAN_POINT ( 'NONE',  ( -7.484956994628422677, 40.70736991036710606, -59.65999153245496700 ) ) ;
#51306=CARTESIAN_POINT ( 'NONE',  ( 6.806778131844891000, 41.25019534418786549, -70.74215739200818120 ) ) ;
#51396=CARTESIAN_POINT ( 'NONE',  ( -2.912673042965788187E-14, 42.00000000000000000, -90.56128410203886858 ) ) ;
#51407=CARTESIAN_POINT ( 'NONE',  ( -31.42849905601886817, 40.83882027459411290, 56.97537319886429685 ) ) ;
#51416=CARTESIAN_POINT ( 'NONE',  ( -6.019162162299732444, 41.99999999999999289, -71.20548073449060666 ) ) ;
#51424=CARTESIAN_POINT ( 'NONE',  ( -2.617478844992341180, 49.99999999999999289, -75.26027323389158141 ) ) ;
#51429=CARTESIAN_POINT ( 'NONE',  ( -7.412969763095563103, 41.14559726925956085, -68.91429205793708945 ) ) ;
#51433=ORIENTED_EDGE ( 'NONE', *, *, #91606, .T. ) ;
#51450=( BOUNDED_CURVE ( )  B_SPLINE_CURVE ( 2, ( #52392, #76666, #87441 ),
 .UNSPECIFIED., .F., .F. ) 
 B_SPLINE_CURVE_WITH_KNOTS ( ( 3, 3 ),
 ( 0.000000000000000000, 1.000000000000000000 ),
 .UNSPECIFIED. ) 
 CURVE ( )  GEOMETRIC_REPRESENTATION_ITEM ( )  RATIONAL_B_SPLINE_CURVE ( ( 1.000000000000000000, 1.857142857142858317, 1.000000000000000000 ) ) 
 REPRESENTATION_ITEM ( '' )  );
#51463=CARTESIAN_POINT ( 'NONE',  ( -18.10250950527013813, 45.00000000000000000, 62.50294572439922547 ) ) ;
#51475=EDGE_LOOP ( 'NONE', ( #29551, #48611, #1975, #79993, #57678, #73073, #30240 ) ) ;
#51492=SURFACE_SIDE_STYLE ('',( #27276 ) ) ;
#51519=CARTESIAN_POINT ( 'NONE',  ( -6.641837642500876271, 41.74662713182689089, -59.04567091375639620 ) ) ;
#51525=CARTESIAN_POINT ( 'NONE',  ( -8.464095510818648194, -5.000000000000260236, -16.25913807934452393 ) ) ;
#51528=CARTESIAN_POINT ( 'NONE',  ( 17.56618469255510817, 50.00000000000001421, 62.84295761643686262 ) ) ;
#51531=EDGE_CURVE ( 'NONE', #26788, #80415, #99941, .T. ) ;
#51533=( NAMED_UNIT ( * ) PLANE_ANGLE_UNIT ( ) SI_UNIT ( $, .RADIAN. ) );
#51541=CARTESIAN_POINT ( 'NONE',  ( -6.738141070038324187, -4.358126490537220121, -16.85492060643100842 ) ) ;
#51551=CARTESIAN_POINT ( 'NONE',  ( 6.840797686643921516, 41.85687274158131288, -69.25136110413218660 ) ) ;
#51552=CARTESIAN_POINT ( 'NONE',  ( 50.18984356158254201, 50.00000000000000000, 38.51389699555568313 ) ) ;
#51562=CARTESIAN_POINT ( 'NONE',  ( -30.50942973404921332, 18.64284798593271475, -23.36871039511863657 ) ) ;
#51576=CARTESIAN_POINT ( 'NONE',  ( 28.42041225899258450, 41.23827639480541052, -68.38640372166889847 ) ) ;
#51579=PLANE ( 'NONE',  #5389 ) ;
#51582=ORIENTED_EDGE ( 'NONE', *, *, #55946, .F. ) ;
#51591=CARTESIAN_POINT ( 'NONE',  ( 9.999999999999989342, 49.99999999999999289, -86.30899693748767731 ) ) ;
#51635=FILL_AREA_STYLE_COLOUR ( '', #36779 ) ;
#51638=CARTESIAN_POINT ( 'NONE',  ( 18.91791044776121211, 46.00000000000000000, 62.18611311450883505 ) ) ;
#51678=CARTESIAN_POINT ( 'NONE',  ( -7.070595406388543225, 41.16321361949651703, -58.51508551921422452 ) ) ;
#51687=CARTESIAN_POINT ( 'NONE',  ( 12.50000000000000711, 3.927497522143841291, -21.92086562379284587 ) ) ;
#51697=CARTESIAN_POINT ( 'NONE',  ( -72.41885610115939187, 42.00000000000000000, 55.65414010178468374 ) ) ;
#51737=CARTESIAN_POINT ( 'NONE',  ( -7.500000000000007105, -3.000000000000000000, -68.91429205785459544 ) ) ;
#51786=CARTESIAN_POINT ( 'NONE',  ( 9.999999999999994671, -3.000000000000002665, -83.69100306252322241 ) ) ;
#51793=CARTESIAN_POINT ( 'NONE',  ( -10.49999999997808331, -5.000000000000000000, -12.52300748972991506 ) ) ;
#51794=CARTESIAN_POINT ( 'NONE',  ( -15.51786670351801689, -4.332661967059642016, 9.509450810728861114 ) ) ;
#51824=CARTESIAN_POINT ( 'NONE',  ( -12.29798915171474150, -4.463815859614853387, -12.75153713776978037 ) ) ;
#51830=SURFACE_SIDE_STYLE ('',( #2747 ) ) ;
#51845=CARTESIAN_POINT ( 'NONE',  ( -18.98212999821499380, 49.45283421538681523, 61.95133595785922864 ) ) ;
#51846=CARTESIAN_POINT ( 'NONE',  ( -6.943035977205679998, 41.50417750172036335, -58.81491712266881677 ) ) ;
#51861=CARTESIAN_POINT ( 'NONE',  ( 7.126148245860624009, 41.12758397993106740, -58.55282951229289523 ) ) ;
#51863=CARTESIAN_POINT ( 'NONE',  ( 10.48543666094731996, -5.000000000000002665, -78.95657223723277696 ) ) ;
#51883=CARTESIAN_POINT ( 'NONE',  ( 4.491425985184478442, 18.64284798592898795, 38.16738163467809386 ) ) ;
#51904=CARTESIAN_POINT ( 'NONE',  ( 10.74465425723776058, 49.99999999999999289, -95.72854256507095272 ) ) ;
#51905=ORIENTED_EDGE ( 'NONE', *, *, #73333, .F. ) ;
#51913=CARTESIAN_POINT ( 'NONE',  ( 52.56483885390523625, 40.83906611471594061, -38.23529411764706509 ) ) ;
#51927=CARTESIAN_POINT ( 'NONE',  ( -57.69562748396144514, 41.99999999999999289, -15.50526908263377734 ) ) ;
#51944=CARTESIAN_POINT ( 'NONE',  ( 7.135888613855538409, 41.99999999999999289, -71.74865085751123672 ) ) ;
#51951=CARTESIAN_POINT ( 'NONE',  ( -1.308996937483428491, 49.99999999999999289, -95.00000000000001421 ) ) ;
#51961=VERTEX_POINT ( 'NONE', #98071 ) ;
#51963=CARTESIAN_POINT ( 'NONE',  ( -5.036189803708991164, 47.99999999999998579, -93.73786388354257326 ) ) ;
#51976=( NAMED_UNIT ( * ) PLANE_ANGLE_UNIT ( ) SI_UNIT ( $, .RADIAN. ) );
#51977=( GEOMETRIC_REPRESENTATION_CONTEXT ( 3 ) GLOBAL_UNCERTAINTY_ASSIGNED_CONTEXT ( ( #63576 ) ) GLOBAL_UNIT_ASSIGNED_CONTEXT ( ( #57167, #89556, #24837 ) ) REPRESENTATION_CONTEXT ( 'NONE', 'WORKASPACE' ) );
#51978=CARTESIAN_POINT ( 'NONE',  ( -6.952098965573305200, 40.29466765805469919, -71.12438203485694999 ) ) ;
#51992=CARTESIAN_POINT ( 'NONE',  ( -17.95175771543782162, 45.00000000000000711, 62.60109665436401372 ) ) ;
#51997=ORIENTED_EDGE ( 'NONE', *, *, #60913, .F. ) ;
#52012=CARTESIAN_POINT ( 'NONE',  ( -25.45921313960911903, 43.62243447522785544, -75.49936859611810291 ) ) ;
#52028=CARTESIAN_POINT ( 'NONE',  ( -5.428831668361731033, 41.92214390794531198, -59.12797028773363905 ) ) ;
#52030=CARTESIAN_POINT ( 'NONE',  ( 12.34835181856063002, -4.332967528434596538, -12.86601580078908214 ) ) ;
#52043=CARTESIAN_POINT ( 'NONE',  ( -55.22048556080177661, 48.00000000000000000, 34.80214219306111545 ) ) ;
#52070=CARTESIAN_POINT ( 'NONE',  ( -5.075741750048029743, -4.332638003024074536, -17.09621982684887698 ) ) ;
#52077=DIRECTION ( 'NONE',  ( 0.000000000000000000, 0.000000000000000000, 1.000000000000000000 ) ) ;
#52079=( BOUNDED_SURFACE ( )  B_SPLINE_SURFACE ( 2, 3, ( 
 ( #90427, #25187, #49421, #33805, #82324, #74754, #8435, #58598, #99562, #24652, #41335, #17077, #41866, #65620, #64564, #74227, #99024, #304, #98502, #97432, #58045, #90968, #25742, #49953, #97979, #81247, #834, #48355, #23593, #82862, #66682, #89373, #7363, #50476 ),
 ( #89891, #6838, #40275, #15461, #73151, #106053, #65081, #73695, #24132, #56977, #7896, #19779, #67748, #1928, #9485, #92546, #3007, #100635, #51006, #52610, #19254, #61262, #2465, #28388, #44548, #18693, #34879, #27873, #27339, #60217, #77437, #52083, #11080, #93083 ),
 ( #101708, #68830, #1384, #35414, #59665, #85539, #59132, #42396, #84996, #11619, #51552, #60738, #75291, #3551, #44005, #36490, #76892, #35958, #83923, #102237, #34352, #94150, #84465, #67226, #69358, #26795, #10558, #68283, #43475, #76352, #93626, #101179, #20321, #83388 ) ),
 .UNSPECIFIED., .F., .F., .F. ) 
 B_SPLINE_SURFACE_WITH_KNOTS ( ( 3, 3 ),
 ( 4, 2, 2, 2, 2, 2, 2, 2, 2, 2, 2, 2, 2, 2, 2, 2, 4 ),
 ( 0.000000000000000000, 1.000000000000000000 ),
 ( 0.9419214012998449181, 1.216880307836088360, 1.491839214372332023, 1.766798120908575465, 2.041757027444818906, 2.316715933981062570, 2.591674840517305789, 2.866633747053549452, 3.141592653589793116, 3.416551560126036780, 3.691510466662280443, 3.966469373198524107, 4.241428279734767770, 4.516387186271010989, 4.791346092807254209, 5.066304999343497428, 5.341263905879741536 ),
 .UNSPECIFIED. ) 
 GEOMETRIC_REPRESENTATION_ITEM ( )  RATIONAL_B_SPLINE_SURFACE ( (
 ( 1.000000000000000000, 1.000000000000000000, 1.000000000000000000, 1.000000000000000000, 1.000000000000000000, 1.000000000000000000, 1.000000000000000000, 1.000000000000000000, 1.000000000000000000, 1.000000000000000000, 1.000000000000000000, 1.000000000000000000, 1.000000000000000000, 1.000000000000000000, 1.000000000000000000, 1.000000000000000000, 1.000000000000000000, 1.000000000000000000, 1.000000000000000000, 1.000000000000000000, 1.000000000000000000, 1.000000000000000000, 1.000000000000000000, 1.000000000000000000, 1.000000000000000000, 1.000000000000000000, 1.000000000000000000, 1.000000000000000000, 1.000000000000000000, 1.000000000000000000, 1.000000000000000000, 1.000000000000000000, 1.000000000000000000, 1.000000000000000000),
 ( 1.857142857142858317, 1.857142857142858317, 1.857142857142858317, 1.857142857142858317, 1.857142857142858317, 1.857142857142858317, 1.857142857142858317, 1.857142857142858317, 1.857142857142858317, 1.857142857142858317, 1.857142857142858317, 1.857142857142858317, 1.857142857142858317, 1.857142857142858317, 1.857142857142858317, 1.857142857142858317, 1.857142857142858317, 1.857142857142858317, 1.857142857142858317, 1.857142857142858317, 1.857142857142858317, 1.857142857142858317, 1.857142857142858317, 1.857142857142858317, 1.857142857142858317, 1.857142857142858317, 1.857142857142858317, 1.857142857142858317, 1.857142857142858317, 1.857142857142858317, 1.857142857142858317, 1.857142857142858317, 1.857142857142858317, 1.857142857142858317),
 ( 1.000000000000000000, 1.000000000000000000, 1.000000000000000000, 1.000000000000000000, 1.000000000000000000, 1.000000000000000000, 1.000000000000000000, 1.000000000000000000, 1.000000000000000000, 1.000000000000000000, 1.000000000000000000, 1.000000000000000000, 1.000000000000000000, 1.000000000000000000, 1.000000000000000000, 1.000000000000000000, 1.000000000000000000, 1.000000000000000000, 1.000000000000000000, 1.000000000000000000, 1.000000000000000000, 1.000000000000000000, 1.000000000000000000, 1.000000000000000000, 1.000000000000000000, 1.000000000000000000, 1.000000000000000000, 1.000000000000000000, 1.000000000000000000, 1.000000000000000000, 1.000000000000000000, 1.000000000000000000, 1.000000000000000000, 1.000000000000000000) ) ) 
 REPRESENTATION_ITEM ( '' )  SURFACE ( )  );
#52083=CARTESIAN_POINT ( 'NONE',  ( -58.90678327790940472, 50.00000000004006750, -28.11551192219710771 ) ) ;
#52106=ORIENTED_EDGE ( 'NONE', *, *, #18042, .T. ) ;
#52114=ORIENTED_EDGE ( 'NONE', *, *, #85377, .F. ) ;
#52123=CARTESIAN_POINT ( 'NONE',  ( -9.999999999999989342, 49.99999999999999289, -86.30899693748770574 ) ) ;
#52167=CARTESIAN_POINT ( 'NONE',  ( -51.48757442383521976, 38.95383793070303824, -37.45149417477430376 ) ) ;
#52205=FACE_OUTER_BOUND ( 'NONE', #34659, .T. ) ;
#52210=CARTESIAN_POINT ( 'NONE',  ( -6.372519863258895967, 41.41795155077670643, -58.45320710872936587 ) ) ;
#52228=CARTESIAN_POINT ( 'NONE',  ( 7.109733078360420677, 41.69026692163959069, -59.69141567447950081 ) ) ;
#52229=CARTESIAN_POINT ( 'NONE',  ( 38.36535705883633085, 18.64316884711714550, -5.022013495247578341 ) ) ;
#52240=CARTESIAN_POINT ( 'NONE',  ( 5.921004257435177998, 41.52415860376049750, -58.52392854124622801 ) ) ;
#52242=ORIENTED_EDGE ( 'NONE', *, *, #76568, .T. ) ;
#52245=DIRECTION ( 'NONE',  ( 0.000000000000000000, 0.000000000000000000, 1.000000000000000000 ) ) ;
#52257=CARTESIAN_POINT ( 'NONE',  ( 7.036764706176849238, 40.29466777802799271, -71.06385277369803077 ) ) ;
#52266=CARTESIAN_POINT ( 'NONE',  ( 52.27951051746358502, 47.99999999999999289, 38.96734372144647551 ) ) ;
#52286=SURFACE_SIDE_STYLE ('',( #4813 ) ) ;
#52297=CARTESIAN_POINT ( 'NONE',  ( -17.49999999999997513, 51.99999999999955946, 59.64162155654619824 ) ) ;
#52325=CARTESIAN_POINT ( 'NONE',  ( -14.99896353599397258, -5.000000000000000888, 9.191463535712019350 ) ) ;
#52346=STYLED_ITEM ( 'NONE', ( #62408 ), #54736 ) ;
#52349=ORIENTED_EDGE ( 'NONE', *, *, #94786, .F. ) ;
#52350=CARTESIAN_POINT ( 'NONE',  ( 19.49911599185411148, 49.99996344174991236, 59.94524073513129991 ) ) ;
#52362=FILL_AREA_STYLE ('',( #36766 ) ) ;
#52374=CARTESIAN_POINT ( 'NONE',  ( -19.20197792873035425, 49.77790350908116324, 61.55673312277118470 ) ) ;
#52375=CARTESIAN_POINT ( 'NONE',  ( -7.484880931609037447, 40.61737797493887570, -59.44023054564222264 ) ) ;
#52376=CARTESIAN_POINT ( 'NONE',  ( 6.686881269052097565, 40.00000000387462507, -71.19596970773797295 ) ) ;
#52392=CARTESIAN_POINT ( 'NONE',  ( 4.852941176470592310, -3.000000000000002665, -70.80672828634229177 ) ) ;
#52395=CARTESIAN_POINT ( 'NONE',  ( 11.68767211932355998, -5.000000000000002665, -81.85902538600510070 ) ) ;
#52413=CARTESIAN_POINT ( 'NONE',  ( 38.20903166376764659, 18.64284798592685632, 4.122114450692562215 ) ) ;
#52423=STYLED_ITEM ( 'NONE', ( #54597 ), #85465 ) ;
#52432=CARTESIAN_POINT ( 'NONE',  ( 12.13034742782427955, 48.00000000000000000, -93.82352941176471006 ) ) ;
#52450=EDGE_CURVE ( 'NONE', #15506, #38679, #25744, .T. ) ;
#52459=CARTESIAN_POINT ( 'NONE',  ( -57.69562748392037577, 41.99999999991776178, 15.50526908263360681 ) ) ;
#52466=CARTESIAN_POINT ( 'NONE',  ( -62.40055500521754794, 40.83861719869454987, 18.44141605947073970 ) ) ;
#52472=EDGE_LOOP ( 'NONE', ( #12392, #65115 ) ) ;
#52475=FACE_OUTER_BOUND ( 'NONE', #71307, .T. ) ;
#52483=CARTESIAN_POINT ( 'NONE',  ( 6.043427762771891310, 50.00000000000000000, -95.48543666094653304 ) ) ;
#52502=CARTESIAN_POINT ( 'NONE',  ( -7.500000000000007105, -3.000000000000000000, -68.91429205785459544 ) ) ;
#52513=CARTESIAN_POINT ( 'NONE',  ( -5.556063244994718708, 40.28998690596864662, -71.04001413054817249 ) ) ;
#52525=CARTESIAN_POINT ( 'NONE',  ( -17.53184552654991180, 45.00000000000001421, 63.43879945933183961 ) ) ;
#52528=CARTESIAN_POINT ( 'NONE',  ( 17.50000000000004974, 48.00000000000341771, 64.09949417230997426 ) ) ;
#52538=ADVANCED_FACE ( 'NONE', ( #89612 ), #4194, .T. ) ;
#52541=CARTESIAN_POINT ( 'NONE',  ( -16.52732684424165654, 43.98685724163156863, -87.77868211029610279 ) ) ;
#52543=EDGE_CURVE ( 'NONE', #89905, #93842, #10207, .T. ) ;
#52571=CARTESIAN_POINT ( 'NONE',  ( 1.308996938995747872, -3.000000000000001776, -95.00000000000001421 ) ) ;
#52580=CARTESIAN_POINT ( 'NONE',  ( -6.031326303077676698, 41.99459390127218938, -59.73016711425880487 ) ) ;
#52608=CARTESIAN_POINT ( 'NONE',  ( 6.159998411599313606, 41.93068706783093091, -70.02314924739579283 ) ) ;
#52610=CARTESIAN_POINT ( 'NONE',  ( -23.38163988261890225, 49.99999999999999289, 60.94087333798560735 ) ) ;
#52635=CARTESIAN_POINT ( 'NONE',  ( 41.70086632176889196, 39.59106985249150057, -50.69632281737485613 ) ) ;
#52652=CARTESIAN_POINT ( 'NONE',  ( 25.60851123679735863, 50.00000000031798919, -75.29411764726214074 ) ) ;
#52654=CARTESIAN_POINT ( 'NONE',  ( -11.68767211932491179, 50.00000000000000000, -81.85902538600507228 ) ) ;
#52696=CARTESIAN_POINT ( 'NONE',  ( -30.04543272336563575, 41.08154905281699598, -66.19662526517841172 ) ) ;
#52699=CARTESIAN_POINT ( 'NONE',  ( 7.022229286271646664, -4.221542269094484823, -17.11103215588186544 ) ) ;
#52724=CARTESIAN_POINT ( 'NONE',  ( 10.47772246152095477, 50.00000000000000711, -91.06170733474699830 ) ) ;
#52740=DIRECTION ( 'NONE',  ( 0.000000000000000000, 1.000000000000000000, 0.000000000000000000 ) ) ;
#52741=CARTESIAN_POINT ( 'NONE',  ( -5.175364584845236315, 41.93912275385426369, -69.86374487332780348 ) ) ;
#52743=DIRECTION ( 'NONE',  ( 0.000000000000000000, 1.000000000000000000, 0.000000000000000000 ) ) ;
#52745=CARTESIAN_POINT ( 'NONE',  ( -16.39454849390063629, -4.999999999999998224, -0.9786395306135168282 ) ) ;
#52746=CARTESIAN_POINT ( 'NONE',  ( -5.659803839289578420, 41.67004224697031844, -58.69865676442391589 ) ) ;
#52751=EDGE_CURVE ( 'NONE', #103692, #57232, #8910, .T. ) ;
#52771=CARTESIAN_POINT ( 'NONE',  ( -38.36535705883633085, 18.64316884711714195, 5.022013495247505510 ) ) ;
#52778=CARTESIAN_POINT ( 'NONE',  ( 7.090506028190234566, 41.24768140130692728, -58.61601156502441512 ) ) ;
#52783=SURFACE_SIDE_STYLE ('',( #53327 ) ) ;
#52803=CARTESIAN_POINT ( 'NONE',  ( -13.00569629258622939, 42.57699573218433642, -92.62012368208512214 ) ) ;
#52807=MECHANICAL_DESIGN_GEOMETRIC_PRESENTATION_REPRESENTATION('',(#95854),#97519);
#52818=CARTESIAN_POINT ( 'NONE',  ( -10.71924530988990476, -5.000000000000002665, -74.44967652504222144 ) ) ;
#52866=CARTESIAN_POINT ( 'NONE',  ( -17.55833715088017044, -4.999999999999999112, -1.075502477179389960 ) ) ;
#52878=STYLED_ITEM ( 'NONE', ( #47273 ), #59337 ) ;
#52881=SHAPE_REPRESENTATION ( '2. Holder', ( #10728 ), #93449 ) ;
#52885=ORIENTED_EDGE ( 'NONE', *, *, #7981, .T. ) ;
#52894=CARTESIAN_POINT ( 'NONE',  ( 19.49590807900633038, 49.99971735798833095, 59.99840023191819682 ) ) ;
#52903=CARTESIAN_POINT ( 'NONE',  ( -11.55835547680480069, -4.925501566984745061, -12.56497939361423200 ) ) ;
#52907=CARTESIAN_POINT ( 'NONE',  ( -7.500000000000001776, 13.44157116919690331, -32.95552552993890316 ) ) ;
#52918=CARTESIAN_POINT ( 'NONE',  ( -19.34201468796980095, 49.89488280191405778, 61.20624413881779446 ) ) ;
#52919=CARTESIAN_POINT ( 'NONE',  ( 5.548194972809757708, 40.55407393629103296, -71.04437963701762726 ) ) ;
#52932=CARTESIAN_POINT ( 'NONE',  ( 5.294781512610923002, 18.76028034990808635, -38.10389976851315907 ) ) ;
#52939=SURFACE_SIDE_STYLE ('',( #87447 ) ) ;
#52948=FILL_AREA_STYLE_COLOUR ( '', #78584 ) ;
#52968=CARTESIAN_POINT ( 'NONE',  ( 6.145819459792239314, -5.000000000000000000, 7.996135855217247013 ) ) ;
#52979=VERTEX_POINT ( 'NONE', #12667 ) ;
#52997=EDGE_CURVE ( 'NONE', #72225, #5970, #95251, .T. ) ;
#52998=CARTESIAN_POINT ( 'NONE',  ( 39.84006773347349650, 41.92684729384938436, -55.72896217575698330 ) ) ;
#53006=CARTESIAN_POINT ( 'NONE',  ( 37.36680950587120975, 18.64316884708630084, 10.04205104290988437 ) ) ;
#53013=CARTESIAN_POINT ( 'NONE',  ( 14.81491239056285991, 40.83920115135541096, 63.35878236462720281 ) ) ;
#53031=( BOUNDED_CURVE ( )  B_SPLINE_CURVE ( 2, ( #15413, #24075, #5731 ),
 .UNSPECIFIED., .F., .F. ) 
 B_SPLINE_CURVE_WITH_KNOTS ( ( 3, 3 ),
 ( 0.000000000000000000, 1.000000000000000000 ),
 .UNSPECIFIED. ) 
 CURVE ( )  GEOMETRIC_REPRESENTATION_ITEM ( )  RATIONAL_B_SPLINE_CURVE ( ( 1.000000000000000000, 1.857142857142858317, 1.000000000000000000 ) ) 
 REPRESENTATION_ITEM ( '' )  );
#53033=CARTESIAN_POINT ( 'NONE',  ( -1.570796324976843295, 50.00000000000000000, -73.00000000000001421 ) ) ;
#53054=CARTESIAN_POINT ( 'NONE',  ( 6.573529411764729602, 40.00000000373363918, -71.39502911389392636 ) ) ;
#53062=CARTESIAN_POINT ( 'NONE',  ( -5.207235045403211693, 40.28819020782994187, -70.92786788965571532 ) ) ;
#53065=( GEOMETRIC_REPRESENTATION_CONTEXT ( 3 ) GLOBAL_UNCERTAINTY_ASSIGNED_CONTEXT ( ( #55962 ) ) GLOBAL_UNIT_ASSIGNED_CONTEXT ( ( #19870, #64020, #88802 ) ) REPRESENTATION_CONTEXT ( 'NONE', 'WORKASPACE' ) );
#53067=ORIENTED_EDGE ( 'NONE', *, *, #19213, .F. ) ;
#53098=COLOUR_RGB ( '', 0.66274510, 0.83137255, 0.94901961) ;
#53126=CARTESIAN_POINT ( 'NONE',  ( 63.03617022296134564, 48.00000000000000000, -16.93907820452146851 ) ) ;
#53131=CARTESIAN_POINT ( 'NONE',  ( -6.913779242700421435, 41.73441082398074542, -59.30275289623196500 ) ) ;
#53135=CARTESIAN_POINT ( 'NONE',  ( 7.500000000000007105, -3.000000000000000000, -68.91429205785459544 ) ) ;
#53141=CARTESIAN_POINT ( 'NONE',  ( 17.66271159654818845, 50.00000000000000711, 62.46904644769021075 ) ) ;
#53158=ORIENTED_EDGE ( 'NONE', *, *, #86406, .T. ) ;
#53164=CARTESIAN_POINT ( 'NONE',  ( 5.465597732043399049, 41.93635053422439540, -70.00903522191315176 ) ) ;
#53205=CARTESIAN_POINT ( 'NONE',  ( -6.145467200818548470, 49.99999999999999289, -77.00333157709850695 ) ) ;
#53226=AXIS2_PLACEMENT_3D ( 'NONE', #40833, #18175, #66168 ) ;
#53229=FACE_OUTER_BOUND ( 'NONE', #38060, .T. ) ;
#53248=SURFACE_SIDE_STYLE ('',( #75916 ) ) ;
#53250=CARTESIAN_POINT ( 'NONE',  ( -18.83156529568702808, 50.00000000000000000, 60.81392993381482626 ) ) ;
#53251=CARTESIAN_POINT ( 'NONE',  ( 18.91791044776121211, 45.00000000000000711, 62.18611311450882795 ) ) ;
#53283=ADVANCED_FACE ( 'NONE', ( #91361 ), #12372, .T. ) ;
#53290=CARTESIAN_POINT ( 'NONE',  ( 14.68325236364846198, -5.000000000000000000, -7.358060591975124076 ) ) ;
#53291=CARTESIAN_POINT ( 'NONE',  ( -6.453255531754163776, 41.48539074419475980, -58.52372506869146918 ) ) ;
#53311=CARTESIAN_POINT ( 'NONE',  ( -7.754160006593189713, 42.00000000000000711, 59.23741894013591036 ) ) ;
#53321=CARTESIAN_POINT ( 'NONE',  ( -7.500000000000007105, 42.00000000000000711, -62.89165061483231511 ) ) ;
#53327=SURFACE_STYLE_FILL_AREA ( #68990 ) ;
#53356=CARTESIAN_POINT ( 'NONE',  ( 10.71924530989560154, -5.000000000000002665, -74.44967652503841293 ) ) ;
#53396=ORIENTED_EDGE ( 'NONE', *, *, #34685, .F. ) ;
#53409=CARTESIAN_POINT ( 'NONE',  ( -3.510455435514055811, -4.999999999999999112, 17.23741894013592102 ) ) ;
#53433=CARTESIAN_POINT ( 'NONE',  ( 6.256238905641753334, -4.999999999999998224, -71.20382033076053574 ) ) ;
#53442=CARTESIAN_POINT ( 'NONE',  ( -7.500000000018718360, -2.376982511157173406, -18.31627213068317062 ) ) ;
#53457=CARTESIAN_POINT ( 'NONE',  ( 5.625019092414619948, 41.66287055497627989, -70.61600277306789053 ) ) ;
#53472=CARTESIAN_POINT ( 'NONE',  ( -6.397334739185441599, -3.000000000000000444, -4.916373759799320453 ) ) ;
#53475=SURFACE_STYLE_FILL_AREA ( #69141 ) ;
#53479=VERTEX_POINT ( 'NONE', #79809 ) ;
#53509=FILL_AREA_STYLE_COLOUR ( '', #60207 ) ;
#53536=CARTESIAN_POINT ( 'NONE',  ( -33.52312678242540755, 18.64316884714407152, -19.32152200344674498 ) ) ;
#53544=CARTESIAN_POINT ( 'NONE',  ( -65.03121167221090104, 39.42464376491766842, -2.179090956683532809 ) ) ;
#53550=ORIENTED_EDGE ( 'NONE', *, *, #50569, .F. ) ;
#53561=CARTESIAN_POINT ( 'NONE',  ( 7.374560640984048732, 50.00000000000000000, -94.59600210749853488 ) ) ;
#53567=CARTESIAN_POINT ( 'NONE',  ( -38.34155876363399074, 18.64284798593178394, -2.616639027941926710 ) ) ;
#53572=CARTESIAN_POINT ( 'NONE',  ( -9.739726766683149961, 48.00000000000000000, -82.38252115640720774 ) ) ;
#53587=CARTESIAN_POINT ( 'NONE',  ( -5.569577480994083452, 40.00000000004619949, -71.04463856145632406 ) ) ;
#53596=CARTESIAN_POINT ( 'NONE',  ( -17.96996975600059088, 45.00000000000001421, 62.58803962699757761 ) ) ;
#53599=ORIENTED_EDGE ( 'NONE', *, *, #103844, .T. ) ;
#53600=CARTESIAN_POINT ( 'NONE',  ( 17.50000000000002842, 47.00000000000000000, 64.09953197959339377 ) ) ;
#53614=CARTESIAN_POINT ( 'NONE',  ( 7.133125581337410814, 41.57693000336763589, -59.23559349472980529 ) ) ;
#53635=CARTESIAN_POINT ( 'NONE',  ( -14.82275922467060347, -4.333298119783967728, -10.06958627510921467 ) ) ;
#53647=CARTESIAN_POINT ( 'NONE',  ( 62.34828826643940403, 50.00000000000000000, -10.72527895994504199 ) ) ;
#53651=CARTESIAN_POINT ( 'NONE',  ( -15.01526311245582335, 41.97362032292153344, -85.67311622495091683 ) ) ;
#53652=CARTESIAN_POINT ( 'NONE',  ( -5.682852537008046490, 41.94661668455005810, -59.19459683319861654 ) ) ;
#53661=CARTESIAN_POINT ( 'NONE',  ( 18.71624549538633531, 50.00000000000000711, 60.97025553402504272 ) ) ;
#53670=CARTESIAN_POINT ( 'NONE',  ( 63.05051047626579219, 50.00000000000000000, -0.01845826744785798376 ) ) ;
#53673=VERTEX_POINT ( 'NONE', #7494 ) ;
#53678=VERTEX_POINT ( 'NONE', #99166 ) ;
#53705=SURFACE_STYLE_USAGE ( .BOTH. , #95766 ) ;
#53707=CARTESIAN_POINT ( 'NONE',  ( 31.59761973271792002, 40.88238628480267067, -64.13876536422311858 ) ) ;
#53712=ORIENTED_EDGE ( 'NONE', *, *, #38903, .F. ) ;
#53726=CARTESIAN_POINT ( 'NONE',  ( 9.739726766100236688, 48.00000000000000000, -87.61747884500007899 ) ) ;
#53764=EDGE_CURVE ( 'NONE', #9002, #72021, #2398, .T. ) ;
#53768=CARTESIAN_POINT ( 'NONE',  ( 7.270302578000960914, -3.659675574284857458, -18.03744543698567782 ) ) ;
#53801=CARTESIAN_POINT ( 'NONE',  ( 1.494796585009793288, -5.000000000000002665, -71.77219432632382734 ) ) ;
#53802=CARTESIAN_POINT ( 'NONE',  ( -5.892293466952475356, 42.00785640414562039, -69.46301900959564080 ) ) ;
#53806=CARTESIAN_POINT ( 'NONE',  ( 12.86717642718393151, -5.000000000000000000, -10.20629072649130009 ) ) ;
#53807=CARTESIAN_POINT ( 'NONE',  ( -5.398219627755024952, 41.68867587866067481, -58.74408776841643487 ) ) ;
#53824=CARTESIAN_POINT ( 'NONE',  ( 6.913779129928546929, 41.73441125232163529, -59.30275354417915423 ) ) ;
#53825=CARTESIAN_POINT ( 'NONE',  ( -36.40416150961017649, 41.99999999999999289, 47.37019975558912677 ) ) ;
#53836=COLOUR_RGB ( '', 0.08235294, 0.09019608, 0.10196078) ;
#53873=CARTESIAN_POINT ( 'NONE',  ( 13.14930780082191752, -5.000000000000002665, -86.33530272369397096 ) ) ;
#53877=FACE_OUTER_BOUND ( 'NONE', #50729, .T. ) ;
#53894=COLOUR_RGB ( '', 0.09019608, 0.27058824, 0.51372549) ;
#53916=CARTESIAN_POINT ( 'NONE',  ( -10.34493385746986505, -4.332661967061189223, -14.59917742215393588 ) ) ;
#53938=CARTESIAN_POINT ( 'NONE',  ( 19.47291202602108484, 49.99135632267985585, 60.38177670907871430 ) ) ;
#53942=( BOUNDED_CURVE ( )  B_SPLINE_CURVE ( 2, ( #598, #33563, #27089 ),
 .UNSPECIFIED., .F., .F. ) 
 B_SPLINE_CURVE_WITH_KNOTS ( ( 3, 3 ),
 ( 0.4303818025102752465, 1.000000000000000000 ),
 .UNSPECIFIED. ) 
 CURVE ( )  GEOMETRIC_REPRESENTATION_ITEM ( )  RATIONAL_B_SPLINE_CURVE ( ( 1.420262811277054782, 1.488244169276907503, 1.000000000000000000 ) ) 
 REPRESENTATION_ITEM ( '' )  );
#53951=ORIENTED_EDGE ( 'NONE', *, *, #22910, .F. ) ;
#53958=CARTESIAN_POINT ( 'NONE',  ( -18.96508653188647031, 49.38837234725952641, 61.98939791137838995 ) ) ;
#53959=CARTESIAN_POINT ( 'NONE',  ( 6.392921707093107919, 41.54610357469336179, -70.64273453041053585 ) ) ;
#53970=B_SPLINE_CURVE_WITH_KNOTS ( 'NONE', 3,
 ( #2960, #19736, #85497, #84956 ),
 .UNSPECIFIED., .F., .F.,
 ( 4, 4 ),
 ( 0.000000000000000000, 1.000000000000000000 ),
 .UNSPECIFIED. ) ;
#53980=CARTESIAN_POINT ( 'NONE',  ( 2.617478844991767861, -5.000000000000002665, -75.26027323389092771 ) ) ;
#54017=CARTESIAN_POINT ( 'NONE',  ( 2.354803500934600891, 50.00000000000001421, -100.0000000000000000 ) ) ;
#54026=EDGE_CURVE ( 'NONE', #31057, #86235, #34728, .T. ) ;
#54030=CARTESIAN_POINT ( 'NONE',  ( 43.64059727138994305, 41.42723139259643972, -50.50409788923168009 ) ) ;
#54037=CARTESIAN_POINT ( 'NONE',  ( 59.23741894013591036, 42.00000000000000711, -7.754160006507188285 ) ) ;
#54042=B_SPLINE_CURVE_WITH_KNOTS ( 'NONE', 3,
 ( #77922, #77387, #53635, #78970, #84946, #94656, #3501, #46088, #36442, #94100, #70362, #12108, #11036, #76845, #86568, #5095, #2950, #20802 ),
 .UNSPECIFIED., .F., .F.,
 ( 4, 2, 2, 2, 2, 2, 2, 2, 4 ),
 ( 0.000000000000000000, 0.06249999999964576253, 0.1249999999992915251, 0.1874999999989372945, 0.2499999999985830501, 0.3124999999982288057, 0.3749999999978745890, 0.4374999999975203169, 0.4999999999971661002 ),
 .UNSPECIFIED. ) ;
#54045=CARTESIAN_POINT ( 'NONE',  ( -62.40064228140166591, 39.42532419955585254, 18.44113199567702921 ) ) ;
#54080=CARTESIAN_POINT ( 'NONE',  ( 9.361783665678713007, -4.999999999999999112, -18.66271547844284484 ) ) ;
#54084=( NAMED_UNIT ( * ) PLANE_ANGLE_UNIT ( ) SI_UNIT ( $, .RADIAN. ) );
#54085=SURFACE_STYLE_FILL_AREA ( #77856 ) ;
#54094=CARTESIAN_POINT ( 'NONE',  ( -5.558537907172038217, 40.95020998767025588, -70.99752123435956719 ) ) ;
#54116=CARTESIAN_POINT ( 'NONE',  ( -12.50000000000000178, 28.79325661138934223, -46.42958547950013326 ) ) ;
#54119=EDGE_LOOP ( 'NONE', ( #93729, #96956 ) ) ;
#54130=CARTESIAN_POINT ( 'NONE',  ( 6.827804075408431927, -2.999999999999529265, -71.19745151638494463 ) ) ;
#54154=CARTESIAN_POINT ( 'NONE',  ( -22.66220480930539338, 50.00000000000000000, 59.06576954297837290 ) ) ;
#54159=CARTESIAN_POINT ( 'NONE',  ( -6.982952086341226661, 41.78396327145789257, -59.69785475644857797 ) ) ;
#54181=FILL_AREA_STYLE_COLOUR ( '', #78671 ) ;
#54212=FACE_OUTER_BOUND ( 'NONE', #37111, .T. ) ;
#54231=CARTESIAN_POINT ( 'NONE',  ( 9.999999999999994671, 48.00000000000000000, -86.30899693747679180 ) ) ;
#54234=CARTESIAN_POINT ( 'NONE',  ( 51.48757442383973881, 38.95383793068620548, -37.45149417477089315 ) ) ;
#54245=( NAMED_UNIT ( * ) PLANE_ANGLE_UNIT ( ) SI_UNIT ( $, .RADIAN. ) );
#54250=EDGE_CURVE ( 'NONE', #70585, #86317, #73253, .T. ) ;
#54269=CARTESIAN_POINT ( 'NONE',  ( -19.51721550458913512, 41.98713167543638036, -83.66826477877489765 ) ) ;
#54280=CIRCLE ( 'NONE', #35410, 60.00000000000000000 ) ;
#54308=CARTESIAN_POINT ( 'NONE',  ( -6.914762185086790858, 41.79847498657338889, -69.55926089113090427 ) ) ;
#54313=CARTESIAN_POINT ( 'NONE',  ( -6.340295924924054916, 41.77218093381596020, -58.92363190012176233 ) ) ;
#54319=CARTESIAN_POINT ( 'NONE',  ( -7.109733192396789470, 41.69026681596732686, -59.69141549319190432 ) ) ;
#54334=CARTESIAN_POINT ( 'NONE',  ( 51.76085035120648570, 42.00000000008225953, -29.83308852628573860 ) ) ;
#54340=VERTEX_POINT ( 'NONE', #28808 ) ;
#54380=CARTESIAN_POINT ( 'NONE',  ( 11.46641754970814020, -5.000000000000002665, -75.26692388747053997 ) ) ;
#54381=CARTESIAN_POINT ( 'NONE',  ( 3.490407211888509836E-12, -4.332980043422162808, 17.83347932686506354 ) ) ;
#54395=DIRECTION ( 'NONE',  ( 0.000000000000000000, 0.000000000000000000, 1.000000000000000000 ) ) ;
#54449=CARTESIAN_POINT ( 'NONE',  ( 18.93747938551456755, 49.20024086922183670, 62.06708146542941762 ) ) ;
#54459=EDGE_CURVE ( 'NONE', #67790, #17802, #12714, .T. ) ;
#54464=ORIENTED_EDGE ( 'NONE', *, *, #73366, .F. ) ;
#54472=ORIENTED_EDGE ( 'NONE', *, *, #59776, .T. ) ;
#54480=CARTESIAN_POINT ( 'NONE',  ( 5.231947904347590494, 41.12212780562299486, -70.85062122746499824 ) ) ;
#54484=CARTESIAN_POINT ( 'NONE',  ( 12.50000000000000711, -3.000000000000000000, -79.51734232575269345 ) ) ;
#54501=CARTESIAN_POINT ( 'NONE',  ( 8.737863884121436442, -3.000000000000002665, -90.03618980231149749 ) ) ;
#54502=PRESENTATION_STYLE_ASSIGNMENT (( #70187 ) ) ;
#54504=ORIENTED_EDGE ( 'NONE', *, *, #64030, .T. ) ;
#54508=B_SPLINE_CURVE_WITH_KNOTS ( 'NONE', 3,
 ( #103819, #38578, #31036, #6715 ),
 .UNSPECIFIED., .F., .F.,
 ( 4, 4 ),
 ( 0.000000000000000000, 1.000000000000000000 ),
 .UNSPECIFIED. ) ;
#54515=CARTESIAN_POINT ( 'NONE',  ( -34.19924320383960037, 42.71174251760211860, -63.48381379246026768 ) ) ;
#54531=FILL_AREA_STYLE ('',( #21697 ) ) ;
#54545=CARTESIAN_POINT ( 'NONE',  ( -37.21429643540999876, 40.15975205826806160, -56.67536727291939513 ) ) ;
#54558=CARTESIAN_POINT ( 'NONE',  ( 39.07650750593464295, 42.03392408367576394, -56.77868393786336298 ) ) ;
#54569=CARTESIAN_POINT ( 'NONE',  ( -5.022013495303277786, 18.64316884711714550, 38.36535705883633085 ) ) ;
#54574=CARTESIAN_POINT ( 'NONE',  ( -62.81225381387285722, 38.95404345811080304, -10.80315792554570109 ) ) ;
#54591=CARTESIAN_POINT ( 'NONE',  ( 7.996668422910687468, 48.00000000000000000, -78.85453279917973646 ) ) ;
#54597=PRESENTATION_STYLE_ASSIGNMENT (( #79427 ) ) ;
#54604=CARTESIAN_POINT ( 'NONE',  ( 7.435358954047280200, -4.999999999999999112, -15.55677955364923726 ) ) ;
#54643=CARTESIAN_POINT ( 'NONE',  ( -12.50000000000000533, 35.89804743376623719, -55.74191270041429647 ) ) ;
#54647=CARTESIAN_POINT ( 'NONE',  ( -4.852941176470598528, -3.000000000000002665, -70.80672828634229177 ) ) ;
#54662=CARTESIAN_POINT ( 'NONE',  ( 7.499999999943863571, 33.41357786079682768, -51.06910100954272735 ) ) ;
#54689=CARTESIAN_POINT ( 'NONE',  ( 62.59524157948160905, 49.99999999997998401, 18.50207713769105311 ) ) ;
#54693=ADVANCED_FACE ( 'NONE', ( #20403 ), #59986, .T. ) ;
#54695=CARTESIAN_POINT ( 'NONE',  ( 12.13202714166731155, -4.667418019610191315, -76.82053255073324749 ) ) ;
#54702=CARTESIAN_POINT ( 'NONE',  ( 19.11706402096854873, 50.00000000000000711, 60.42677271361581148 ) ) ;
#54714=CARTESIAN_POINT ( 'NONE',  ( 62.27995339080301562, 50.00000000000000711, 9.818926026722518685 ) ) ;
#54736=MANIFOLD_SOLID_BREP ( 'Fillet3', #42920 ) ;
#54744=CARTESIAN_POINT ( 'NONE',  ( 7.126148245860624009, 41.12758397993106740, -58.55282951229289523 ) ) ;
#54750=CARTESIAN_POINT ( 'NONE',  ( 17.50000000000002487, 46.94999999999998153, 62.61746187599675295 ) ) ;
#54769=CARTESIAN_POINT ( 'NONE',  ( 7.996668422910687468, 48.00000000000000000, -78.85453279917973646 ) ) ;
#54786=SURFACE_SIDE_STYLE ('',( #21936 ) ) ;
#54793=CARTESIAN_POINT ( 'NONE',  ( 8.000000000000000000, -4.999999999999998224, -2.094395098902536834 ) ) ;
#54815=CARTESIAN_POINT ( 'NONE',  ( -17.75781974272246444, 50.00000000000000000, 62.25693441398608741 ) ) ;
#54823=SURFACE_STYLE_USAGE ( .BOTH. , #95838 ) ;
#54852=CARTESIAN_POINT ( 'NONE',  ( -6.192998293236303908, 41.95244004339406274, -69.88363007943512173 ) ) ;
#54865=CARTESIAN_POINT ( 'NONE',  ( -6.738100187484505454, 41.71798639774085160, -59.05424569925489209 ) ) ;
#54886=AXIS2_PLACEMENT_3D ( 'NONE', #40355, #98057, #72198 ) ;
#54932=CARTESIAN_POINT ( 'NONE',  ( 10.00000000000000000, -5.000000000000000000, 2.617993873628172263 ) ) ;
#54937=SURFACE_STYLE_FILL_AREA ( #80812 ) ;
#54968=ORIENTED_EDGE ( 'NONE', *, *, #56763, .F. ) ;
#54991=VERTEX_POINT ( 'NONE', #49243 ) ;
#54992=CARTESIAN_POINT ( 'NONE',  ( 18.93607640110042212, 49.18420685015853167, 62.07208393010721892 ) ) ;
#55014=CARTESIAN_POINT ( 'NONE',  ( -19.40660811090403826, 49.94503873469690092, 60.93944725389842176 ) ) ;
#55022=CARTESIAN_POINT ( 'NONE',  ( 10.50000000000000000, -5.000000000000000000, -8.595933841506987250 ) ) ;
#55040=CARTESIAN_POINT ( 'NONE',  ( 6.145467200820246667, -3.000000000000002665, -92.99666842291070168 ) ) ;
#55052=CARTESIAN_POINT ( 'NONE',  ( 6.904524730080239259, -5.000000000010798473, -16.27804637754277550 ) ) ;
#55093=CARTESIAN_POINT ( 'NONE',  ( 36.39385630396220250, 42.41148509302271208, -60.46671959672418950 ) ) ;
#55098=B_SPLINE_CURVE_WITH_KNOTS ( 'NONE', 3,
 ( #65998, #105912, #41193, #90815, #74078, #163, #40130, #49808, #73008, #98873 ),
 .UNSPECIFIED., .F., .F.,
 ( 4, 2, 2, 2, 4 ),
 ( 0.000000000000000000, 0.2500000000000000000, 0.5000000000000000000, 0.7500000000000000000, 1.000000000000000000 ),
 .UNSPECIFIED. ) ;
#55105=CARTESIAN_POINT ( 'NONE',  ( 7.754160006507071046, 42.00000000000000711, -59.23741894013591036 ) ) ;
#55112=CARTESIAN_POINT ( 'NONE',  ( 52.56491209535275289, 39.42572890907100458, -38.23519342730396176 ) ) ;
#55130=CARTESIAN_POINT ( 'NONE',  ( 1.224646799147352073E-15, 49.99999999999999289, -75.00000000000001421 ) ) ;
#55145=CARTESIAN_POINT ( 'NONE',  ( 6.229963766635606248, -5.000000000000000000, -15.35262140457759727 ) ) ;
#55150=FACE_OUTER_BOUND ( 'NONE', #68557, .T. ) ;
#55169=CARTESIAN_POINT ( 'NONE',  ( -18.44955509589851061, 45.00000000000001421, 62.33994477147084723 ) ) ;
#55181=CARTESIAN_POINT ( 'NONE',  ( -12.50000000000000355, 41.59226156894883530, -76.70843802411151557 ) ) ;
#55191=CARTESIAN_POINT ( 'NONE',  ( 7.176875381352203931, 41.55694707671359112, -59.30926837872168988 ) ) ;
#55212=CARTESIAN_POINT ( 'NONE',  ( 5.500000000000006217, 42.00000000000000000, -58.69229087761227248 ) ) ;
#55226=CARTESIAN_POINT ( 'NONE',  ( 42.35263604940418958, 50.00000000000000000, 46.99568999590452734 ) ) ;
#55238=CARTESIAN_POINT ( 'NONE',  ( 18.33022316120833750, 50.00000000000000000, 61.47368443700771934 ) ) ;
#55249=CARTESIAN_POINT ( 'NONE',  ( 62.90157831112001929, 50.00000000000000000, -3.733503276916400715 ) ) ;
#55263=MECHANICAL_DESIGN_GEOMETRIC_PRESENTATION_REPRESENTATION('',(#48327),#10457);
#55284=CARTESIAN_POINT ( 'NONE',  ( -9.609938133626268808, -5.000000000000000000, -77.63956163934031451 ) ) ;
#55294=CARTESIAN_POINT ( 'NONE',  ( 52.56483885390522914, 40.83906611471594061, -38.23529411764711483 ) ) ;
#55301=CARTESIAN_POINT ( 'NONE',  ( -8.737863884121431113, 48.00000000000000000, -79.96381019768850251 ) ) ;
#55315=VERTEX_POINT ( 'NONE', #83610 ) ;
#55317=( NAMED_UNIT ( * ) SI_UNIT ( $, .STERADIAN. ) SOLID_ANGLE_UNIT ( ) );
#55323=CARTESIAN_POINT ( 'NONE',  ( -8.000000000000000000, -4.999999999999998224, 2.094395098902548824 ) ) ;
#55342=CARTESIAN_POINT ( 'NONE',  ( -27.00467402917412585, 41.40534817802205936, -70.25900587838104627 ) ) ;
#55343=CARTESIAN_POINT ( 'NONE',  ( -18.15598277398370541, 50.00000000000001421, 61.69040288260701033 ) ) ;
#55350=CARTESIAN_POINT ( 'NONE',  ( 17.50000000000004974, 49.99999999999836575, 59.91915230424464767 ) ) ;
#55352=COLOUR_RGB ( '', 0.09019608, 0.27058824, 0.51372549) ;
#55357=CARTESIAN_POINT ( 'NONE',  ( -7.499994653025497726, -2.925861026131086007, -20.99866594782981011 ) ) ;
#55381=PRESENTATION_STYLE_ASSIGNMENT (( #22539 ) ) ;
#55394=CARTESIAN_POINT ( 'NONE',  ( -21.23076943214345391, 18.64284798593011061, 32.03398753740776783 ) ) ;
#55449=DIRECTION ( 'NONE',  ( 0.000000000000000000, 0.000000000000000000, 1.000000000000000000 ) ) ;
#55453=CARTESIAN_POINT ( 'NONE',  ( 17.11334244676965000, -4.333298119783723479, -5.314533759803898860 ) ) ;
#55458=CARTESIAN_POINT ( 'NONE',  ( 8.000000000000000000, -4.999999999999998224, -2.094395098902536834 ) ) ;
#55514=CARTESIAN_POINT ( 'NONE',  ( 19.09871521262170546, 49.67080660516045043, 61.74181558515030588 ) ) ;
#55540=CARTESIAN_POINT ( 'NONE',  ( -19.48790983171578617, 49.99824972418149116, 60.16135127412848504 ) ) ;
#55553=EDGE_CURVE ( 'NONE', #37125, #19635, #35882, .T. ) ;
#55564=CARTESIAN_POINT ( 'NONE',  ( -2.617478844992338516, -5.000000000000015099, -94.73972676610841859 ) ) ;
#55574=CARTESIAN_POINT ( 'NONE',  ( 7.500141383065412448, -5.000000000000024869, -20.99866593659988823 ) ) ;
#55576=CARTESIAN_POINT ( 'NONE',  ( -7.360624614890398654, 50.00000000000001421, -94.61012438779899014 ) ) ;
#55589=CARTESIAN_POINT ( 'NONE',  ( -6.828042834505471781, 41.63841151066672808, -58.95291702778770571 ) ) ;
#55597=DIRECTION ( 'NONE',  ( 0.000000000000000000, 0.000000000000000000, 1.000000000000000000 ) ) ;
#55604=UNCERTAINTY_MEASURE_WITH_UNIT (LENGTH_MEASURE( 1.000000000000000082E-05 ), #29536, 'distance_accuracy_value', 'NONE');
#55613=SURFACE_STYLE_FILL_AREA ( #19 ) ;
#55628=CARTESIAN_POINT ( 'NONE',  ( 43.67028230287913004, 39.42405813808058923, 48.51753365052933020 ) ) ;
#55647=CARTESIAN_POINT ( 'NONE',  ( -5.036189802313092656, 48.00000000000000000, -93.73786388412078452 ) ) ;
#55653=( LENGTH_UNIT ( ) NAMED_UNIT ( * ) SI_UNIT ( .MILLI., .METRE. ) );
#55661=CARTESIAN_POINT ( 'NONE',  ( 8.435052862587294698, -4.999999999999999112, -16.32561095844542720 ) ) ;
#55673=CARTESIAN_POINT ( 'NONE',  ( 9.500000000000003553, -5.000000000000000000, -68.91429205785459544 ) ) ;
#55691=CARTESIAN_POINT ( 'NONE',  ( 7.126323127734462304, 41.48433382013136139, -70.04207035317314478 ) ) ;
#55698=CARTESIAN_POINT ( 'NONE',  ( -12.50000000000000355, 34.57130022983270834, -53.73004006193110627 ) ) ;
#55729=CARTESIAN_POINT ( 'NONE',  ( 7.500000000000007105, 40.00000000000000000, -58.69229087761227248 ) ) ;
#55740=CARTESIAN_POINT ( 'NONE',  ( -60.62677696746660416, 49.99999999999999289, 24.18439665019479179 ) ) ;
#55754=CARTESIAN_POINT ( 'NONE',  ( 18.11660520461541068, 50.00000000000000711, 61.73928013098095846 ) ) ;
#55756=EDGE_CURVE ( 'NONE', #5970, #89905, #49957, .T. ) ;
#55771=CARTESIAN_POINT ( 'NONE',  ( -12.50000000000000178, -1.322513981592677412, -16.28752265597966087 ) ) ;
#55788=DIRECTION ( 'NONE',  ( 0.000000000000000000, 0.000000000000000000, 1.000000000000000000 ) ) ;
#55794=ORIENTED_EDGE ( 'NONE', *, *, #45173, .F. ) ;
#55828=EDGE_CURVE ( 'NONE', #78737, #61410, #76894, .T. ) ;
#55837=CARTESIAN_POINT ( 'NONE',  ( -2.617993873628327250, -5.000000000000000000, 10.00000000000000000 ) ) ;
#55863=CARTESIAN_POINT ( 'NONE',  ( 17.50000000000004974, 51.99999999999999289, 59.86364615470024830 ) ) ;
#55872=CARTESIAN_POINT ( 'NONE',  ( -5.079306836894615707, -4.308466644846057569, -17.11871833148123301 ) ) ;
#55919=CARTESIAN_POINT ( 'NONE',  ( 6.570529166336707583, 41.93002594905234304, -59.71599377568048794 ) ) ;
#55935=ORIENTED_EDGE ( 'NONE', *, *, #5503, .T. ) ;
#55946=EDGE_CURVE ( 'NONE', #106540, #91293, #35666, .T. ) ;
#55961=CARTESIAN_POINT ( 'NONE',  ( -12.49999999999998757, -3.165118404322636803, -76.70900766830885686 ) ) ;
#55962=UNCERTAINTY_MEASURE_WITH_UNIT (LENGTH_MEASURE( 1.000000000000000082E-05 ), #19870, 'distance_accuracy_value', 'NONE');
#55979=CARTESIAN_POINT ( 'NONE',  ( -5.219866590718559962, -5.000000000000000000, 8.922269033012391048 ) ) ;
#55984=CARTESIAN_POINT ( 'NONE',  ( -12.50000000000000000, -3.000000000000000000, -11.21398294031087062 ) ) ;
#55985=CARTESIAN_POINT ( 'NONE',  ( 10.47796581435272145, -5.000000000000000000, -91.06180813480403913 ) ) ;
#55987=CARTESIAN_POINT ( 'NONE',  ( 5.363597346073513350, 41.33266196706048845, -58.39526881795627844 ) ) ;
#56022=CARTESIAN_POINT ( 'NONE',  ( 9.235395886531431551E-16, -3.000000000000000000, -8.000000000000000000 ) ) ;
#56042=CARTESIAN_POINT ( 'NONE',  ( 19.46222512963864304, 49.98514627502216712, 60.50669264090301880 ) ) ;
#56069=SURFACE_STYLE_FILL_AREA ( #88484 ) ;
#56085=CARTESIAN_POINT ( 'NONE',  ( -18.91791044776116237, 44.85000000000000853, 62.18611311450883505 ) ) ;
#56097=CARTESIAN_POINT ( 'NONE',  ( 12.44963615882576491, -4.333246069852155991, -12.76855431082354997 ) ) ;
#56099=CARTESIAN_POINT ( 'NONE',  ( 7.731157688189080446, -4.999999999993458566, -17.87147387709585900 ) ) ;
#56102=CARTESIAN_POINT ( 'NONE',  ( -42.46496487705343270, 41.57317828158753059, -52.12032522017845082 ) ) ;
#56132=CARTESIAN_POINT ( 'NONE',  ( -11.99999999999999467, -5.000000000000002665, -86.57079632497431021 ) ) ;
#56146=CARTESIAN_POINT ( 'NONE',  ( -11.20285577171231139, -4.999999999999999112, -78.29797948823949127 ) ) ;
#56175=CARTESIAN_POINT ( 'NONE',  ( 5.036189802309444907, 49.99999999999999289, -76.26213611588271135 ) ) ;
#56181=CARTESIAN_POINT ( 'NONE',  ( -14.90155535903825701, 42.58002643001272958, -90.01374837838967835 ) ) ;
#56190=CARTESIAN_POINT ( 'NONE',  ( 6.144360409390458244, -5.000000000000002665, -15.35739152976048594 ) ) ;
#56205=VERTEX_POINT ( 'NONE', #65335 ) ;
#56215=CARTESIAN_POINT ( 'NONE',  ( 7.013017687956457635, 40.92324830026397819, -70.84400559921924412 ) ) ;
#56218=CARTESIAN_POINT ( 'NONE',  ( -7.251493771303348268, 41.03131504527001283, -58.65725810227473858 ) ) ;
#56224=CARTESIAN_POINT ( 'NONE',  ( -12.50000000000000711, 30.94869521958284864, -48.87257972625063474 ) ) ;
#56238=CARTESIAN_POINT ( 'NONE',  ( 7.251694438969768619, 41.54830556103024719, -59.82648080958256287 ) ) ;
#56266=CARTESIAN_POINT ( 'NONE',  ( 5.957442974983132800, 40.83906611472426817, 64.99999999999700151 ) ) ;
#56270=CARTESIAN_POINT ( 'NONE',  ( -50.94745919686192082, 50.00000000000000000, -37.05882352941185331 ) ) ;
#56338=CARTESIAN_POINT ( 'NONE',  ( -1.591643166418952315, -5.000000000000000000, -73.00000000000002842 ) ) ;
#56345=CARTESIAN_POINT ( 'NONE',  ( 31.48004117150884085, 41.29391029462509266, -67.22209853552702441 ) ) ;
#56374=CARTESIAN_POINT ( 'NONE',  ( 0.000000000000000000, -4.999999999999998224, 8.000000000000000000 ) ) ;
#56404=CARTESIAN_POINT ( 'NONE',  ( 17.50000000000308020, 49.96115704435360527, 61.85088014401689094 ) ) ;
#56409=CARTESIAN_POINT ( 'NONE',  ( 4.205882352941182845, -5.000000000000000000, -72.69916451482998809 ) ) ;
#56415=CARTESIAN_POINT ( 'NONE',  ( -4.903611268973031123, -5.000000000000039968, -16.52575844349512835 ) ) ;
#56470=CARTESIAN_POINT ( 'NONE',  ( 6.771647573939279852, 41.86512692430649452, -59.59160515849491446 ) ) ;
#56480=CARTESIAN_POINT ( 'NONE',  ( 1.833333333264058229, 42.00000000000000000, -60.21711271837359902 ) ) ;
#56485=( LENGTH_UNIT ( ) NAMED_UNIT ( * ) SI_UNIT ( .MILLI., .METRE. ) );
#56486=ORIENTED_EDGE ( 'NONE', *, *, #80167, .T. ) ;
#56521=( NAMED_UNIT ( * ) PLANE_ANGLE_UNIT ( ) SI_UNIT ( $, .RADIAN. ) );
#56527=FILL_AREA_STYLE_COLOUR ( '', #104857 ) ;
#56533=( GEOMETRIC_REPRESENTATION_CONTEXT ( 3 ) GLOBAL_UNCERTAINTY_ASSIGNED_CONTEXT ( ( #83915 ) ) GLOBAL_UNIT_ASSIGNED_CONTEXT ( ( #62526, #56521, #23139 ) ) REPRESENTATION_CONTEXT ( 'NONE', 'WORKASPACE' ) );
#56562=CARTESIAN_POINT ( 'NONE',  ( 7.157960986247998925, -5.000000000000000000, -14.69147069243657100 ) ) ;
#56604=CARTESIAN_POINT ( 'NONE',  ( 5.415856237588537958, 41.85405046271414875, -58.97635192936115800 ) ) ;
#56627=CARTESIAN_POINT ( 'NONE',  ( -6.390922558478501436, -4.999999999999999112, -15.34850256275529112 ) ) ;
#56649=CARTESIAN_POINT ( 'NONE',  ( -39.01859936591235112, 42.04209281348008176, -56.85829446836521583 ) ) ;
#56657=STYLED_ITEM ( 'NONE', ( #96697 ), #33066 ) ;
#56659=CARTESIAN_POINT ( 'NONE',  ( -43.69716417776824358, 40.83906611472755088, 48.48761666261796677 ) ) ;
#56666=CARTESIAN_POINT ( 'NONE',  ( -6.931554132395168821, -5.000000000000945022, -71.13906995425499247 ) ) ;
#56678=CARTESIAN_POINT ( 'NONE',  ( -23.97670849968361395, 41.62117736604113816, -74.33761154807883997 ) ) ;
#56685=CARTESIAN_POINT ( 'NONE',  ( 9.596002107491598210, -5.000000000000002665, -92.37456064098007857 ) ) ;
#56687=MECHANICAL_DESIGN_GEOMETRIC_PRESENTATION_REPRESENTATION('',(#103226),#5059);
#56698=CARTESIAN_POINT ( 'NONE',  ( -12.12948968253070881, -5.000000000000000000, -89.82632555826474174 ) ) ;
#56704=CARTESIAN_POINT ( 'NONE',  ( -14.49391709338271816, 38.95396881702665581, 62.06433840696379178 ) ) ;
#56722=CARTESIAN_POINT ( 'NONE',  ( -10.59260543037239799, -5.000000000000000000, -12.53864087336843447 ) ) ;
#56734=( GEOMETRIC_REPRESENTATION_CONTEXT ( 3 ) GLOBAL_UNCERTAINTY_ASSIGNED_CONTEXT ( ( #78496 ) ) GLOBAL_UNIT_ASSIGNED_CONTEXT ( ( #97084, #16704, #84631 ) ) REPRESENTATION_CONTEXT ( 'NONE', 'WORKASPACE' ) );
#56739=CARTESIAN_POINT ( 'NONE',  ( -52.56491209535032993, 39.42572890908718364, -38.23519342730719472 ) ) ;
#56740=CARTESIAN_POINT ( 'NONE',  ( -7.054523059426879961, 41.71556238290650498, -59.55896278357374030 ) ) ;
#56760=CARTESIAN_POINT ( 'NONE',  ( 7.071721972134253242, 41.30029428951767301, -70.42654619687203876 ) ) ;
#56763=EDGE_CURVE ( 'NONE', #78737, #37873, #22809, .T. ) ;
#56769=CARTESIAN_POINT ( 'NONE',  ( -5.787521267941007963, 41.99999999999999289, -59.87256577776128097 ) ) ;
#56784=CARTESIAN_POINT ( 'NONE',  ( 34.12287332558704378, 18.64284798592593262, -17.67912453243325999 ) ) ;
#56792=B_SPLINE_CURVE_WITH_KNOTS ( 'NONE', 3,
 ( #76647, #77192, #2758, #61561 ),
 .UNSPECIFIED., .F., .F.,
 ( 4, 4 ),
 ( 0.000000000000000000, 1.000000000000000000 ),
 .UNSPECIFIED. ) ;
#56794=PRODUCT_CONTEXT ( 'NONE', #71366, 'mechanical' ) ;
#56803=( NAMED_UNIT ( * ) SI_UNIT ( $, .STERADIAN. ) SOLID_ANGLE_UNIT ( ) );
#56821=ORIENTED_EDGE ( 'NONE', *, *, #8268, .F. ) ;
#56827=CARTESIAN_POINT ( 'NONE',  ( -6.457005523775564804, 41.52802923939503899, -70.63630686657118929 ) ) ;
#56877=STYLED_ITEM ( 'NONE', ( #43224 ), #46730 ) ;
#56898=CARTESIAN_POINT ( 'NONE',  ( 39.12903940704961769, 38.95383793072134182, 50.91589357078481726 ) ) ;
#56911=CARTESIAN_POINT ( 'NONE',  ( 7.137815226410046066, -3.000000000000000000, 4.175893272574714210 ) ) ;
#56930=( LENGTH_UNIT ( ) NAMED_UNIT ( * ) SI_UNIT ( .MILLI., .METRE. ) );
#56938=CARTESIAN_POINT ( 'NONE',  ( 17.50000000000007105, 48.00000000000682832, 64.09945636502658317 ) ) ;
#56950=CARTESIAN_POINT ( 'NONE',  ( -6.618366600633001084, -4.380080200176828420, -16.79229307443615582 ) ) ;
#56963=CARTESIAN_POINT ( 'NONE',  ( 0.000000000000000000, 45.00000000000000711, 65.00000000000000000 ) ) ;
#56977=CARTESIAN_POINT ( 'NONE',  ( 55.22048556082879145, 50.00000000002004441, 34.80214219306057544 ) ) ;
#57029=( GEOMETRIC_REPRESENTATION_CONTEXT ( 3 ) GLOBAL_UNCERTAINTY_ASSIGNED_CONTEXT ( ( #43003 ) ) GLOBAL_UNIT_ASSIGNED_CONTEXT ( ( #26301, #42429, #11647 ) ) REPRESENTATION_CONTEXT ( 'NONE', 'WORKASPACE' ) );
#57031=ORIENTED_EDGE ( 'NONE', *, *, #45167, .T. ) ;
#57033=DIRECTION ( 'NONE',  ( 0.000000000000000000, 0.000000000000000000, 1.000000000000000000 ) ) ;
#57057=CARTESIAN_POINT ( 'NONE',  ( -7.137815226412437930, -4.999999999998865796, -4.175893272574592530 ) ) ;
#57059=DIRECTION ( 'NONE',  ( 0.000000000000000000, 0.000000000000000000, 1.000000000000000000 ) ) ;
#57064=CARTESIAN_POINT ( 'NONE',  ( -12.50000000000000178, -3.000000000000000000, -34.12705337366766400 ) ) ;
#57065=CARTESIAN_POINT ( 'NONE',  ( 11.99986829839165203, -5.000000000000000000, -83.40936345626406023 ) ) ;
#57090=LINE ( 'NONE', #58714, #104616 ) ;
#57121=CARTESIAN_POINT ( 'NONE',  ( -6.738100187484505454, 41.71798639774085160, -59.05424569925489209 ) ) ;
#57128=MECHANICAL_DESIGN_GEOMETRIC_PRESENTATION_REPRESENTATION('',(#93335),#91577);
#57152=CARTESIAN_POINT ( 'NONE',  ( 18.01087898364460216, 44.99999999999999289, 62.56010773621230214 ) ) ;
#57167=( LENGTH_UNIT ( ) NAMED_UNIT ( * ) SI_UNIT ( .MILLI., .METRE. ) );
#57176=CARTESIAN_POINT ( 'NONE',  ( 5.686850908482750988, -4.337623088852442521, -16.91150612930258035 ) ) ;
#57178=CARTESIAN_POINT ( 'NONE',  ( -6.061707334783565493, 50.00000000000000000, -95.47772246151531306 ) ) ;
#57187=CARTESIAN_POINT ( 'NONE',  ( -39.04923757955551622, 40.83906611472718140, 52.30342408729326564 ) ) ;
#57191=CARTESIAN_POINT ( 'NONE',  ( -17.49999999999978684, 49.99999999999968026, 59.86364615470553474 ) ) ;
#57205=CARTESIAN_POINT ( 'NONE',  ( -24.08450779687392895, 41.61345875976761732, -74.19243768968262032 ) ) ;
#57211=CARTESIAN_POINT ( 'NONE',  ( 6.043427762770655853, -5.000000000000002665, -95.48543666094731464 ) ) ;
#57232=VERTEX_POINT ( 'NONE', #30898 ) ;
#57233=CARTESIAN_POINT ( 'NONE',  ( -48.74182829061921041, 38.95314221987509029, 41.06628751931371113 ) ) ;
#57267=CARTESIAN_POINT ( 'NONE',  ( -6.866539648855182421, 41.67963793714291398, -59.06571870949380809 ) ) ;
#57299=CARTESIAN_POINT ( 'NONE',  ( -24.21469879905009392, 50.00000000000000000, 58.37456082337698149 ) ) ;
#57312=CARTESIAN_POINT ( 'NONE',  ( 7.484880573657958003, 40.61738193562707977, -59.44022980582506221 ) ) ;
#57328=CARTESIAN_POINT ( 'NONE',  ( 12.13034742782337538, 42.00000149833409324, -93.82352941176404215 ) ) ;
#57334=CARTESIAN_POINT ( 'NONE',  ( -4.205882352941162416, -5.000000000000000000, -72.69916451482997388 ) ) ;
#57335=CARTESIAN_POINT ( 'NONE',  ( 11.91432047162523311, 40.83906611472392001, 64.17585289265115023 ) ) ;
#57352=FILL_AREA_STYLE ('',( #65471 ) ) ;
#57384=CARTESIAN_POINT ( 'NONE',  ( -2.354743324221993728, 47.99999999999999289, -99.86073547176457055 ) ) ;
#57388=CARTESIAN_POINT ( 'NONE',  ( -7.150000000000003908, 41.64999999999997726, -68.91429205801804869 ) ) ;
#57419=ORIENTED_EDGE ( 'NONE', *, *, #12175, .T. ) ;
#57422=STYLED_ITEM ( 'NONE', ( #36571 ), #54693 ) ;
#57432=B_SPLINE_CURVE_WITH_KNOTS ( 'NONE', 3,
 ( #40917, #31269, #64153, #72738 ),
 .UNSPECIFIED., .F., .F.,
 ( 4, 4 ),
 ( 0.4999999999999996114, 1.000000000000000000 ),
 .UNSPECIFIED. ) ;
#57469=CARTESIAN_POINT ( 'NONE',  ( 17.50000000000261124, 50.02580020274679384, 60.61389435659040004 ) ) ;
#57477=CARTESIAN_POINT ( 'NONE',  ( -6.735051087780404622, -4.346205982504359078, -16.86563398496736710 ) ) ;
#57528=CARTESIAN_POINT ( 'NONE',  ( 23.96490998088334479, 41.62201801232857434, -74.35350452741216998 ) ) ;
#57542=ADVANCED_FACE ( 'NONE', ( #77171 ), #31007, .T. ) ;
#57583=CARTESIAN_POINT ( 'NONE',  ( -17.49999999999997158, 48.39190472549704936, 64.09945637329882118 ) ) ;
#57585=CARTESIAN_POINT ( 'NONE',  ( -12.50000000000000533, -3.000000000000000000, -55.73109925765190553 ) ) ;
#57618=EDGE_CURVE ( 'NONE', #74620, #45703, #79171, .T. ) ;
#57660=CARTESIAN_POINT ( 'NONE',  ( 5.897541335056488698, 41.82858996958378128, -58.91931118675405799 ) ) ;
#57664=EDGE_CURVE ( 'NONE', #99282, #45623, #7990, .T. ) ;
#57671=FACE_OUTER_BOUND ( 'NONE', #41333, .T. ) ;
#57678=ORIENTED_EDGE ( 'NONE', *, *, #18042, .F. ) ;
#57684=CARTESIAN_POINT ( 'NONE',  ( -9.368151975306767909, -4.999999999999999112, -18.70424021566291373 ) ) ;
#57700=CARTESIAN_POINT ( 'NONE',  ( -10.71924530989230107, -3.000000000000002665, -74.44967652503967770 ) ) ;
#57719=CARTESIAN_POINT ( 'NONE',  ( -17.50000000000511235, 49.61376050340021493, 62.33429930757461790 ) ) ;
#57733=CARTESIAN_POINT ( 'NONE',  ( -34.80075338857600542, 40.47836787973446349, -59.87678982950887274 ) ) ;
#57739=CARTESIAN_POINT ( 'NONE',  ( -11.99999999999999467, -5.000000000000002665, -83.42920367502566137 ) ) ;
#57740=CARTESIAN_POINT ( 'NONE',  ( -7.063836241042545261, 41.16939184123525308, -58.51214979689661533 ) ) ;
#57743=CARTESIAN_POINT ( 'NONE',  ( 7.500000000000005329, 24.91666666666666430, -68.91429205785459544 ) ) ;
#57756=CARTESIAN_POINT ( 'NONE',  ( 10.50000000000000711, -5.000000000000000000, -77.33514508527181874 ) ) ;
#57763=CARTESIAN_POINT ( 'NONE',  ( 59.21693087040298309, 38.95252063249746044, 23.56881319470565828 ) ) ;
#57804=CARTESIAN_POINT ( 'NONE',  ( 6.960057398333424850, 40.00000000387299082, -71.11869238929793369 ) ) ;
#57824=CARTESIAN_POINT ( 'NONE',  ( -7.461257001076914364, 40.57433524249821488, -59.19359852711440340 ) ) ;
#57829=VERTEX_POINT ( 'NONE', #70083 ) ;
#57839=VERTEX_POINT ( 'NONE', #95419 ) ;
#57841=CARTESIAN_POINT ( 'NONE',  ( 16.68184208837833538, 18.64284798592490944, -34.62135284424456927 ) ) ;
#57848=ADVANCED_FACE ( 'NONE', ( #63604 ), #14473, .T. ) ;
#57858=CARTESIAN_POINT ( 'NONE',  ( 1.262844703064978993E-15, -3.000000000000002665, -95.00000000000000000 ) ) ;
#57859=CARTESIAN_POINT ( 'NONE',  ( 12.13034742782246767, 42.00000000000000000, -93.82352941176338845 ) ) ;
#57873=STYLED_ITEM ( 'NONE', ( #28125 ), #57542 ) ;
#57876=CARTESIAN_POINT ( 'NONE',  ( -54.34415824576156950, 50.00000000000000000, -32.38913437803946493 ) ) ;
#57887=( NAMED_UNIT ( * ) PLANE_ANGLE_UNIT ( ) SI_UNIT ( $, .RADIAN. ) );
#57891=EDGE_CURVE ( 'NONE', #45623, #99282, #92370, .T. ) ;
#57920=CARTESIAN_POINT ( 'NONE',  ( -6.872826227116265230, 41.26098032275474026, -70.68506212612362560 ) ) ;
#57929=CARTESIAN_POINT ( 'NONE',  ( -8.716576110315918058, -5.000000000000000000, 5.062272329162047946 ) ) ;
#57952=CARTESIAN_POINT ( 'NONE',  ( 12.50000000000000711, 33.88168340297682590, -52.67689954243009964 ) ) ;
#57956=CARTESIAN_POINT ( 'NONE',  ( -7.036764705882382565, 40.00000000007575807, -71.06385277390852195 ) ) ;
#57964=ORIENTED_EDGE ( 'NONE', *, *, #105868, .F. ) ;
#57969=CARTESIAN_POINT ( 'NONE',  ( 17.50000000000002842, 49.00623182211167972, 64.05145124195381356 ) ) ;
#57991=FILL_AREA_STYLE_COLOUR ( '', #93921 ) ;
#57997=CARTESIAN_POINT ( 'NONE',  ( 5.668940197363838251, 41.88723871811491506, -59.02759513106027356 ) ) ;
#58003=CARTESIAN_POINT ( 'NONE',  ( 16.52731600354976393, 43.98685737190850631, -87.77869701378344303 ) ) ;
#58008=CARTESIAN_POINT ( 'NONE',  ( 18.91772294278459654, 48.00000000000000000, 62.18609455171460354 ) ) ;
#58011=CARTESIAN_POINT ( 'NONE',  ( -6.511374603264941996, 41.81948973637988587, -59.12906223371311398 ) ) ;
#58015=CARTESIAN_POINT ( 'NONE',  ( -5.689604056833319490, -4.325321803341545923, -16.92223617909959898 ) ) ;
#58045=CARTESIAN_POINT ( 'NONE',  ( -28.89099332390824770, 48.00000000000000000, 58.53034795347328867 ) ) ;
#58075=VERTEX_POINT ( 'NONE', #55987 ) ;
#58085=ORIENTED_EDGE ( 'NONE', *, *, #55756, .T. ) ;
#58087=SURFACE_STYLE_USAGE ( .BOTH. , #346 ) ;
#58173=CARTESIAN_POINT ( 'NONE',  ( -18.91781669292785395, 48.00000000000000000, 62.18610382930904734 ) ) ;
#58176=CARTESIAN_POINT ( 'NONE',  ( -1.841875822471433519E-14, -3.000000000000002665, -70.00227127314062159 ) ) ;
#58199=CARTESIAN_POINT ( 'NONE',  ( -72.41885610115926397, 42.00000000000000000, -55.65414010186705696 ) ) ;
#58224=CARTESIAN_POINT ( 'NONE',  ( 17.60863369925912991, 45.00000000000000711, 63.07564956641097353 ) ) ;
#58229=CARTESIAN_POINT ( 'NONE',  ( -6.367479334539770441, -4.999999999999999112, -15.34856421866666665 ) ) ;
#58247=CARTESIAN_POINT ( 'NONE',  ( 4.651269564039822946, -4.999999999999991118, -15.66707428873065311 ) ) ;
#58249=( NAMED_UNIT ( * ) SI_UNIT ( $, .STERADIAN. ) SOLID_ANGLE_UNIT ( ) );
#58250=CARTESIAN_POINT ( 'NONE',  ( -43.54683447650032946, 41.43851002137547823, -50.63300042071738005 ) ) ;
#58270=CARTESIAN_POINT ( 'NONE',  ( -17.49999999999995737, 48.29516379691337136, 64.09945637126308782 ) ) ;
#58274=EDGE_LOOP ( 'NONE', ( #16649, #61987, #61694, #100876 ) ) ;
#58283=CARTESIAN_POINT ( 'NONE',  ( -24.94875383206915487, 41.54882598256691040, -73.03065563107891478 ) ) ;
#58290=CARTESIAN_POINT ( 'NONE',  ( 7.374560640984048732, -5.000000000000002665, -75.40399789250147933 ) ) ;
#58300=ORIENTED_EDGE ( 'NONE', *, *, #59223, .F. ) ;
#58314=CARTESIAN_POINT ( 'NONE',  ( 63.58085507674907433, 38.95394049974004247, 6.694916254277349488 ) ) ;
#58417=CARTESIAN_POINT ( 'NONE',  ( -7.500000000000004441, 9.833333333333344584, -71.71180648257555390 ) ) ;
#58468=CARTESIAN_POINT ( 'NONE',  ( -12.49198003592475459, -3.425909553771215865, -13.84024797512535088 ) ) ;
#58469=CARTESIAN_POINT ( 'NONE',  ( 11.43775816216263053, 48.00000000000000000, -94.77568223238719725 ) ) ;
#58470=B_SPLINE_CURVE_WITH_KNOTS ( 'NONE', 3,
 ( #11028, #52028, #59615, #75777, #67167, #75231, #43421, #50952 ),
 .UNSPECIFIED., .F., .F.,
 ( 4, 2, 2, 4 ),
 ( 0.000000000000000000, 0.4999999999999997780, 0.7499999999999998890, 1.000000000000000000 ),
 .UNSPECIFIED. ) ;
#58473=CARTESIAN_POINT ( 'NONE',  ( -6.978962160530237213, 41.42610738227783429, -70.37780172426575120 ) ) ;
#58510=CARTESIAN_POINT ( 'NONE',  ( 12.50000000000000888, 22.13452033257601315, -39.57065185985111100 ) ) ;
#58519=VERTEX_POINT ( 'NONE', #64525 ) ;
#58571=CARTESIAN_POINT ( 'NONE',  ( -6.338673264423879239, 41.81695718870634693, -59.02782128990620691 ) ) ;
#58573=CARTESIAN_POINT ( 'NONE',  ( -1.224646799147352665E-15, -3.000000000000002665, -75.00000000000001421 ) ) ;
#58576=CARTESIAN_POINT ( 'NONE',  ( -7.154160341167064452, -5.000000000000055955, -15.39637319599203380 ) ) ;
#58598=CARTESIAN_POINT ( 'NONE',  ( 62.59524157943331346, 48.00000000000000000, 18.50207713769442819 ) ) ;
#58611=B_SPLINE_CURVE_WITH_KNOTS ( 'NONE', 3,
 ( #6797, #57997, #97931, #39717, #81723, #41822, #7850, #47775, #66100, #23019 ),
 .UNSPECIFIED., .F., .F.,
 ( 4, 2, 2, 2, 4 ),
 ( 0.000000000000000000, 0.5000000000000000000, 0.7500000000000000000, 0.8750000000000000000, 1.000000000000000000 ),
 .UNSPECIFIED. ) ;
#58612=CARTESIAN_POINT ( 'NONE',  ( -32.23780387955194016, 18.64284798593076076, 20.91998874883119441 ) ) ;
#58681=( NAMED_UNIT ( * ) PLANE_ANGLE_UNIT ( ) SI_UNIT ( $, .RADIAN. ) );
#58682=EDGE_CURVE ( 'NONE', #14419, #35975, #95806, .T. ) ;
#58714=CARTESIAN_POINT ( 'NONE',  ( 0.000000000000000000, -79.93083296558610584, -70.00000000000000000 ) ) ;
#58732=CARTESIAN_POINT ( 'NONE',  ( -6.894536899122033269, 41.40764853481034891, -58.61755485280149713 ) ) ;
#58741=ORIENTED_EDGE ( 'NONE', *, *, #102106, .F. ) ;
#58752=CARTESIAN_POINT ( 'NONE',  ( 88.20421627921849961, 42.00000000000000000, -23.70422451876603631 ) ) ;
#58755=SURFACE_STYLE_FILL_AREA ( #97582 ) ;
#58760=CARTESIAN_POINT ( 'NONE',  ( 6.228838983406037144, 41.78908903116954576, -58.91794007031819547 ) ) ;
#58761=FACE_OUTER_BOUND ( 'NONE', #29588, .T. ) ;
#58771=CARTESIAN_POINT ( 'NONE',  ( -1.224646799147352665E-15, -3.000000000000002665, -75.00000000000001421 ) ) ;
#58776=CARTESIAN_POINT ( 'NONE',  ( 18.29504988740597327, 45.00000000000001421, 62.40888277855877675 ) ) ;
#58782=CARTESIAN_POINT ( 'NONE',  ( -7.560791642129985668, -4.999999999999999112, -15.61553843468903935 ) ) ;
#58800=CARTESIAN_POINT ( 'NONE',  ( 9.474439531901662548, -5.000000000000000888, -19.39817504954017480 ) ) ;
#58822=CARTESIAN_POINT ( 'NONE',  ( -17.49999999999920419, 50.00907933620717927, 60.12834585266249121 ) ) ;
#58834=CARTESIAN_POINT ( 'NONE',  ( -28.42068399381476951, 41.23824823255147010, -68.38603598170872999 ) ) ;
#58841=CARTESIAN_POINT ( 'NONE',  ( 8.737863884121436442, -3.000000000000002665, -90.03618980231149749 ) ) ;
#58862=EDGE_CURVE ( 'NONE', #58519, #15506, #85486, .T. ) ;
#58869=VERTEX_POINT ( 'NONE', #40637 ) ;
#58891=AXIS2_PLACEMENT_3D ( 'NONE', #66564, #1267, #33690 ) ;
#58902=CARTESIAN_POINT ( 'NONE',  ( -7.302131129577486668, 41.45639756854046709, -59.68093842325847476 ) ) ;
#58911=VERTEX_POINT ( 'NONE', #89738 ) ;
#58927=CARTESIAN_POINT ( 'NONE',  ( -62.95721822007438107, 50.00000000000000000, 4.916537939864575435 ) ) ;
#58989=CARTESIAN_POINT ( 'NONE',  ( -11.84571380832733567, 40.83929531345456354, 63.98140447915187679 ) ) ;
#58991=ORIENTED_EDGE ( 'NONE', *, *, #55756, .F. ) ;
#58992=CARTESIAN_POINT ( 'NONE',  ( 14.73061849464112782, 41.88685504477518862, -82.04001408458998412 ) ) ;
#59008=CARTESIAN_POINT ( 'NONE',  ( -7.432465545960663000, 40.29241764077763577, -70.20619433869296699 ) ) ;
#59028=SURFACE_SIDE_STYLE ('',( #49854 ) ) ;
#59044=CARTESIAN_POINT ( 'NONE',  ( 12.50000000000000178, 40.45931421048912568, -67.96789048815475098 ) ) ;
#59051=CARTESIAN_POINT ( 'NONE',  ( 5.373715277452113526, 41.43915641971339170, -58.48990532576927848 ) ) ;
#59054=VERTEX_POINT ( 'NONE', #33631 ) ;
#59089=FACE_OUTER_BOUND ( 'NONE', #31776, .T. ) ;
#59094=CARTESIAN_POINT ( 'NONE',  ( 11.91432047182400211, 48.00000000000000000, 64.17585289259234571 ) ) ;
#59109=CARTESIAN_POINT ( 'NONE',  ( -8.068282690937467194, -4.999999999999939604, -15.79776062907038714 ) ) ;
#59132=CARTESIAN_POINT ( 'NONE',  ( 62.91825180719526145, 50.00000000000000000, 6.605622457241173251 ) ) ;
#59143=CARTESIAN_POINT ( 'NONE',  ( -25.95755237147325545, 18.64284798593299186, -28.33950252051109686 ) ) ;
#59156=CARTESIAN_POINT ( 'NONE',  ( 21.52118987190722166, 41.77684893734424776, -77.65348390093303976 ) ) ;
#59176=CARTESIAN_POINT ( 'NONE',  ( 9.739726766101595601, 49.99999999999999289, -87.61747884500120165 ) ) ;
#59216=EDGE_CURVE ( 'NONE', #288, #36397, #4841, .T. ) ;
#59223=EDGE_CURVE ( 'NONE', #36789, #88651, #23805, .T. ) ;
#59271=CARTESIAN_POINT ( 'NONE',  ( -39.08667504521158520, 48.00000000000000000, -56.76470588235294912 ) ) ;
#59273=CARTESIAN_POINT ( 'NONE',  ( 12.50000000000000355, 11.21173235486268105, -29.16573252495493307 ) ) ;
#59281=CARTESIAN_POINT ( 'NONE',  ( -17.49999999999997513, 46.00000000000000000, 64.09953197959339377 ) ) ;
#59288=ORIENTED_EDGE ( 'NONE', *, *, #91739, .F. ) ;
#59301=CARTESIAN_POINT ( 'NONE',  ( 1.778928937981565150, -4.332661967054583840, -18.07496135556122141 ) ) ;
#59329=( NAMED_UNIT ( * ) PLANE_ANGLE_UNIT ( ) SI_UNIT ( $, .RADIAN. ) );
#59330=CARTESIAN_POINT ( 'NONE',  ( -14.33052326666859777, -3.000000000000003109, -89.63170281047537458 ) ) ;
#59337=ADVANCED_FACE ( 'NONE', ( #13842 ), #48281, .F. ) ;
#59365=ORIENTED_EDGE ( 'NONE', *, *, #17824, .T. ) ;
#59408=CARTESIAN_POINT ( 'NONE',  ( 6.256238905933717120, -3.000000000000470290, -71.20382035666703757 ) ) ;
#59434=CARTESIAN_POINT ( 'NONE',  ( -7.320805857562880270, 41.41776710089564517, -59.82972164228972645 ) ) ;
#59493=FILL_AREA_STYLE ('',( #1750 ) ) ;
#59514=CARTESIAN_POINT ( 'NONE',  ( -55.65414010186720617, 42.00000000000000000, -72.41885610115910765 ) ) ;
#59524=CARTESIAN_POINT ( 'NONE',  ( -65.03121895707504052, 40.83786248443141176, -2.178857803530889647 ) ) ;
#59543=CARTESIAN_POINT ( 'NONE',  ( -8.737863884120026015, 49.99999999999999289, -79.96381019768847409 ) ) ;
#59554=CARTESIAN_POINT ( 'NONE',  ( 1.301042606982605321E-15, -5.000000000000000000, -10.00000000000000000 ) ) ;
#59555=CARTESIAN_POINT ( 'NONE',  ( 4.852941176821355285, 40.28748324523049007, -70.80672828646224559 ) ) ;
#59558=B_SPLINE_CURVE_WITH_KNOTS ( 'NONE', 3,
 ( #86171, #70497, #51638, #53251 ),
 .UNSPECIFIED., .F., .F.,
 ( 4, 4 ),
 ( 0.000000000000000000, 1.000000000000000000 ),
 .UNSPECIFIED. ) ;
#59610=FILL_AREA_STYLE_COLOUR ( '', #17684 ) ;
#59615=CARTESIAN_POINT ( 'NONE',  ( -5.437559411288403588, 41.94910065564111790, -59.21852893438062893 ) ) ;
#59665=CARTESIAN_POINT ( 'NONE',  ( 62.34828826643940403, 50.00000000000000000, -10.72527895994504199 ) ) ;
#59679=( GEOMETRIC_REPRESENTATION_CONTEXT ( 3 ) GLOBAL_UNCERTAINTY_ASSIGNED_CONTEXT ( ( #45877 ) ) GLOBAL_UNIT_ASSIGNED_CONTEXT ( ( #60632, #54084, #86509 ) ) REPRESENTATION_CONTEXT ( 'NONE', 'WORKASPACE' ) );
#59690=VERTEX_POINT ( 'NONE', #40127 ) ;
#59692=CARTESIAN_POINT ( 'NONE',  ( 32.97698008590906227, 40.71205098343299511, -62.29860342917670835 ) ) ;
#59710=CARTESIAN_POINT ( 'NONE',  ( -1.308996937480700895, 49.99999999999999289, -75.00000000000001421 ) ) ;
#59720=EDGE_CURVE ( 'NONE', #103692, #8947, #91780, .T. ) ;
#59776=EDGE_CURVE ( 'NONE', #58911, #65010, #80042, .T. ) ;
#59800=CARTESIAN_POINT ( 'NONE',  ( -6.767547366757451499, 41.65232185610268090, -58.92985803237888121 ) ) ;
#59817=FACE_OUTER_BOUND ( 'NONE', #39135, .T. ) ;
#59871=CARTESIAN_POINT ( 'NONE',  ( -15.17227823171737100, -3.000000000000002665, -86.54073391196324394 ) ) ;
#59872=CARTESIAN_POINT ( 'NONE',  ( -14.67571981731716946, -3.000000000000003109, -81.61772031542342631 ) ) ;
#59913=COLOUR_RGB ( '', 0.72549020, 0.75294118, 0.79215686) ;
#59916=CARTESIAN_POINT ( 'NONE',  ( 9.739726766100236688, -3.000000000000002665, -82.38252115499993522 ) ) ;
#59926=CARTESIAN_POINT ( 'NONE',  ( -18.00094660900732535, -4.332661967061336661, 2.683237397145228798 ) ) ;
#59948=AXIS2_PLACEMENT_3D ( 'NONE', #87543, #47583, #78901 ) ;
#59949=CARTESIAN_POINT ( 'NONE',  ( 14.91338090413193918, 41.98696021714861359, -86.62221405687449760 ) ) ;
#59966=( GEOMETRIC_REPRESENTATION_CONTEXT ( 3 ) GLOBAL_UNCERTAINTY_ASSIGNED_CONTEXT ( ( #76346 ) ) GLOBAL_UNIT_ASSIGNED_CONTEXT ( ( #70229, #35777, #11435 ) ) REPRESENTATION_CONTEXT ( 'NONE', 'WORKASPACE' ) );
#59976=CARTESIAN_POINT ( 'NONE',  ( -19.17233543272195462, 49.75016788851922911, 61.61326636310676719 ) ) ;
#59977=CARTESIAN_POINT ( 'NONE',  ( -7.436486834768465393, 40.68079689291138124, -59.06589860020129379 ) ) ;
#59982=VECTOR ( 'NONE', #48483, 1000.000000000000114 ) ;
#59986=( BOUNDED_SURFACE ( )  B_SPLINE_SURFACE ( 2, 3, ( 
 ( #52167, #85080, #19862, #92094, #29026, #52696, #55342, #46737, #79626, #105500 ),
 ( #31124, #88793, #5744, #88271, #96886, #45686, #38663, #6800, #54269, #95830 ),
 ( #87211, #22501, #95302, #37632, #70495, #47255, #87744, #103386, #14882, #62936 ) ),
 .UNSPECIFIED., .F., .F., .F. ) 
 B_SPLINE_SURFACE_WITH_KNOTS ( ( 3, 3 ),
 ( 4, 2, 2, 2, 4 ),
 ( 0.000000000000000000, 1.000000000000000000 ),
 ( 0.000000000000000000, 0.01533609458748647764, 0.03067218917497295527, 0.04600828376245943291, 0.06134437834994591054 ),
 .UNSPECIFIED. ) 
 GEOMETRIC_REPRESENTATION_ITEM ( )  RATIONAL_B_SPLINE_SURFACE ( (
 ( 1.000000000000000000, 1.000000000000000000, 1.000000000000000000, 1.000000000000000000, 1.000000000000000000, 1.000000000000000000, 1.000000000000000000, 1.000000000000000000, 1.000000000000000000, 1.000000000000000000),
 ( 1.857142857142858317, 1.857142857142858317, 1.857142857142858317, 1.857142857142858317, 1.857142857142858317, 1.857142857142858317, 1.857142857142858317, 1.857142857142858317, 1.857142857142858317, 1.857142857142858317),
 ( 1.000000000000000000, 1.000000000000000000, 1.000000000000000000, 1.000000000000000000, 1.000000000000000000, 1.000000000000000000, 1.000000000000000000, 1.000000000000000000, 1.000000000000000000, 1.000000000000000000) ) ) 
 REPRESENTATION_ITEM ( '' )  SURFACE ( )  );
#60001=CARTESIAN_POINT ( 'NONE',  ( -11.68767211932491179, -5.000000000000002665, -88.14097461399494193 ) ) ;
#60002=UNCERTAINTY_MEASURE_WITH_UNIT (LENGTH_MEASURE( 1.000000000000000082E-05 ), #2939, 'distance_accuracy_value', 'NONE');
#60024=COLOUR_RGB ( '', 0.40784314, 0.44705882, 0.49803922) ;
#60039=CARTESIAN_POINT ( 'NONE',  ( 4.080003621828020677, 50.00000000000000000, -97.51073764067400873 ) ) ;
#60047=CARTESIAN_POINT ( 'NONE',  ( 17.49999999999959144, 49.99999999999815259, 59.82664205501160382 ) ) ;
#60063=CARTESIAN_POINT ( 'NONE',  ( -90.56128410203886858, 42.00000000000000000, 11.85444436786840328 ) ) ;
#60070=CARTESIAN_POINT ( 'NONE',  ( -51.64414839223339015, 40.83902574785438588, 39.58156097992099376 ) ) ;
#60080=CARTESIAN_POINT ( 'NONE',  ( -8.169585525225413036, 41.99999999999999289, -72.41994148081866456 ) ) ;
#60088=( NAMED_UNIT ( * ) PLANE_ANGLE_UNIT ( ) SI_UNIT ( $, .RADIAN. ) );
#60089=CARTESIAN_POINT ( 'NONE',  ( -12.49018806437142715, -3.466428895744098515, -13.79302967849227457 ) ) ;
#60115=CARTESIAN_POINT ( 'NONE',  ( -6.924711584187146940, 40.92328497002484511, -70.90711766174086961 ) ) ;
#60129=CARTESIAN_POINT ( 'NONE',  ( -17.59737154672216164, 45.00000000000000000, 63.11098746908783141 ) ) ;
#60132=ORIENTED_EDGE ( 'NONE', *, *, #52997, .F. ) ;
#60148=CARTESIAN_POINT ( 'NONE',  ( -25.23529853069842588, 43.63852619275398581, -75.80720028947999367 ) ) ;
#60158=CARTESIAN_POINT ( 'NONE',  ( 10.50000000000000711, -5.000000000000000000, -77.33514508527181874 ) ) ;
#60175=CARTESIAN_POINT ( 'NONE',  ( 9.500000000000007105, -5.000000000000000000, -68.91429205785459544 ) ) ;
#60181=CARTESIAN_POINT ( 'NONE',  ( -23.38163988261910831, 48.00000000000000000, 60.94087333798633210 ) ) ;
#60207=COLOUR_RGB ( '', 0.31764706, 0.68627451, 0.89019608) ;
#60214=FILL_AREA_STYLE ('',( #94145 ) ) ;
#60216=CARTESIAN_POINT ( 'NONE',  ( 5.700740065103228282, 42.00193813223110340, -69.19507478788203514 ) ) ;
#60217=CARTESIAN_POINT ( 'NONE',  ( -64.32759900501736183, 49.99999999999999289, -11.06576400629343659 ) ) ;
#60256=FILL_AREA_STYLE_COLOUR ( '', #7013 ) ;
#60259=CARTESIAN_POINT ( 'NONE',  ( -7.996668422907487361, 49.99999999999999289, -91.14546720082822162 ) ) ;
#60267=VERTEX_POINT ( 'NONE', #1643 ) ;
#60326=ORIENTED_EDGE ( 'NONE', *, *, #79363, .F. ) ;
#60358=CARTESIAN_POINT ( 'NONE',  ( 6.711450852063899575, 41.78336497133594207, -59.19447471094596835 ) ) ;
#60359=CARTESIAN_POINT ( 'NONE',  ( 33.52312678242137167, 18.64316884714798306, 19.32152200346563120 ) ) ;
#60367=CARTESIAN_POINT ( 'NONE',  ( 6.592761323367946069, 41.57274267171208493, -58.68933690419966354 ) ) ;
#60409=CARTESIAN_POINT ( 'NONE',  ( 13.83769416169610444, -3.000000000000003109, -79.05569278145411261 ) ) ;
#60414=AXIS2_PLACEMENT_3D ( 'NONE', #104703, #63738, #55597 ) ;
#60460=CARTESIAN_POINT ( 'NONE',  ( -9.999008799017543581, -5.000000000000578204, -14.11099437790245226 ) ) ;
#60483=CARTESIAN_POINT ( 'NONE',  ( 7.230783165913826416, -2.999999999999999112, -70.90935356275363688 ) ) ;
#60491=CARTESIAN_POINT ( 'NONE',  ( -11.99733130326054997, -4.773999631974040092, -12.57663782514888240 ) ) ;
#60506=CARTESIAN_POINT ( 'NONE',  ( -18.91781669292785395, 48.00000000000000000, 62.18610382930904734 ) ) ;
#60507=CARTESIAN_POINT ( 'NONE',  ( -7.274255425475363523, 41.49770500802092243, -59.52552341803120584 ) ) ;
#60508=CARTESIAN_POINT ( 'NONE',  ( 4.854898838401722649, 40.57569111244889370, -70.80100276615310406 ) ) ;
#60519=CARTESIAN_POINT ( 'NONE',  ( 5.311458304196372104, 22.41101449600902740, -41.39308602215781718 ) ) ;
#60520=CARTESIAN_POINT ( 'NONE',  ( 12.48910114120020687, -3.488630791343517945, -13.76724771964344640 ) ) ;
#60521=CARTESIAN_POINT ( 'NONE',  ( -6.990291106834062518, -3.000000000000000444, 4.028951842967197550 ) ) ;
#60524=FILL_AREA_STYLE_COLOUR ( '', #55352 ) ;
#60549=CARTESIAN_POINT ( 'NONE',  ( 1.301042606982605321E-15, -5.000000000000000000, -10.00000000000000000 ) ) ;
#60571=CARTESIAN_POINT ( 'NONE',  ( 19.21238756580750717, 49.78778941994806218, 61.53710458952721041 ) ) ;
#60588=( NAMED_UNIT ( * ) SI_UNIT ( $, .STERADIAN. ) SOLID_ANGLE_UNIT ( ) );
#60596=CARTESIAN_POINT ( 'NONE',  ( 11.87327623748599770, 40.83929701193095951, 63.97656400230257390 ) ) ;
#60602=ORIENTED_EDGE ( 'NONE', *, *, #39209, .T. ) ;
#60614=( LENGTH_UNIT ( ) NAMED_UNIT ( * ) SI_UNIT ( .MILLI., .METRE. ) );
#60632=( LENGTH_UNIT ( ) NAMED_UNIT ( * ) SI_UNIT ( .MILLI., .METRE. ) );
#60641=CARTESIAN_POINT ( 'NONE',  ( -6.060118994825670846, 40.55658335032454431, -71.16215350181603583 ) ) ;
#60653=CARTESIAN_POINT ( 'NONE',  ( -18.28239497294003968, 45.00000000000002132, 62.41453136349703357 ) ) ;
#60656=VERTEX_POINT ( 'NONE', #64685 ) ;
#60674=CYLINDRICAL_SURFACE ( 'NONE', #62031, 60.00000000000000000 ) ;
#60679=B_SPLINE_CURVE_WITH_KNOTS ( 'NONE', 3,
 ( #72812, #64742, #88496, #106238, #71754, #64229, #73340, #32398, #48539, #97101, #97618, #23242, #81430, #65270, #104663, #96588, #23784, #6490 ),
 .UNSPECIFIED., .F., .F.,
 ( 4, 2, 2, 2, 2, 2, 2, 2, 4 ),
 ( 0.5000000000000000000, 0.5625000000000000000, 0.6250000000000000000, 0.6875000000000000000, 0.7500000000000000000, 0.8125000000000000000, 0.8750000000000000000, 0.9375000000000000000, 1.000000000000000000 ),
 .UNSPECIFIED. ) ;
#60685=CARTESIAN_POINT ( 'NONE',  ( 11.07494621800369039, -4.984107567658546678, -12.57739282099218592 ) ) ;
#60701=CARTESIAN_POINT ( 'NONE',  ( 51.78317192862468943, 48.00000000000000000, 39.73656039225600978 ) ) ;
#60707=CARTESIAN_POINT ( 'NONE',  ( -6.417056615203631686, 41.92969948368747168, -59.44199727782134346 ) ) ;
#60737=CARTESIAN_POINT ( 'NONE',  ( 6.821510612526563655, 41.53001914900257674, -70.37925568709802349 ) ) ;
#60738=CARTESIAN_POINT ( 'NONE',  ( 42.35263604940418958, 50.00000000000000000, 46.99568999590452734 ) ) ;
#60763=CARTESIAN_POINT ( 'NONE',  ( 32.37035071761208371, 40.78778520401346697, -63.10690315066334932 ) ) ;
#60778=CARTESIAN_POINT ( 'NONE',  ( -3.140974613990812792, 50.00000000000000000, -73.31232788067644890 ) ) ;
#60834=CARTESIAN_POINT ( 'NONE',  ( 0.000000000000000000, 45.00000000000000711, 0.000000000000000000 ) ) ;
#60856=CARTESIAN_POINT ( 'NONE',  ( -5.622681999521890184, 41.99823411347379931, -69.46127173319746362 ) ) ;
#60860=CARTESIAN_POINT ( 'NONE',  ( 10.50000000000000178, -5.000000000000000000, -12.52300748975612166 ) ) ;
#60880=CARTESIAN_POINT ( 'NONE',  ( -33.52312678242540755, 18.64316884714407152, -19.32152200344674498 ) ) ;
#60889=CARTESIAN_POINT ( 'NONE',  ( 5.383907448094620740, 41.54392475608550939, -58.58678525159944428 ) ) ;
#60901=B_SPLINE_CURVE_WITH_KNOTS ( 'NONE', 3,
 ( #60158, #94090, #84408, #93023 ),
 .UNSPECIFIED., .F., .F.,
 ( 4, 4 ),
 ( 0.000000000000000000, 1.000000000000000000 ),
 .UNSPECIFIED. ) ;
#60902=EDGE_CURVE ( 'NONE', #288, #57839, #49129, .T. ) ;
#60910=CARTESIAN_POINT ( 'NONE',  ( 7.113472013431289653, 40.00000000359433017, -71.00901315851923812 ) ) ;
#60913=EDGE_CURVE ( 'NONE', #67484, #78737, #4083, .T. ) ;
#60929=CARTESIAN_POINT ( 'NONE',  ( -13.73780227957324129, -5.000000000000002665, -78.37846873786800472 ) ) ;
#60945=CARTESIAN_POINT ( 'NONE',  ( -17.49999999999997513, 51.99999999999981526, 59.56761335716019801 ) ) ;
#60964=CARTESIAN_POINT ( 'NONE',  ( -5.902962327514317487, 41.87327319969161010, -59.02279321040224147 ) ) ;
#60978=CARTESIAN_POINT ( 'NONE',  ( 9.117185603066571886, -4.332661967060696284, -15.39580070564444014 ) ) ;
#60999=COLOUR_RGB ( '', 0.09019608, 0.27058824, 0.51372549) ;
#61002=CARTESIAN_POINT ( 'NONE',  ( 15.47979971815697908, 42.57621410692647146, -89.21879381463644165 ) ) ;
#61004=CARTESIAN_POINT ( 'NONE',  ( 5.902907888931476776, -4.999999999999999112, -73.20788160635341058 ) ) ;
#61027=CARTESIAN_POINT ( 'NONE',  ( -19.30670087550686986, 49.86676902829839264, 61.31490456933869382 ) ) ;
#61028=DIRECTION ( 'NONE',  ( 1.000000000000000000, 0.000000000000000000, -0.000000000000000000 ) ) ;
#61029=CARTESIAN_POINT ( 'NONE',  ( 6.455413918329012013, 41.05104878809925850, -71.04266228314376974 ) ) ;
#61043=CARTESIAN_POINT ( 'NONE',  ( 5.282975838324663442, 16.24034189271231909, -35.83174429344832390 ) ) ;
#61046=CARTESIAN_POINT ( 'NONE',  ( 4.651269564039822946, -4.999999999999991118, -15.66707428873065311 ) ) ;
#61114=CARTESIAN_POINT ( 'NONE',  ( 31.45106920060756295, 40.83882431089578091, 56.96264530398576653 ) ) ;
#61116=ORIENTED_EDGE ( 'NONE', *, *, #67802, .F. ) ;
#61131=PRESENTATION_STYLE_ASSIGNMENT (( #8307 ) ) ;
#61136=ORIENTED_EDGE ( 'NONE', *, *, #16169, .F. ) ;
#61145=CARTESIAN_POINT ( 'NONE',  ( 6.757705285491359071, 41.35007050631321590, -70.67351639401239538 ) ) ;
#61149=FACE_OUTER_BOUND ( 'NONE', #78619, .T. ) ;
#61160=CARTESIAN_POINT ( 'NONE',  ( -5.211028242775610053, 40.56334570827803532, -70.92280011129018646 ) ) ;
#61183=EDGE_CURVE ( 'NONE', #96838, #20, #14799, .T. ) ;
#61205=CARTESIAN_POINT ( 'NONE',  ( 11.05388719230748684, -4.985422414517793221, -12.57711417799305664 ) ) ;
#61214=CARTESIAN_POINT ( 'NONE',  ( 2.617478843592802473, 48.00000000000000711, -94.73972676668314818 ) ) ;
#61215=EDGE_CURVE ( 'NONE', #33315, #86317, #20945, .T. ) ;
#61218=CARTESIAN_POINT ( 'NONE',  ( 7.500000000000007105, -4.999999999999999112, -52.94236561372729000 ) ) ;
#61229=CARTESIAN_POINT ( 'NONE',  ( -6.275176166263391586, 41.94081489990061584, -59.38054223964236655 ) ) ;
#61239=ORIENTED_EDGE ( 'NONE', *, *, #45173, .T. ) ;
#61251=DIRECTION ( 'NONE',  ( -0.5882352941176471894, 0.000000000000000000, -0.8086898285216187476 ) ) ;
#61261=CARTESIAN_POINT ( 'NONE',  ( 4.999060825136298014, 41.75164249415627182, -70.37937598343344803 ) ) ;
#61262=CARTESIAN_POINT ( 'NONE',  ( -39.04923757934999884, 49.99999999997997691, 52.30342408740197158 ) ) ;
#61273=EDGE_LOOP ( 'NONE', ( #9152, #70523, #73767, #83501 ) ) ;
#61295=CARTESIAN_POINT ( 'NONE',  ( 22.54429042550015083, 43.83586977107353988, -79.50672479082321331 ) ) ;
#61303=CARTESIAN_POINT ( 'NONE',  ( 11.99999999999999467, 50.00000000000000000, -83.42920367501479006 ) ) ;
#61319=CARTESIAN_POINT ( 'NONE',  ( -9.999999999999992895, -3.000000000000002665, -86.30899693899574743 ) ) ;
#61325=FILL_AREA_STYLE_COLOUR ( '', #48685 ) ;
#61350=CARTESIAN_POINT ( 'NONE',  ( -17.49999999999998224, 50.00000000000000000, 63.60712894880522583 ) ) ;
#61351=CARTESIAN_POINT ( 'NONE',  ( 6.738141070036321345, -4.358126490543069664, -16.85492060642626200 ) ) ;
#61373=CARTESIAN_POINT ( 'NONE',  ( 3.122594241960849448, 50.00000000000000711, -96.69514296590838853 ) ) ;
#61389=CARTESIAN_POINT ( 'NONE',  ( -6.675188372276874560, 41.63185016722236043, -70.36443417157406088 ) ) ;
#61395=CARTESIAN_POINT ( 'NONE',  ( -6.744834067507015085, 41.44195096935217748, -58.57194677540513794 ) ) ;
#61398=DIRECTION ( 'NONE',  ( 0.000000000000000000, 1.000000000000000000, 0.000000000000000000 ) ) ;
#61410=VERTEX_POINT ( 'NONE', #103173 ) ;
#61414=CARTESIAN_POINT ( 'NONE',  ( 6.786616689952412074, 41.72678941544184994, -59.11526159199856068 ) ) ;
#61416=CARTESIAN_POINT ( 'NONE',  ( -23.57730434129643626, 18.64316884713158728, -30.67950393661452679 ) ) ;
#61424=CARTESIAN_POINT ( 'NONE',  ( 6.372521186659901637, 41.41795280492296172, -58.45320835100594081 ) ) ;
#61450=SURFACE_SIDE_STYLE ('',( #102959 ) ) ;
#61461=CARTESIAN_POINT ( 'NONE',  ( 0.000000000000000000, 47.00000000000000000, 0.000000000000000000 ) ) ;
#61467=CARTESIAN_POINT ( 'NONE',  ( 4.766030446259729381, -5.000000000000002665, -97.32770387339404294 ) ) ;
#61516=CARTESIAN_POINT ( 'NONE',  ( 3.631902923573203879, -4.332661967060489339, 17.83376356531591611 ) ) ;
#61519=ORIENTED_EDGE ( 'NONE', *, *, #17969, .T. ) ;
#61542=CARTESIAN_POINT ( 'NONE',  ( 4.852941176470592310, -2.999999999999999112, -70.80672828634229177 ) ) ;
#61553=CARTESIAN_POINT ( 'NONE',  ( -7.500000000000007105, 42.86855997971688481, -62.45407030448338048 ) ) ;
#61561=CARTESIAN_POINT ( 'NONE',  ( -9.500000000000000000, -5.000000000000000000, -20.99851272547259384 ) ) ;
#61564=SURFACE_STYLE_USAGE ( .BOTH. , #79310 ) ;
#61565=CARTESIAN_POINT ( 'NONE',  ( 6.195804100829465533, 41.59435685053998810, -70.65487364791137281 ) ) ;
#61574=ORIENTED_EDGE ( 'NONE', *, *, #63299, .F. ) ;
#61580=CARTESIAN_POINT ( 'NONE',  ( 5.221682558027961107, 7.016321058000157151, -27.48376762107660554 ) ) ;
#61581=CARTESIAN_POINT ( 'NONE',  ( 12.47891400660274464, -3.648257510622830768, -13.58339488149144003 ) ) ;
#61582=CARTESIAN_POINT ( 'NONE',  ( -7.791781413346525298, -2.999999999999999556, 2.093983074874242956 ) ) ;
#61585=CARTESIAN_POINT ( 'NONE',  ( 1.570796324976846403, -5.000000000000002665, -97.00000000000000000 ) ) ;
#61588=CARTESIAN_POINT ( 'NONE',  ( -7.500000000000006217, 39.99999999999999289, -62.89165061481655528 ) ) ;
#61630=CARTESIAN_POINT ( 'NONE',  ( -2.040829700809986047, 50.00000000000000000, -98.00000000000000000 ) ) ;
#61645=CARTESIAN_POINT ( 'NONE',  ( 39.45041558553427308, 41.98133502302429321, -56.26464531454707441 ) ) ;
#61656=CARTESIAN_POINT ( 'NONE',  ( -29.83308852624522345, 41.99999999999999289, 51.76085035109112198 ) ) ;
#61665=CARTESIAN_POINT ( 'NONE',  ( 55.21742879405702098, 39.42598490589298876, 34.80677065731995867 ) ) ;
#61667=EDGE_CURVE ( 'NONE', #58869, #54340, #3815, .T. ) ;
#61685=CARTESIAN_POINT ( 'NONE',  ( -6.043427762771305112, 50.00000000000000000, -74.51456333905269958 ) ) ;
#61689=CARTESIAN_POINT ( 'NONE',  ( -28.08715220167751170, 18.64284798593048365, 26.23039857545936826 ) ) ;
#61694=ORIENTED_EDGE ( 'NONE', *, *, #48848, .T. ) ;
#61700=SURFACE_SIDE_STYLE ('',( #102120 ) ) ;
#61708=CARTESIAN_POINT ( 'NONE',  ( -5.231947880461875755, 41.12212895974708715, -70.85062085811149757 ) ) ;
#61738=CARTESIAN_POINT ( 'NONE',  ( 6.784953749580444615, 41.67963532863181797, -59.00226812211813154 ) ) ;
#61745=CARTESIAN_POINT ( 'NONE',  ( 5.327003236163648126, 25.27808877631457207, -43.98407828350998727 ) ) ;
#61756=CARTESIAN_POINT ( 'NONE',  ( 7.500000000000007105, 42.00000000000000711, -58.69229087761227959 ) ) ;
#61763=CARTESIAN_POINT ( 'NONE',  ( 5.036189803708993828, 48.00000000000000711, -93.73786388354255905 ) ) ;
#61766=CARTESIAN_POINT ( 'NONE',  ( 7.500000000000001776, -3.000000000000000000, -36.97043916959991350 ) ) ;
#61771=CARTESIAN_POINT ( 'NONE',  ( 57.09426686933954898, 50.00000000000000000, -27.25041924768392576 ) ) ;
#61776=CARTESIAN_POINT ( 'NONE',  ( -6.700949174070592207, 41.88761787213280741, -59.59787320614237416 ) ) ;
#61786=CARTESIAN_POINT ( 'NONE',  ( 17.75966234059601234, 50.00000000000002132, 62.25802333796747945 ) ) ;
#61809=CARTESIAN_POINT ( 'NONE',  ( 5.687763635532137485, 41.86978750169822661, -70.29636349754139246 ) ) ;
#61827=ORIENTED_EDGE ( 'NONE', *, *, #86669, .T. ) ;
#61831=CARTESIAN_POINT ( 'NONE',  ( 42.00322489364931755, 39.55629383142768773, -50.29209334003609655 ) ) ;
#61843=CARTESIAN_POINT ( 'NONE',  ( 39.08667504540952109, 49.99999999999999289, -56.76470588249685534 ) ) ;
#61846=CARTESIAN_POINT ( 'NONE',  ( -9.999999999999996447, 48.00000000000000000, -83.69100306252323662 ) ) ;
#61862=B_SPLINE_CURVE_WITH_KNOTS ( 'NONE', 3,
 ( #67589, #42227, #84295, #75658 ),
 .UNSPECIFIED., .F., .F.,
 ( 4, 4 ),
 ( 0.000000000000000000, 1.000000000000000000 ),
 .UNSPECIFIED. ) ;
#61890=FILL_AREA_STYLE_COLOUR ( '', #60999 ) ;
#61891=CARTESIAN_POINT ( 'NONE',  ( -18.00109036083110681, 50.00000000000000711, 61.88627459926749452 ) ) ;
#61893=COLOUR_RGB ( '', 0.09019608, 0.27058824, 0.51372549) ;
#61903=DIRECTION ( 'NONE',  ( 0.000000000000000000, 0.000000000000000000, 1.000000000000000000 ) ) ;
#61907=FILL_AREA_STYLE ('',( #95847 ) ) ;
#61931=CARTESIAN_POINT ( 'NONE',  ( -6.996268133785214616, 41.79455485337270204, -69.25931873534777594 ) ) ;
#61936=CARTESIAN_POINT ( 'NONE',  ( -15.35350627405965085, -5.000000000000000000, -5.840883397579456293 ) ) ;
#61937=CARTESIAN_POINT ( 'NONE',  ( -5.660418747924874872, 41.80469015519229714, -58.87109497794652668 ) ) ;
#61952=CARTESIAN_POINT ( 'NONE',  ( 6.676660777536701730, 41.76849096538412454, -59.12256610131672119 ) ) ;
#61953=CARTESIAN_POINT ( 'NONE',  ( 59.23741894013591036, 42.00000000000000711, 7.754160006506985781 ) ) ;
#61970=ORIENTED_EDGE ( 'NONE', *, *, #36163, .F. ) ;
#61987=ORIENTED_EDGE ( 'NONE', *, *, #99234, .F. ) ;
#61988=DIRECTION ( 'NONE',  ( 0.000000000000000000, 0.000000000000000000, 1.000000000000000000 ) ) ;
#62002=ORIENTED_EDGE ( 'NONE', *, *, #24537, .F. ) ;
#62005=CARTESIAN_POINT ( 'NONE',  ( -10.50942704840529629, -5.000000000000002665, -93.01494055617339995 ) ) ;
#62007=COLOUR_RGB ( '', 0.66274510, 0.83137255, 0.94901961) ;
#62031=AXIS2_PLACEMENT_3D ( 'NONE', #19180, #19708, #12608 ) ;
#62034=EDGE_LOOP ( 'NONE', ( #101284, #72419, #89065, #44712 ) ) ;
#62051=ORIENTED_EDGE ( 'NONE', *, *, #84869, .F. ) ;
#62057=CARTESIAN_POINT ( 'NONE',  ( 7.012902693339095883, -4.999999999998556710, 16.13291991228437894 ) ) ;
#62078=CARTESIAN_POINT ( 'NONE',  ( 18.99451835574970815, 49.48953773287491487, 61.92607718230669178 ) ) ;
#62100=CARTESIAN_POINT ( 'NONE',  ( -18.91772294158991130, 48.18297239048385450, 62.18609455207817405 ) ) ;
#62102=CARTESIAN_POINT ( 'NONE',  ( 6.309251617458595085, 40.00000000335901973, -71.19739464403906481 ) ) ;
#62105=CARTESIAN_POINT ( 'NONE',  ( 12.49999999999999822, -4.999999999999999112, -8.595933841506987250 ) ) ;
#62116=COLOUR_RGB ( '', 0.08235294, 0.09019608, 0.10196078) ;
#62123=CARTESIAN_POINT ( 'NONE',  ( 0.000000000000000000, -5.000000000000002665, -75.00000000000001421 ) ) ;
#62155=CARTESIAN_POINT ( 'NONE',  ( -4.852941176470592310, -2.999999999999999112, -70.80672828634229177 ) ) ;
#62161=CARTESIAN_POINT ( 'NONE',  ( 10.74465425721583856, 48.00000000000000000, -95.72854256505367232 ) ) ;
#62166=CARTESIAN_POINT ( 'NONE',  ( 6.786616689952412074, 41.72678941544184994, -59.11526159199856068 ) ) ;
#62174=CARTESIAN_POINT ( 'NONE',  ( 16.52731600354976393, 43.98685737190850631, -87.77869701378344303 ) ) ;
#62188=CARTESIAN_POINT ( 'NONE',  ( 10.04205104294044482, 18.64316884711816513, -37.36680950588930727 ) ) ;
#62197=CARTESIAN_POINT ( 'NONE',  ( -59.26337206958330484, 39.42463816063593640, 26.86447829808549059 ) ) ;
#62226=CARTESIAN_POINT ( 'NONE',  ( 6.123233995736763324E-16, 48.00000000000000000, -75.00000000000001421 ) ) ;
#62229=CARTESIAN_POINT ( 'NONE',  ( 4.998455113691382401, -5.000000000000000000, -15.56475508679018027 ) ) ;
#62230=CARTESIAN_POINT ( 'NONE',  ( -5.500000000000007105, 42.00000000000000000, -62.89165061492693809 ) ) ;
#62234=( NAMED_UNIT ( * ) SI_UNIT ( $, .STERADIAN. ) SOLID_ANGLE_UNIT ( ) );
#62241=CARTESIAN_POINT ( 'NONE',  ( -6.422423974165688776, 41.30029428932490987, -70.89074254924834406 ) ) ;
#62261=CARTESIAN_POINT ( 'NONE',  ( -12.50000000000001066, 39.72486035274638283, -64.91592812567742499 ) ) ;
#62268=CARTESIAN_POINT ( 'NONE',  ( 6.123233995736763324E-16, 48.00000000000000000, -95.00000000000000000 ) ) ;
#62269=CARTESIAN_POINT ( 'NONE',  ( 6.866539600944548738, 41.67963879285974116, -59.06571970116536363 ) ) ;
#62283=CARTESIAN_POINT ( 'NONE',  ( 7.500000000000007994, 40.00000000000000000, -72.67206406577979294 ) ) ;
#62295=CARTESIAN_POINT ( 'NONE',  ( 60.66923414622826982, 50.00000000000000000, 17.93278245653309710 ) ) ;
#62300=CARTESIAN_POINT ( 'NONE',  ( -7.109733192396789470, 41.69026681596732686, -59.69141549319190432 ) ) ;
#62301=CARTESIAN_POINT ( 'NONE',  ( 12.45393346519260724, -3.927217745179178099, -76.72514752459306919 ) ) ;
#62317=( NAMED_UNIT ( * ) PLANE_ANGLE_UNIT ( ) SI_UNIT ( $, .RADIAN. ) );
#62327=CARTESIAN_POINT ( 'NONE',  ( 5.754767977403508539, 41.95837094234298092, -69.99685021967000864 ) ) ;
#62349=ORIENTED_EDGE ( 'NONE', *, *, #75294, .T. ) ;
#62352=CARTESIAN_POINT ( 'NONE',  ( 17.50000000000002132, 46.94999999999998153, 64.09953197957062798 ) ) ;
#62362=ORIENTED_EDGE ( 'NONE', *, *, #38683, .T. ) ;
#62364=SURFACE_STYLE_USAGE ( .BOTH. , #77473 ) ;
#62366=MECHANICAL_DESIGN_GEOMETRIC_PRESENTATION_REPRESENTATION('',(#89896),#84749);
#62372=CARTESIAN_POINT ( 'NONE',  ( -9.739726766104087829, 48.00000000000000000, -87.61747884499078509 ) ) ;
#62381=CARTESIAN_POINT ( 'NONE',  ( -7.150000000000001243, 41.64999999999999147, -68.91429205801802027 ) ) ;
#62395=DIRECTION ( 'NONE',  ( 1.000000000000000000, 0.000000000000000000, 1.160749806054361473E-16 ) ) ;
#62408=PRESENTATION_STYLE_ASSIGNMENT (( #23021 ) ) ;
#62409=CARTESIAN_POINT ( 'NONE',  ( -17.51905876331014511, 50.00000000000000711, 63.23049753801218742 ) ) ;
#62425=CARTESIAN_POINT ( 'NONE',  ( -13.32558116180121921, 42.77601834456852714, -92.18035469403051252 ) ) ;
#62436=ORIENTED_EDGE ( 'NONE', *, *, #594, .T. ) ;
#62444=ADVANCED_FACE ( 'NONE', ( #83023 ), #15272, .T. ) ;
#62445=CARTESIAN_POINT ( 'NONE',  ( -4.205882352941185509, -5.000000000000002665, -72.69916451482998809 ) ) ;
#62446=CARTESIAN_POINT ( 'NONE',  ( -6.057904167604424295, 41.61856606222242050, -70.65344123333893833 ) ) ;
#62450=CARTESIAN_POINT ( 'NONE',  ( -3.302423421000036718, -5.000000000000001776, 16.08808873516354510 ) ) ;
#62451=CARTESIAN_POINT ( 'NONE',  ( -5.663714540180169621, 41.53602265354958689, -58.55436150342320190 ) ) ;
#62469=CARTESIAN_POINT ( 'NONE',  ( -51.76085035125569789, 42.00000000008225953, 29.83308852628617203 ) ) ;
#62491=CYLINDRICAL_SURFACE ( 'NONE', #37885, 8.000000000000000000 ) ;
#62499=CARTESIAN_POINT ( 'NONE',  ( 16.00313525666932435, 43.99315673427333451, -88.49932639890887742 ) ) ;
#62521=CARTESIAN_POINT ( 'NONE',  ( -9.290012601901949552, -5.000000000000002665, -75.85638632170552853 ) ) ;
#62526=( LENGTH_UNIT ( ) NAMED_UNIT ( * ) SI_UNIT ( .MILLI., .METRE. ) );
#62546=( GEOMETRIC_REPRESENTATION_CONTEXT ( 3 ) GLOBAL_UNCERTAINTY_ASSIGNED_CONTEXT ( ( #92418 ) ) GLOBAL_UNIT_ASSIGNED_CONTEXT ( ( #46940, #79840, #38872 ) ) REPRESENTATION_CONTEXT ( 'NONE', 'WORKASPACE' ) );
#62550=CARTESIAN_POINT ( 'NONE',  ( 0.000000000000000000, 0.000000000000000000, 0.000000000000000000 ) ) ;
#62585=ORIENTED_EDGE ( 'NONE', *, *, #861, .T. ) ;
#62590=CARTESIAN_POINT ( 'NONE',  ( 19.24691749296559351, 49.81725912942741985, 61.46328798589317444 ) ) ;
#62615=CARTESIAN_POINT ( 'NONE',  ( 6.478079979052916215, 41.41225025427277728, -70.77206711466079980 ) ) ;
#62618=CARTESIAN_POINT ( 'NONE',  ( 12.50000000000000711, -4.999999999999999112, -78.42624373368740009 ) ) ;
#62623=ORIENTED_EDGE ( 'NONE', *, *, #46210, .F. ) ;
#62630=CARTESIAN_POINT ( 'NONE',  ( 5.222004380948645164, 7.054286485517851979, -27.51823936837747198 ) ) ;
#62635=CARTESIAN_POINT ( 'NONE',  ( 5.036189802310915731, -3.000000000000002665, -93.73786388412167980 ) ) ;
#62672=CARTESIAN_POINT ( 'NONE',  ( -7.141975279401744814, -2.999999999999884537, -70.98863559355044117 ) ) ;
#62674=VECTOR ( 'NONE', #51276, 1000.000000000000000 ) ;
#62700=CARTESIAN_POINT ( 'NONE',  ( -7.754160006593189713, 42.00000000000000711, 59.23741894013591036 ) ) ;
#62706=CARTESIAN_POINT ( 'NONE',  ( -60.44716248555326388, 39.42448426419966268, 24.08435288277104291 ) ) ;
#62725=CARTESIAN_POINT ( 'NONE',  ( 9.999999999999994671, 48.00000000000000000, -83.69100306252322241 ) ) ;
#62732=CARTESIAN_POINT ( 'NONE',  ( -15.33144028279955329, 43.81371552016283033, -89.42275431741276748 ) ) ;
#62739=CARTESIAN_POINT ( 'NONE',  ( -5.500000000000007994, 42.00000000000000000, -68.91429205818155879 ) ) ;
#62741=CARTESIAN_POINT ( 'NONE',  ( -4.852941176470594975, 11.33333333333377269, -70.80672828634229177 ) ) ;
#62743=SURFACE_SIDE_STYLE ('',( #54085 ) ) ;
#62758=CARTESIAN_POINT ( 'NONE',  ( -7.036764705882381676, 40.00000000007575807, -71.06385277390852195 ) ) ;
#62766=ADVANCED_FACE ( 'NONE', ( #65656 ), #63484, .T. ) ;
#62790=CARTESIAN_POINT ( 'NONE',  ( 5.243676916559595114, 9.267627703000917094, -29.53296413887904848 ) ) ;
#62812=CARTESIAN_POINT ( 'NONE',  ( -1.224646799147352665E-15, -3.000000000000002665, -75.00000000000001421 ) ) ;
#62816=CARTESIAN_POINT ( 'NONE',  ( -58.90678327790172375, 48.00000000000000000, -28.11551192219426909 ) ) ;
#62821=CARTESIAN_POINT ( 'NONE',  ( -6.570528617701141272, 41.93002611759227705, -59.71599440453709917 ) ) ;
#62822=CARTESIAN_POINT ( 'NONE',  ( 11.17909359582588102, -4.978490734258791406, -77.11252404932572801 ) ) ;
#62830=CARTESIAN_POINT ( 'NONE',  ( 18.48043600567737954, 50.00000000000001421, 61.28289380712539014 ) ) ;
#62844=UNCERTAINTY_MEASURE_WITH_UNIT (LENGTH_MEASURE( 1.000000000000000082E-05 ), #21511, 'distance_accuracy_value', 'NONE');
#62854=ORIENTED_EDGE ( 'NONE', *, *, #27391, .T. ) ;
#62864=CARTESIAN_POINT ( 'NONE',  ( -6.075724000949984216, 41.99394325426889196, -59.86320218788793568 ) ) ;
#62872=CARTESIAN_POINT ( 'NONE',  ( 7.500000000000006217, 39.99999999999942446, -59.88032989331673406 ) ) ;
#62896=CARTESIAN_POINT ( 'NONE',  ( -1.308996937480702005, 48.00000000000000000, -75.00000000000001421 ) ) ;
#62897=ORIENTED_EDGE ( 'NONE', *, *, #81900, .F. ) ;
#62925=FILL_AREA_STYLE_COLOUR ( '', #62007 ) ;
#62936=CARTESIAN_POINT ( 'NONE',  ( -16.52732684424164944, 43.98685724163156863, -87.77868211029608858 ) ) ;
#62937=CARTESIAN_POINT ( 'NONE',  ( -19.17751609777260313, 50.00000000000000711, 60.34505262736215059 ) ) ;
#62942=FILL_AREA_STYLE ('',( #93717 ) ) ;
#62972=CARTESIAN_POINT ( 'NONE',  ( 4.852941176470595863, -3.000000000000002665, -70.80672828634229177 ) ) ;
#62973=CARTESIAN_POINT ( 'NONE',  ( -6.195804093982627769, 41.59435685013754380, -70.65487364512668478 ) ) ;
#62985=CARTESIAN_POINT ( 'NONE',  ( -6.786616733794231138, 41.72678875807561383, -59.11526074045958268 ) ) ;
#62986=ORIENTED_EDGE ( 'NONE', *, *, #4946, .T. ) ;
#62999=CARTESIAN_POINT ( 'NONE',  ( 6.338673411933466006, 41.81695763293575396, -59.02782193812689115 ) ) ;
#63017=CARTESIAN_POINT ( 'NONE',  ( -52.56483885390523625, -79.93083296558610584, -38.23529411764706509 ) ) ;
#63045=CARTESIAN_POINT ( 'NONE',  ( -12.50000000000000355, -3.000000000000001776, -76.70872284621019332 ) ) ;
#63052=SURFACE_STYLE_USAGE ( .BOTH. , #30167 ) ;
#63061=COLOUR_RGB ( '', 0.72549020, 0.75294118, 0.79215686) ;
#63079=CARTESIAN_POINT ( 'NONE',  ( -8.245342207438692839, 41.99999999999999289, -58.66077168407692710 ) ) ;
#63112=CARTESIAN_POINT ( 'NONE',  ( 18.92698369676902814, 49.06730440414835925, 62.10640571433232537 ) ) ;
#63147=CARTESIAN_POINT ( 'NONE',  ( 12.50000000000000711, -3.000000000000000000, -80.60844091781802945 ) ) ;
#63164=CARTESIAN_POINT ( 'NONE',  ( 1.308996937483426715, -3.000000000000002665, -75.00000000000001421 ) ) ;
#63176=CARTESIAN_POINT ( 'NONE',  ( 4.903611268973771864, -4.999999999999984901, -16.52575844349507861 ) ) ;
#63179=CARTESIAN_POINT ( 'NONE',  ( -25.39209522342085279, 43.62729496076146063, -75.59164047554419597 ) ) ;
#63200=CARTESIAN_POINT ( 'NONE',  ( -7.500000000000003553, -2.999999999998154365, -69.80246343544763477 ) ) ;
#63221=CARTESIAN_POINT ( 'NONE',  ( 41.97891391008103312, 41.63476235974957262, -52.78853482450573864 ) ) ;
#63232=CARTESIAN_POINT ( 'NONE',  ( -33.52312678239033517, 18.64316884709848665, 19.32152200342503079 ) ) ;
#63238=CARTESIAN_POINT ( 'NONE',  ( -62.84968139608024273, 39.42568783935983134, -16.84587978088738325 ) ) ;
#63255=( GEOMETRIC_REPRESENTATION_CONTEXT ( 3 ) GLOBAL_UNCERTAINTY_ASSIGNED_CONTEXT ( ( #38064 ) ) GLOBAL_UNIT_ASSIGNED_CONTEXT ( ( #56485, #41909, #15507 ) ) REPRESENTATION_CONTEXT ( 'NONE', 'WORKASPACE' ) );
#63258=CARTESIAN_POINT ( 'NONE',  ( 2.617478844990903664, 48.00000000000000000, -75.26027323389595836 ) ) ;
#63271=CARTESIAN_POINT ( 'NONE',  ( 9.246231975912676759, -4.999999999999999112, -18.06183020392694871 ) ) ;
#63275=FILL_AREA_STYLE_COLOUR ( '', #65297 ) ;
#63299=EDGE_CURVE ( 'NONE', #86892, #89440, #42569, .T. ) ;
#63308=CARTESIAN_POINT ( 'NONE',  ( -12.50000000000000355, 26.18163903155594596, -43.67239987017219960 ) ) ;
#63310=CARTESIAN_POINT ( 'NONE',  ( 5.441822646184710344, 41.96569307385608028, -59.31342461362935836 ) ) ;
#63330=CARTESIAN_POINT ( 'NONE',  ( 4.852941176470592310, -3.000000000000002665, -70.80672828634229177 ) ) ;
#63355=CARTESIAN_POINT ( 'NONE',  ( 5.957442974701733007, 49.99999999999999289, 65.00000000000000000 ) ) ;
#63370=CARTESIAN_POINT ( 'NONE',  ( 18.96929081463403932, 50.00000000000001421, 60.62668834763405812 ) ) ;
#63380=CARTESIAN_POINT ( 'NONE',  ( -1.899844873468226281, 42.00000000000000711, -68.00838909559428203 ) ) ;
#63385=CARTESIAN_POINT ( 'NONE',  ( 24.21392849876044906, 50.00000000000000711, 58.37490609712320833 ) ) ;
#63403=CARTESIAN_POINT ( 'NONE',  ( -6.757705282517541434, 41.35007050579768162, -70.67351639275690900 ) ) ;
#63408=UNCERTAINTY_MEASURE_WITH_UNIT (LENGTH_MEASURE( 1.000000000000000082E-05 ), #32657, 'distance_accuracy_value', 'NONE');
#63409=ORIENTED_EDGE ( 'NONE', *, *, #92115, .F. ) ;
#63436=CARTESIAN_POINT ( 'NONE',  ( -6.145467200824003662, 48.00000000000000000, -77.00333157709306420 ) ) ;
#63457=CARTESIAN_POINT ( 'NONE',  ( 10.00000000000000000, -5.000000000000000000, -2.617993873628171375 ) ) ;
#63461=CARTESIAN_POINT ( 'NONE',  ( -5.292942464630674415, 18.36785030193200896, -37.75007169989023481 ) ) ;
#63473=CARTESIAN_POINT ( 'NONE',  ( 0.000000000000000000, 0.000000000000000000, 65.00000000000000000 ) ) ;
#63476=CARTESIAN_POINT ( 'NONE',  ( -18.13920979082782736, 50.00000000000000000, 61.71120590876283529 ) ) ;
#63484=B_SPLINE_SURFACE_WITH_KNOTS ( 'NONE', 3, 3, ( 
 ( #8997, #74791, #7399, #869, #15504, #31714, #49455, #48392, #65118, #24168 ),
 ( #48915, #106634, #82364, #8470, #25778, #78387, #44983, #95126, #94601, #77335 ),
 ( #12580, #11511, #46034, #36392, #62241, #86517, #45513, #27766, #13106, #99600 ),
 ( #68728, #70309, #101612, #3446, #84893, #43898, #93528, #29350, #61708, #4504 ),
 ( #60115, #35851, #69779, #28285, #37440, #103204, #21257, #54094, #87037, #94047 ),
 ( #78915, #33848, #85981, #66720, #36908, #92979, #60641, #19673, #61160, #19139 ),
 ( #77869, #51978, #10981, #3979, #76787, #2891, #20207, #52513, #53062, #85428 ),
 ( #44439, #69259, #102130, #102670, #12054, #28833, #20748, #53587, #47599, #29874 ) ),
 .UNSPECIFIED., .F., .F., .F.,
 ( 4, 2, 2, 4 ),
 ( 4, 2, 2, 2, 4 ),
 ( 0.000000000000000000, 0.2500000000000000000, 0.5000000000000000000, 1.000000000000000000 ),
 ( 0.000000000000000000, 0.1250000000000000000, 0.2500000000000000000, 0.5000000000000000000, 1.000000000000000000 ),
 .UNSPECIFIED. ) ;
#63511=( LENGTH_UNIT ( ) NAMED_UNIT ( * ) SI_UNIT ( .MILLI., .METRE. ) );
#63536=CARTESIAN_POINT ( 'NONE',  ( 6.846705483647400392, 41.84866126346769732, -59.70429168036804413 ) ) ;
#63575=CARTESIAN_POINT ( 'NONE',  ( -12.48746907676934370, -3.545640499966867143, -76.71370838498235400 ) ) ;
#63576=UNCERTAINTY_MEASURE_WITH_UNIT (LENGTH_MEASURE( 1.000000000000000082E-05 ), #57167, 'distance_accuracy_value', 'NONE');
#63594=CARTESIAN_POINT ( 'NONE',  ( 0.000000000000000000, -5.000000000000000000, 10.00000000000000000 ) ) ;
#63604=FACE_OUTER_BOUND ( 'NONE', #24430, .T. ) ;
#63625=CARTESIAN_POINT ( 'NONE',  ( -7.416129379031016100, 42.00000000000000000, -59.68109090348218615 ) ) ;
#63643=CARTESIAN_POINT ( 'NONE',  ( -64.32470902915410704, 48.00000000000000711, 10.67393577672269167 ) ) ;
#63656=ORIENTED_EDGE ( 'NONE', *, *, #10831, .F. ) ;
#63657=CARTESIAN_POINT ( 'NONE',  ( 19.10507480816155734, 49.67854560040533585, 61.73104169122685647 ) ) ;
#63688=CARTESIAN_POINT ( 'NONE',  ( 10.50000000000000711, -5.000000000000000000, -78.42624373368740009 ) ) ;
#63706=CARTESIAN_POINT ( 'NONE',  ( -6.145467200824003662, -3.000000000000002665, -92.99666842290695001 ) ) ;
#63713=ORIENTED_EDGE ( 'NONE', *, *, #19756, .F. ) ;
#63715=CARTESIAN_POINT ( 'NONE',  ( 6.738141070036304470, -4.358126490543009268, -16.85492060642630818 ) ) ;
#63731=CARTESIAN_POINT ( 'NONE',  ( -23.38163988282185812, 40.83906611472609427, 60.94087333793187611 ) ) ;
#63734=ORIENTED_EDGE ( 'NONE', *, *, #17969, .F. ) ;
#63737=CARTESIAN_POINT ( 'NONE',  ( -6.827804075409870777, -2.999999999999648281, -71.19745151638491620 ) ) ;
#63738=DIRECTION ( 'NONE',  ( 0.000000000000000000, 1.000000000000000000, 0.000000000000000000 ) ) ;
#63745=CARTESIAN_POINT ( 'NONE',  ( -48.49771892682847607, 39.00440505407896552, -41.54732596423969682 ) ) ;
#63750=CARTESIAN_POINT ( 'NONE',  ( 1.570796324980112679, -5.000000000000002665, -73.00000000000001421 ) ) ;
#63753=CARTESIAN_POINT ( 'NONE',  ( 25.57097515258701748, 43.61428196877569263, -75.34572123083053441 ) ) ;
#63770=CARTESIAN_POINT ( 'NONE',  ( -55.03799937935021802, 39.42592066847770127, 34.70786362942529735 ) ) ;
#63790=CARTESIAN_POINT ( 'NONE',  ( 9.999999999999989342, 49.99999999999999289, -83.69100306251233690 ) ) ;
#63804=CARTESIAN_POINT ( 'NONE',  ( 9.359070339229566216, -5.000000000000000000, -18.64538651940581815 ) ) ;
#63829=CARTESIAN_POINT ( 'NONE',  ( 7.125691916903468481, 41.67430808309654822, -69.26730091920677523 ) ) ;
#63836=CARTESIAN_POINT ( 'NONE',  ( -12.50000000000000000, 34.76801716932426700, -54.02619666611344229 ) ) ;
#63848=CARTESIAN_POINT ( 'NONE',  ( 7.294237765485898528, 41.09455117511487288, -58.80184355254267103 ) ) ;
#63884=CARTESIAN_POINT ( 'NONE',  ( 52.56483885390522914, 49.99999999999999289, -38.23529411764705799 ) ) ;
#63889=CARTESIAN_POINT ( 'NONE',  ( 10.85300161406142827, -4.996537049336601477, -77.21885189815951378 ) ) ;
#63897=CARTESIAN_POINT ( 'NONE',  ( 17.90864227309694812, 50.00000000000000000, 62.01285158411673137 ) ) ;
#63947=CARTESIAN_POINT ( 'NONE',  ( -7.360624614850912906, -5.000000000000000000, -75.38987561218263522 ) ) ;
#63950=EDGE_LOOP ( 'NONE', ( #2486, #78341, #8551, #7667, #8992, #64873, #64989, #92896 ) ) ;
#63955=FACE_OUTER_BOUND ( 'NONE', #9051, .T. ) ;
#63988=CARTESIAN_POINT ( 'NONE',  ( 4.175893272574590753, -3.000000000000000000, -7.137815226410167746 ) ) ;
#64020=( NAMED_UNIT ( * ) PLANE_ANGLE_UNIT ( ) SI_UNIT ( $, .RADIAN. ) );
#64025=CARTESIAN_POINT ( 'NONE',  ( -7.500000000000007105, 39.99999999999998579, -68.91429205786793943 ) ) ;
#64026=CARTESIAN_POINT ( 'NONE',  ( -4.649486852896246525, -5.000000000000039968, -15.66810684149979771 ) ) ;
#64030=EDGE_CURVE ( 'NONE', #94321, #15506, #26915, .T. ) ;
#64073=CARTESIAN_POINT ( 'NONE',  ( 6.075720087193105634, 41.99394347255277182, -59.86320241472431292 ) ) ;
#64136=PLANE ( 'NONE',  #98714 ) ;
#64153=CARTESIAN_POINT ( 'NONE',  ( -3.294249609603382645, 39.99999999999999289, -70.27378291343094929 ) ) ;
#64187=CARTESIAN_POINT ( 'NONE',  ( 19.09341000947918943, 49.66424469652579887, 61.75080758588853058 ) ) ;
#64214=SURFACE_SIDE_STYLE ('',( #89539 ) ) ;
#64229=CARTESIAN_POINT ( 'NONE',  ( 6.397334739185440711, -2.999999999999999556, -4.916373759799318677 ) ) ;
#64233=CARTESIAN_POINT ( 'NONE',  ( 9.739726766102963396, -5.000000000000000888, -82.38252115499879835 ) ) ;
#64241=CARTESIAN_POINT ( 'NONE',  ( 5.538604458977774314, -5.000000000025686120, -16.33373421804029135 ) ) ;
#64243=CARTESIAN_POINT ( 'NONE',  ( -3.122594241941514692, 50.00000000000000711, -73.30485703408217546 ) ) ;
#64258=CARTESIAN_POINT ( 'NONE',  ( -5.957442974920758694, 40.83906611472500714, 65.00000000000298428 ) ) ;
#64280=CARTESIAN_POINT ( 'NONE',  ( -5.036189802309414709, -5.000000000000015099, -93.73786388411730286 ) ) ;
#64291=CARTESIAN_POINT ( 'NONE',  ( -12.98438343323941346, -5.000000000000000000, -86.33384241255676272 ) ) ;
#64297=CARTESIAN_POINT ( 'NONE',  ( 61.12566064942861033, 38.95341179545530963, 18.04917667391267244 ) ) ;
#64317=CARTESIAN_POINT ( 'NONE',  ( 1.308996937480704670, 48.00000000000000000, -75.00000000000001421 ) ) ;
#64336=CARTESIAN_POINT ( 'NONE',  ( -52.56483885390523625, 40.83906611473335602, -38.23529411764706509 ) ) ;
#64352=ORIENTED_EDGE ( 'NONE', *, *, #57891, .F. ) ;
#64361=CARTESIAN_POINT ( 'NONE',  ( 7.159011423967576171, 41.04792438623271522, -70.58264807953590037 ) ) ;
#64377=EDGE_CURVE ( 'NONE', #90268, #34787, #53031, .T. ) ;
#64392=MECHANICAL_DESIGN_GEOMETRIC_PRESENTATION_REPRESENTATION('',(#7392),#28226);
#64393=CARTESIAN_POINT ( 'NONE',  ( 13.46787234807529288, 42.86411582142483923, -91.98473665448270253 ) ) ;
#64396=CARTESIAN_POINT ( 'NONE',  ( 13.87686780678898479, 43.16530558042392585, -91.42246085994810301 ) ) ;
#64439=CARTESIAN_POINT ( 'NONE',  ( -12.50000000000000178, -2.171334558878634802, -15.32410538599969030 ) ) ;
#64463=CARTESIAN_POINT ( 'NONE',  ( 5.787483263666111100, 41.99999999999999289, -68.91429206946564534 ) ) ;
#64472=FILL_AREA_STYLE_COLOUR ( '', #59913 ) ;
#64478=CARTESIAN_POINT ( 'NONE',  ( 49.53030419665140016, 39.42532954512722654, -42.40708954556809829 ) ) ;
#64501=COLOUR_RGB ( '', 0.40784314, 0.44705882, 0.49803922) ;
#64508=SURFACE_SIDE_STYLE ('',( #97375 ) ) ;
#64525=CARTESIAN_POINT ( 'NONE',  ( 6.516354785991091835E-11, 40.83842593836580903, 65.00000000086684793 ) ) ;
#64527=AXIS2_PLACEMENT_3D ( 'NONE', #47045, #28263, #79943 ) ;
#64533=CARTESIAN_POINT ( 'NONE',  ( 17.50000000000007105, 51.77766888149943014, 61.91533629922624016 ) ) ;
#64541=CARTESIAN_POINT ( 'NONE',  ( -7.466456039917235721, -3.088347863564611995, -19.53079660665211037 ) ) ;
#64564=CARTESIAN_POINT ( 'NONE',  ( 23.38163988261896620, 48.00000000000000000, 60.94087333798638895 ) ) ;
#64590=CARTESIAN_POINT ( 'NONE',  ( 5.989966392672700479, 41.99624791910017763, -59.62336946609740806 ) ) ;
#64603=SURFACE_STYLE_FILL_AREA ( #99610 ) ;
#64637=CARTESIAN_POINT ( 'NONE',  ( 4.175893272574590753, -3.000000000000000000, -7.137815226410167746 ) ) ;
#64642=DIRECTION ( 'NONE',  ( 0.000000000000000000, 1.000000000000000000, 0.000000000000000000 ) ) ;
#64643=CARTESIAN_POINT ( 'NONE',  ( -10.50000000000000000, -5.000000000000000000, -9.904958390907868448 ) ) ;
#64644=B_SPLINE_CURVE_WITH_KNOTS ( 'NONE', 3,
 ( #58771, #83553, #9653, #75466, #35048, #18323, #51177, #10197, #26959, #61319, #3604, #101235, #69406, #68881, #93137, #12735, #27388, #76946 ),
 .UNSPECIFIED., .F., .F.,
 ( 4, 2, 2, 2, 2, 2, 2, 2, 4 ),
 ( 0.000000000000000000, 0.06250000000000000000, 0.1250000000000000000, 0.1875000000000000000, 0.2500000000000000000, 0.3125000000000000000, 0.3750000000000000000, 0.4375000000000000000, 0.5000000000000000000 ),
 .UNSPECIFIED. ) ;
#64664=CARTESIAN_POINT ( 'NONE',  ( 0.000000000000000000, -3.331654917651224235, 18.72828050308589454 ) ) ;
#64682=ADVANCED_FACE ( 'NONE', ( #50953 ), #18092, .T. ) ;
#64685=CARTESIAN_POINT ( 'NONE',  ( 12.50000000000000355, 41.59226156894002457, -76.70843802411151557 ) ) ;
#64712=( LENGTH_UNIT ( ) NAMED_UNIT ( * ) SI_UNIT ( .MILLI., .METRE. ) );
#64716=CARTESIAN_POINT ( 'NONE',  ( 5.402795611188940583, 41.73472188612398526, -58.79867419242892623 ) ) ;
#64724=CARTESIAN_POINT ( 'NONE',  ( -5.787480046464959393, 41.99999999999999289, -68.91429205815936143 ) ) ;
#64738=CARTESIAN_POINT ( 'NONE',  ( -7.503613543180902568, -5.000000000000000888, -15.58785114095667623 ) ) ;
#64742=CARTESIAN_POINT ( 'NONE',  ( 1.047197551196598519, -2.999999999999999556, -7.999999999999998224 ) ) ;
#64758=CARTESIAN_POINT ( 'NONE',  ( 5.073014709119004984, -4.333232302192993934, -17.09748285339890117 ) ) ;
#64761=CARTESIAN_POINT ( 'NONE',  ( -39.97406772777365802, 41.90729804012168103, -55.54474264065575539 ) ) ;
#64771=CARTESIAN_POINT ( 'NONE',  ( -62.59524157938066224, 40.83906611472970383, 18.50207713795375142 ) ) ;
#64784=EDGE_LOOP ( 'NONE', ( #40972, #78721, #30248, #31262 ) ) ;
#64792=CARTESIAN_POINT ( 'NONE',  ( -9.596002107492989097, -5.000000000000002665, -77.62543935900905012 ) ) ;
#64808=DIRECTION ( 'NONE',  ( 0.000000000000000000, 1.000000000000000000, 0.000000000000000000 ) ) ;
#64826=VERTEX_POINT ( 'NONE', #69305 ) ;
#64833=EDGE_CURVE ( 'NONE', #81655, #88824, #96456, .T. ) ;
#64869=CARTESIAN_POINT ( 'NONE',  ( 7.226138801442005821, 41.34018720343522801, -70.07054281437619636 ) ) ;
#64873=ORIENTED_EDGE ( 'NONE', *, *, #48432, .F. ) ;
#64879=CARTESIAN_POINT ( 'NONE',  ( -46.29054874100096129, 50.00000000000002842, 42.75167762495752299 ) ) ;
#64963=CARTESIAN_POINT ( 'NONE',  ( -6.890281280090281513, 41.03680257558234246, -70.85895802555796763 ) ) ;
#64971=FILL_AREA_STYLE ('',( #32093 ) ) ;
#64977=CARTESIAN_POINT ( 'NONE',  ( 6.917892303299533197, 41.82074860089118573, -68.91429206365098992 ) ) ;
#64989=ORIENTED_EDGE ( 'NONE', *, *, #25141, .T. ) ;
#64992=CARTESIAN_POINT ( 'NONE',  ( 36.15879880962841497, 40.31104328174256324, -58.06769010848005053 ) ) ;
#65010=VERTEX_POINT ( 'NONE', #75097 ) ;
#65011=CARTESIAN_POINT ( 'NONE',  ( 17.50000000000002842, 49.71153760032640889, 63.93192698917948746 ) ) ;
#65022=STYLED_ITEM ( 'NONE', ( #18107 ), #7550 ) ;
#65050=CARTESIAN_POINT ( 'NONE',  ( 17.50000000000002842, 51.99987222567164480, 59.97465830876894444 ) ) ;
#65059=CARTESIAN_POINT ( 'NONE',  ( -6.738141070038324187, -4.358126490537220121, -16.85492060643100842 ) ) ;
#65081=CARTESIAN_POINT ( 'NONE',  ( 64.91565662643154155, 50.00000000002004441, 6.815324757472883910 ) ) ;
#65095=CARTESIAN_POINT ( 'NONE',  ( -8.913811505013349290, 18.64284798592955283, 37.38269509653747491 ) ) ;
#65107=CARTESIAN_POINT ( 'NONE',  ( 19.34264572229572821, 41.87583415776160933, -80.60122430450024922 ) ) ;
#65108=CARTESIAN_POINT ( 'NONE',  ( 5.441822646184710344, 41.96569307385608028, -59.31342461362935836 ) ) ;
#65115=ORIENTED_EDGE ( 'NONE', *, *, #38428, .T. ) ;
#65118=CARTESIAN_POINT ( 'NONE',  ( -5.308064226573042887, 41.67430808342687243, -70.56675994572434263 ) ) ;
#65131=AXIS2_PLACEMENT_3D ( 'NONE', #31585, #92432, #18588 ) ;
#65160=CARTESIAN_POINT ( 'NONE',  ( 5.219866590718106991, -5.000000000000000000, 8.922269033012842243 ) ) ;
#65168=( NAMED_UNIT ( * ) PLANE_ANGLE_UNIT ( ) SI_UNIT ( $, .RADIAN. ) );
#65169=CARTESIAN_POINT ( 'NONE',  ( 10.47772246152235986, -5.000000000000000000, -78.93829266523391652 ) ) ;
#65174=( BOUNDED_SURFACE ( )  B_SPLINE_SURFACE ( 2, 3, ( 
 ( #2961, #11044, #101137, #53126, #101673, #27831, #27298, #75796, #86043, #12118, #60701, #43438, #45048, #68243, #100598, #59094, #43965, #1890, #92504, #60181, #93049, #34843, #84432, #10522, #52043, #76854, #95709, #22903, #103787, #29418, #78982, #62816, #39074, #46098 ),
 ( #63884, #104313, #6145, #94668, #39607, #21847, #5106, #54689, #70373, #71956, #38037, #29930, #80560, #30462, #78452, #14232, #63355, #87623, #12641, #104860, #80032, #31002, #20813, #70898, #38547, #55740, #13707, #96774, #46617, #37510, #79514, #103268, #88151, #5626 ),
 ( #88674, #47138, #61771, #71412, #53647, #14764, #96256, #62295, #4572, #22381, #47665, #55226, #6681, #72480, #28897, #86577, #95186, #45573, #21317, #54154, #87095, #13171, #90801, #40643, #106427, #25571, #25021, #49794, #149, #49254, #32586, #48195, #57876, #56270 ) ),
 .UNSPECIFIED., .F., .F., .F. ) 
 B_SPLINE_SURFACE_WITH_KNOTS ( ( 3, 3 ),
 ( 4, 2, 2, 2, 2, 2, 2, 2, 2, 2, 2, 2, 2, 2, 2, 2, 4 ),
 ( 0.000000000000000000, 1.000000000000000000 ),
 ( 0.9419214012998449181, 1.216880307836088360, 1.491839214372332023, 1.766798120908575465, 2.041757027444818906, 2.316715933981062570, 2.591674840517305789, 2.866633747053549452, 3.141592653589793116, 3.416551560126036780, 3.691510466662280443, 3.966469373198524107, 4.241428279734767770, 4.516387186271010989, 4.791346092807254209, 5.066304999343497428, 5.341263905879741536 ),
 .UNSPECIFIED. ) 
 GEOMETRIC_REPRESENTATION_ITEM ( )  RATIONAL_B_SPLINE_SURFACE ( (
 ( 1.000000000000000000, 1.000000000000000000, 1.000000000000000000, 1.000000000000000000, 1.000000000000000000, 1.000000000000000000, 1.000000000000000000, 1.000000000000000000, 1.000000000000000000, 1.000000000000000000, 1.000000000000000000, 1.000000000000000000, 1.000000000000000000, 1.000000000000000000, 1.000000000000000000, 1.000000000000000000, 1.000000000000000000, 1.000000000000000000, 1.000000000000000000, 1.000000000000000000, 1.000000000000000000, 1.000000000000000000, 1.000000000000000000, 1.000000000000000000, 1.000000000000000000, 1.000000000000000000, 1.000000000000000000, 1.000000000000000000, 1.000000000000000000, 1.000000000000000000, 1.000000000000000000, 1.000000000000000000, 1.000000000000000000, 1.000000000000000000),
 ( 1.857142857142858317, 1.857142857142858317, 1.857142857142858317, 1.857142857142858317, 1.857142857142858317, 1.857142857142858317, 1.857142857142858317, 1.857142857142858317, 1.857142857142858317, 1.857142857142858317, 1.857142857142858317, 1.857142857142858317, 1.857142857142858317, 1.857142857142858317, 1.857142857142858317, 1.857142857142858317, 1.857142857142858317, 1.857142857142858317, 1.857142857142858317, 1.857142857142858317, 1.857142857142858317, 1.857142857142858317, 1.857142857142858317, 1.857142857142858317, 1.857142857142858317, 1.857142857142858317, 1.857142857142858317, 1.857142857142858317, 1.857142857142858317, 1.857142857142858317, 1.857142857142858317, 1.857142857142858317, 1.857142857142858317, 1.857142857142858317),
 ( 1.000000000000000000, 1.000000000000000000, 1.000000000000000000, 1.000000000000000000, 1.000000000000000000, 1.000000000000000000, 1.000000000000000000, 1.000000000000000000, 1.000000000000000000, 1.000000000000000000, 1.000000000000000000, 1.000000000000000000, 1.000000000000000000, 1.000000000000000000, 1.000000000000000000, 1.000000000000000000, 1.000000000000000000, 1.000000000000000000, 1.000000000000000000, 1.000000000000000000, 1.000000000000000000, 1.000000000000000000, 1.000000000000000000, 1.000000000000000000, 1.000000000000000000, 1.000000000000000000, 1.000000000000000000, 1.000000000000000000, 1.000000000000000000, 1.000000000000000000, 1.000000000000000000, 1.000000000000000000, 1.000000000000000000, 1.000000000000000000) ) ) 
 REPRESENTATION_ITEM ( '' )  SURFACE ( )  );
#65244=CARTESIAN_POINT ( 'NONE',  ( 5.420470438621152631, 41.88321586334136981, -59.04137885805278785 ) ) ;
#65261=CARTESIAN_POINT ( 'NONE',  ( 17.53457271110117333, 45.00000000000002842, 63.41726470817021521 ) ) ;
#65270=CARTESIAN_POINT ( 'NONE',  ( 4.916373759799319565, -2.999999999999999556, 6.397334739185442487 ) ) ;
#65274=FILL_AREA_STYLE ('',( #48009 ) ) ;
#65283=CARTESIAN_POINT ( 'NONE',  ( 12.39938211278620450, -4.333194019920618700, -12.81742571347198911 ) ) ;
#65288=ADVANCED_FACE ( 'NONE', ( #23278, #103642 ), #14607, .T. ) ;
#65297=COLOUR_RGB ( '', 0.08235294, 0.09019608, 0.10196078) ;
#65306=CARTESIAN_POINT ( 'NONE',  ( -17.49999999999997158, 50.30551795522193004, 63.70247084375006352 ) ) ;
#65320=CARTESIAN_POINT ( 'NONE',  ( -23.98369711357355527, 41.62067903365006316, -74.32819821803104787 ) ) ;
#65326=CARTESIAN_POINT ( 'NONE',  ( 11.68767211932491712, -5.000000000000002665, -88.14097461399492772 ) ) ;
#65331=CARTESIAN_POINT ( 'NONE',  ( 7.500000000000005329, 44.25000000000000711, -71.71180648257555390 ) ) ;
#65335=CARTESIAN_POINT ( 'NONE',  ( 18.91781669292794987, 48.00000000000000000, 62.18610382930901892 ) ) ;
#65340=LINE ( 'NONE', #49679, #19287 ) ;
#65343=ADVANCED_FACE ( 'NONE', ( #70746 ), #1329, .T. ) ;
#65347=CARTESIAN_POINT ( 'NONE',  ( 63.92823401217728474, 38.95221377027642973, 0.7461719994844789872 ) ) ;
#65366=CARTESIAN_POINT ( 'NONE',  ( -11.00613692184842485, -4.988161163938196196, -12.57568679169951054 ) ) ;
#65386=CARTESIAN_POINT ( 'NONE',  ( -6.786616733794230250, 41.72678875807561383, -59.11526074045958268 ) ) ;
#65405=CARTESIAN_POINT ( 'NONE',  ( 7.224854171662427049, 41.52722309002922429, -69.60668040565890635 ) ) ;
#65408=PRODUCT_DEFINITION ( 'UNKNOWN', '', #19877, #26277 ) ;
#65413=CARTESIAN_POINT ( 'NONE',  ( -6.503373625913253520, 41.93912930209143042, -59.84719177782724131 ) ) ;
#65416=CARTESIAN_POINT ( 'NONE',  ( -28.69358546713185021, 50.00000000000000000, 56.30708833178594830 ) ) ;
#65445=CARTESIAN_POINT ( 'NONE',  ( 12.13034742782428310, 42.00000299666817938, -93.82352941176471006 ) ) ;
#65446=B_SPLINE_CURVE_WITH_KNOTS ( 'NONE', 3,
 ( #11313, #22518, #47797, #103013, #85785, #39738, #44787, #72090 ),
 .UNSPECIFIED., .F., .F.,
 ( 4, 2, 2, 4 ),
 ( 0.000000000000000000, 0.2500000000000000000, 0.5000000000000000000, 1.000000000000000000 ),
 .UNSPECIFIED. ) ;
#65471=FILL_AREA_STYLE_COLOUR ( '', #75795 ) ;
#65483=FILL_AREA_STYLE_COLOUR ( '', #98846 ) ;
#65496=CARTESIAN_POINT ( 'NONE',  ( -10.51296777078104050, 50.00000000000000000, -92.64705882352942012 ) ) ;
#65501=CARTESIAN_POINT ( 'NONE',  ( -7.499999999999896971, 40.28819309265733750, -69.28872504362320228 ) ) ;
#65529=FILL_AREA_STYLE_COLOUR ( '', #14850 ) ;
#65552=AXIS2_PLACEMENT_3D ( 'NONE', #90080, #16724, #89027 ) ;
#65583=CARTESIAN_POINT ( 'NONE',  ( 17.50000000000003908, 51.97748320729017735, 60.75044042985544479 ) ) ;
#65592=CARTESIAN_POINT ( 'NONE',  ( -7.597212443346953670, -5.000000000001859846, -19.53267873631771323 ) ) ;
#65612=( BOUNDED_CURVE ( )  B_SPLINE_CURVE ( 2, ( #67842, #93184, #19351 ),
 .UNSPECIFIED., .F., .F. ) 
 B_SPLINE_CURVE_WITH_KNOTS ( ( 3, 3 ),
 ( 0.000000000000000000, 1.000000000000000000 ),
 .UNSPECIFIED. ) 
 CURVE ( )  GEOMETRIC_REPRESENTATION_ITEM ( )  RATIONAL_B_SPLINE_CURVE ( ( 1.000000000000000000, 1.857142857142858317, 1.000000000000000000 ) ) 
 REPRESENTATION_ITEM ( '' )  );
#65620=CARTESIAN_POINT ( 'NONE',  ( 28.89099332390834363, 48.00000000000000000, 58.53034795347323893 ) ) ;
#65644=CARTESIAN_POINT ( 'NONE',  ( 17.33910591856571770, 41.94145800377867062, -83.32002807799533173 ) ) ;
#65656=FACE_OUTER_BOUND ( 'NONE', #11713, .T. ) ;
#65673=ORIENTED_EDGE ( 'NONE', *, *, #48432, .T. ) ;
#65705=PRESENTATION_STYLE_ASSIGNMENT (( #74311 ) ) ;
#65773=FACE_BOUND ( 'NONE', #5260, .T. ) ;
#65799=CARTESIAN_POINT ( 'NONE',  ( -8.772759641400078578, -5.000000000000000888, -16.83842667730707277 ) ) ;
#65816=CARTESIAN_POINT ( 'NONE',  ( -1.590954574004046274, 50.00000000000000711, -73.00000000000002842 ) ) ;
#65817=CARTESIAN_POINT ( 'NONE',  ( -43.48668509622026335, 41.44578431664083951, -50.71569214715880491 ) ) ;
#65831=CARTESIAN_POINT ( 'NONE',  ( -19.03324747453609689, 49.57630456594476698, 61.85387798835519391 ) ) ;
#65835=CARTESIAN_POINT ( 'NONE',  ( -7.141975279369632723, -4.999999999999062972, -70.98863559356212249 ) ) ;
#65846=CARTESIAN_POINT ( 'NONE',  ( -33.48012358427683921, 40.64846154899619535, -61.62971572559018796 ) ) ;
#65853=CARTESIAN_POINT ( 'NONE',  ( -6.145467200819251019, -5.000000000000002665, -77.00333157709852117 ) ) ;
#65869=CARTESIAN_POINT ( 'NONE',  ( -13.05378511524491536, -5.000000000000000000, -85.14608070245081706 ) ) ;
#65881=CARTESIAN_POINT ( 'NONE',  ( -8.641101172624390259, -5.000000000000000888, -72.37542516940096959 ) ) ;
#65912=CARTESIAN_POINT ( 'NONE',  ( -7.109733192396788581, 41.69026681596732686, -59.69141549319190432 ) ) ;
#65913=CARTESIAN_POINT ( 'NONE',  ( 6.836424187873526570, 40.92324844684119967, -70.97025588743883873 ) ) ;
#65935=CARTESIAN_POINT ( 'NONE',  ( 7.245483083000110014, 40.92674623657338628, -70.53853222405051326 ) ) ;
#65965=CARTESIAN_POINT ( 'NONE',  ( -17.49999999999997513, 45.00000000000000711, 100.0000000000000000 ) ) ;
#65969=PRESENTATION_STYLE_ASSIGNMENT (( #8259 ) ) ;
#65976=B_SPLINE_CURVE_WITH_KNOTS ( 'NONE', 3,
 ( #81672, #6202, #105960, #24033, #31069, #16429, #49310, #82221, #6745, #96315, #72541, #22443, #55284, #63947, #80097, #39141, #56338, #104929 ),
 .UNSPECIFIED., .F., .F.,
 ( 4, 2, 2, 2, 2, 2, 2, 2, 4 ),
 ( 0.5000000000000000000, 0.5625000000000000000, 0.6250000000000000000, 0.6875000000000000000, 0.7500000000000000000, 0.8125000000000000000, 0.8750000000000000000, 0.9375000000000000000, 1.000000000000000000 ),
 .UNSPECIFIED. ) ;
#65993=CARTESIAN_POINT ( 'NONE',  ( 23.99113157947469332, 50.00000000000000000, -74.11764705882353610 ) ) ;
#65998=CARTESIAN_POINT ( 'NONE',  ( 5.363597346073513350, 41.33266196706048845, -58.39526881795627844 ) ) ;
#66013=CARTESIAN_POINT ( 'NONE',  ( 17.50000000000002842, 50.00000000000000000, 100.0000000000000000 ) ) ;
#66024=CARTESIAN_POINT ( 'NONE',  ( -7.179418352514219670, 41.32597165265336514, -70.21788016059471715 ) ) ;
#66034=CARTESIAN_POINT ( 'NONE',  ( -8.716351559231869217, -5.000000000000000000, -5.062179317052287075 ) ) ;
#66052=CARTESIAN_POINT ( 'NONE',  ( 39.23171889029396198, 39.86656303868996076, -53.99799529535449238 ) ) ;
#66058=CARTESIAN_POINT ( 'NONE',  ( 12.50000000000000711, 39.79061977335776845, -65.15808776970733618 ) ) ;
#66100=CARTESIAN_POINT ( 'NONE',  ( 6.690415142086856726, 41.73276191905608812, -59.04972836783017698 ) ) ;
#66105=CARTESIAN_POINT ( 'NONE',  ( 14.91270732344407257, 41.98564553269472555, -86.62216337287246404 ) ) ;
#66110=CARTESIAN_POINT ( 'NONE',  ( 19.50000000000160583, 49.99999999999990052, 59.86364615470513684 ) ) ;
#66119=CARTESIAN_POINT ( 'NONE',  ( -6.109877454823899434, -4.349879335532910396, -16.82893417409533399 ) ) ;
#66142=FILL_AREA_STYLE_COLOUR ( '', #15219 ) ;
#66153=CARTESIAN_POINT ( 'NONE',  ( -12.50000000000000711, 18.64303733123573537, -36.27143273323382999 ) ) ;
#66165=CARTESIAN_POINT ( 'NONE',  ( 17.73673397241445926, 41.93065142196708450, -82.77986825849473007 ) ) ;
#66168=DIRECTION ( 'NONE',  ( 0.000000000000000000, 0.000000000000000000, 1.000000000000000000 ) ) ;
#66224=CARTESIAN_POINT ( 'NONE',  ( -17.49999999999997513, 49.32716648907489088, 64.00616971907881236 ) ) ;
#66233=ORIENTED_EDGE ( 'NONE', *, *, #20675, .F. ) ;
#66234=CARTESIAN_POINT ( 'NONE',  ( 12.50000000000000355, -79.93083296558610584, -76.70843802411151557 ) ) ;
#66268=CARTESIAN_POINT ( 'NONE',  ( -6.701893397842001221, 41.44328394191487774, -70.59544911652842814 ) ) ;
#66269=CARTESIAN_POINT ( 'NONE',  ( -18.91791044776116237, 45.00000000000000711, 62.18611311450884926 ) ) ;
#66294=CARTESIAN_POINT ( 'NONE',  ( -2.912673042965788187E-14, 42.00000000000000000, -90.56128410203886858 ) ) ;
#66308=ORIENTED_EDGE ( 'NONE', *, *, #36515, .T. ) ;
#66326=CARTESIAN_POINT ( 'NONE',  ( -9.370229349454282541, -5.000000000000000000, -18.71807701186707362 ) ) ;
#66343=CARTESIAN_POINT ( 'NONE',  ( 9.891797161801495264, -3.000000000000002665, -73.72381496649795452 ) ) ;
#66344=CARTESIAN_POINT ( 'NONE',  ( -37.15195575618992763, 42.30491125877714609, -59.42450515948280554 ) ) ;
#66359=CARTESIAN_POINT ( 'NONE',  ( -17.50000000000567368, 50.03761058180953825, 61.36442103424013794 ) ) ;
#66373=CARTESIAN_POINT ( 'NONE',  ( -33.10889724926384758, 40.69544138183375992, -62.12314050178786573 ) ) ;
#66379=CARTESIAN_POINT ( 'NONE',  ( 1.308996937480706890, -4.999999999999988454, -95.00000000000001421 ) ) ;
#66383=CARTESIAN_POINT ( 'NONE',  ( 5.308064239167483045, 41.67430808361709182, -70.56675995020944470 ) ) ;
#66402=CARTESIAN_POINT ( 'NONE',  ( -11.60300946697521063, 38.95405707135367379, 62.66999883219498457 ) ) ;
#66418=CARTESIAN_POINT ( 'NONE',  ( -10.93463539379134630, -4.991620506566409432, -12.57231523659326555 ) ) ;
#66422=EDGE_CURVE ( 'NONE', #58075, #36, #98890, .T. ) ;
#66436=VERTEX_POINT ( 'NONE', #93002 ) ;
#66470=CARTESIAN_POINT ( 'NONE',  ( -62.09744855146975340, 49.99999999999997868, -11.13337886142409694 ) ) ;
#66480=CARTESIAN_POINT ( 'NONE',  ( 36.90124019532461119, 18.64284798592713344, 10.73407659160235639 ) ) ;
#66487=AXIS2_PLACEMENT_3D ( 'NONE', #5481, #97651, #4957 ) ;
#66490=ORIENTED_EDGE ( 'NONE', *, *, #103971, .T. ) ;
#66492=CARTESIAN_POINT ( 'NONE',  ( 13.44208458454186150, 42.84831587751688886, -92.02018896800140624 ) ) ;
#66500=CARTESIAN_POINT ( 'NONE',  ( -7.500000000000005329, 44.25000000000000000, -68.91429205785459544 ) ) ;
#66502=MECHANICAL_DESIGN_GEOMETRIC_PRESENTATION_REPRESENTATION('',(#75106),#94077);
#66507=CARTESIAN_POINT ( 'NONE',  ( 2.850615045022827587, -4.999999999999999112, -72.23577364510627774 ) ) ;
#66556=CARTESIAN_POINT ( 'NONE',  ( -7.187173619203170993, 40.29457790443799325, -70.92326292136544907 ) ) ;
#66564=CARTESIAN_POINT ( 'NONE',  ( 0.000000000000000000, 50.00000000000000000, 0.000000000000000000 ) ) ;
#66565=CARTESIAN_POINT ( 'NONE',  ( -9.743117168496159053, -5.000000000000000000, -2.583982984173456288 ) ) ;
#66571=ORIENTED_EDGE ( 'NONE', *, *, #98111, .T. ) ;
#66591=CARTESIAN_POINT ( 'NONE',  ( 12.50000000000000711, 27.21546065502551315, -44.75725117832055133 ) ) ;
#66605=CARTESIAN_POINT ( 'NONE',  ( 17.50000000000002487, 49.38220963225677451, 64.00838255298897650 ) ) ;
#66650=CARTESIAN_POINT ( 'NONE',  ( -5.668939695963768344, 41.88723863199725628, -59.02759498664629945 ) ) ;
#66654=ORIENTED_EDGE ( 'NONE', *, *, #86669, .F. ) ;
#66670=CARTESIAN_POINT ( 'NONE',  ( -7.499940182180696802, -3.043015538681149934, -20.22995127276119476 ) ) ;
#66675=AXIS2_PLACEMENT_3D ( 'NONE', #69347, #102225, #61251 ) ;
#66682=CARTESIAN_POINT ( 'NONE',  ( -63.03617022295203753, 48.00000000000000000, -16.93907820454660396 ) ) ;
#66708=CARTESIAN_POINT ( 'NONE',  ( 19.05374491087241751, 41.88689941110012427, -80.99294598599399819 ) ) ;
#66720=CARTESIAN_POINT ( 'NONE',  ( -6.616218520611202081, 40.56071393578208273, -71.17595756557476250 ) ) ;
#66742=UNCERTAINTY_MEASURE_WITH_UNIT (LENGTH_MEASURE( 1.000000000000000082E-05 ), #64712, 'distance_accuracy_value', 'NONE');
#66766=CARTESIAN_POINT ( 'NONE',  ( -7.125691916582566954, 41.67430808341742932, -69.26730091582949456 ) ) ;
#66807=ORIENTED_EDGE ( 'NONE', *, *, #40082, .T. ) ;
#66816=CARTESIAN_POINT ( 'NONE',  ( -6.706751634816551011, 41.66489468247179673, -58.91094301962639435 ) ) ;
#66831=DIRECTION ( 'NONE',  ( 0.000000000000000000, 1.000000000000000000, 0.000000000000000000 ) ) ;
#66834=CARTESIAN_POINT ( 'NONE',  ( 11.85444436799972934, 42.00000000000000000, 90.56128410203886858 ) ) ;
#66882=EDGE_CURVE ( 'NONE', #21082, #57829, #855, .T. ) ;
#66907=CARTESIAN_POINT ( 'NONE',  ( -18.97029851426740521, 49.42830426956749790, 61.97293826772175152 ) ) ;
#66924=CARTESIAN_POINT ( 'NONE',  ( -33.14954961147306278, 40.69031475660899133, -62.06908864790394631 ) ) ;
#66929=CARTESIAN_POINT ( 'NONE',  ( -9.999999999999996447, -3.000000000000002665, -86.30899693747677759 ) ) ;
#66952=EDGE_LOOP ( 'NONE', ( #78968, #104495, #69066, #17905 ) ) ;
#66964=B_SPLINE_CURVE_WITH_KNOTS ( 'NONE', 3,
 ( #30318, #39467, #63745, #22235, #46485, #89068, #31396, #46999, #48053, #105767, #95057, #13032, #45959, #78841, #21708, #4969, #37899, #70759, #54545, #5496, #99253, #57733, #82563, #25974, #106282, #65846, #73385, #32448, #66924, #91729, #90124, #66373, #8667, #73926, #8132, #58834, #7, #25425, #32976, #42630, #58283, #74981, #1072, #41570, #57205, #23834, #48584, #99804, #65320, #91209, #56678, #17316, #74456, #49655, #90657, #50191, #31908, #98725, #24361, #7589, #34047, #83093, #536, #17847, #33496, #50697, #9186, #83612, #9716, #42095 ),
 .UNSPECIFIED., .F., .F.,
 ( 4, 2, 2, 2, 1, 1, 1, 1, 1, 2, 2, 2, 2, 2, 2, 1, 1, 1, 1, 1, 2, 2, 2, 2, 2, 2, 1, 1, 1, 1, 1, 1, 2, 2, 2, 2, 2, 2, 1, 1, 1, 1, 2, 2, 4 ),
 ( 0.000000000000000000, 0.1250000000002316758, 0.1875000000003474998, 0.2187500000004056477, 0.2343750000004347356, 0.2421875000004492517, 0.2460937500004567458, 0.2480468750004604095, 0.2490234375004621026, 0.2495117187504630463, 0.2500000000004640177, 0.3750000000006326606, 0.4375000000007171486, 0.4687500000007595036, 0.4843750000007807088, 0.4921875000007913670, 0.4960937500007965850, 0.4980468750007990830, 0.4990234375008003043, 0.4995117187508010814, 0.4997558593758013035, 0.5000000000008014700, 0.6250000000008512080, 0.6875000000008759660, 0.7187500000008880674, 0.7343750000008941736, 0.7421875000008971712, 0.7460937500008987255, 0.7480468750008993917, 0.7490234375008996137, 0.7495117187508999468, 0.7497558593759003909, 0.7498779296884003909, 0.7500000000009003909, 0.8125000000007255307, 0.8437500000006383782, 0.8593750000005944134, 0.8671875000005724310, 0.8710937500005613288, 0.8730468750005559997, 0.8740234375005532241, 0.8745117187505518919, 0.8747558593755512257, 0.8750000000005505596, 1.000000000000000000 ),
 .UNSPECIFIED. ) ;
#67015=CARTESIAN_POINT ( 'NONE',  ( -62.01418705506001317, 38.95383793061829891, 16.66584972140498166 ) ) ;
#67028=CIRCLE ( 'NONE', #48049, 65.00000000000000000 ) ;
#67079=SURFACE_STYLE_USAGE ( .BOTH. , #75142 ) ;
#67097=CARTESIAN_POINT ( 'NONE',  ( -7.312789287434840801, 41.37363159257076006, -69.62136469306526010 ) ) ;
#67106=CARTESIAN_POINT ( 'NONE',  ( -1.309314578950586894, -5.000000000000000888, 10.00000000000000178 ) ) ;
#67117=VERTEX_POINT ( 'NONE', #37862 ) ;
#67119=B_SPLINE_CURVE_WITH_KNOTS ( 'NONE', 3,
 ( #14286, #32640, #64977, #80088, #89790, #81663, #64463, #48245 ),
 .UNSPECIFIED., .F., .F.,
 ( 4, 2, 2, 4 ),
 ( 0.000000000000000000, 0.2500000000000000000, 0.5000000000000000000, 1.000000000000000000 ),
 .UNSPECIFIED. ) ;
#67131=ORIENTED_EDGE ( 'NONE', *, *, #25141, .F. ) ;
#67133=EDGE_CURVE ( 'NONE', #19635, #21082, #80747, .T. ) ;
#67145=CARTESIAN_POINT ( 'NONE',  ( -14.91271302809441401, 41.98564543112699710, -86.62215342991694911 ) ) ;
#67154=CARTESIAN_POINT ( 'NONE',  ( 7.500000000000000888, -4.999999999999999112, -20.99851272547259384 ) ) ;
#67167=CARTESIAN_POINT ( 'NONE',  ( -5.461524205193410531, 41.98576152084350355, -59.47047328349175643 ) ) ;
#67175=B_SPLINE_CURVE_WITH_KNOTS ( 'NONE', 3,
 ( #8346, #98935, #73603, #59044, #41782, #33715, #41250, #66058, #106507, #15914, #75197, #91414, #25095, #18061, #33188, #24573, #223, #82774, #17527, #90335, #16442, #49326, #50919, #1293, #83831, #57952, #42847, #9940, #16990, #49868, #34795, #1838, #48792, #7807, #82233, #66591, #99472, #25646, #9391, #58510, #50390 ),
 .UNSPECIFIED., .F., .F.,
 ( 4, 1, 1, 1, 1, 1, 1, 1, 1, 2, 2, 1, 1, 1, 1, 1, 1, 1, 1, 2, 2, 1, 1, 1, 1, 1, 1, 1, 1, 1, 2, 2, 4 ),
 ( 0.000000000000000000, 0.1249999999999719946, 0.1874999999999580336, 0.2187499999999505951, 0.2343749999999464040, 0.2421874999999438782, 0.2460937499999431288, 0.2480468749999432398, 0.2490234374999432954, 0.2495117187499428235, 0.2499999999999423517, 0.3749999999998880340, 0.4374999999998607225, 0.4687499999998471223, 0.4843749999998406275, 0.4921874999998376854, 0.4960937499998361866, 0.4980468749998355205, 0.4990234374998349098, 0.4995117187498344657, 0.4999999999998340217, 0.6249999999998132605, 0.6874999999998030464, 0.7187499999997978284, 0.7343749999997949418, 0.7421874999997936095, 0.7460937499997929434, 0.7480468749997928324, 0.7490234374997926103, 0.7495117187497924993, 0.7497558593747926103, 0.7499999999997927214, 1.000000000000000000 ),
 .UNSPECIFIED. ) ;
#67194=CARTESIAN_POINT ( 'NONE',  ( -5.420469775605653240, 41.88321586335170821, -59.04137891894602319 ) ) ;
#67200=CARTESIAN_POINT ( 'NONE',  ( 5.041270396327364622, 41.82074884801023984, -70.25592674792672199 ) ) ;
#67215=CARTESIAN_POINT ( 'NONE',  ( -7.101747359475742982, -4.047770588416829796, -17.37629258578624203 ) ) ;
#67226=CARTESIAN_POINT ( 'NONE',  ( -50.18984356160270011, 50.00000000000000000, 38.51389699557558544 ) ) ;
#67269=CARTESIAN_POINT ( 'NONE',  ( -9.739726766104316980, 49.99999999999999289, -87.61747884499031613 ) ) ;
#67291=STYLED_ITEM ( 'NONE', ( #79184 ), #102995 ) ;
#67328=DIRECTION ( 'NONE',  ( 5.329070518200750605E-15, 0.000000000000000000, -1.000000000000000000 ) ) ;
#67334=B_SPLINE_CURVE_WITH_KNOTS ( 'NONE', 3,
 ( #39028, #70331, #6103, #88107, #63308, #104272, #30960, #21278, #95146, #22861, #21804, #78410, #46056, #71910, #54116, #56224, #30415, #104811, #4524, #55698, #103750, #79470, #103229, #39565, #63836, #88629, #54643, #37469, #78941, #79994, #38507, #29372, #47092, #5063, #96205, #95665, #62261, #6638, #22334, #14719, #55181 ),
 .UNSPECIFIED., .F., .F.,
 ( 4, 1, 1, 1, 1, 1, 1, 1, 1, 1, 2, 2, 1, 1, 1, 1, 1, 1, 1, 1, 2, 2, 1, 1, 1, 1, 1, 1, 1, 1, 2, 2, 4 ),
 ( 0.000000000000000000, 0.1250000000000022482, 0.1875000000000033029, 0.2187500000000036915, 0.2343750000000039413, 0.2421875000000038858, 0.2460937500000036637, 0.2480468750000034694, 0.2490234375000036360, 0.2495117187500037470, 0.2497558593750039968, 0.2500000000000042188, 0.3750000000000879297, 0.4375000000001293410, 0.4687500000001500466, 0.4843750000001602052, 0.4921875000001652567, 0.4960937500001676437, 0.4980468750001689759, 0.4990234375001694755, 0.4995117187501696976, 0.5000000000001699751, 0.6250000000002530198, 0.6875000000002948752, 0.7187500000003157474, 0.7343750000003267386, 0.7421875000003321787, 0.7460937500003348433, 0.7480468750003361755, 0.7490234375003363976, 0.7495117187503365086, 0.7500000000003367306, 1.000000000000000000 ),
 .UNSPECIFIED. ) ;
#67348=CARTESIAN_POINT ( 'NONE',  ( 0.000000000000000000, 47.00000000000000000, -56.99999999999999289 ) ) ;
#67371=FILL_AREA_STYLE_COLOUR ( '', #29098 ) ;
#67374=CARTESIAN_POINT ( 'NONE',  ( 18.91791044776121211, 44.85000000000000853, 62.18611311450882795 ) ) ;
#67375=DIRECTION ( 'NONE',  ( 0.000000000000000000, 0.000000000000000000, -1.000000000000000000 ) ) ;
#67381=CARTESIAN_POINT ( 'NONE',  ( 6.263553873705014041, 41.61160258182582083, -58.64895314702076945 ) ) ;
#67392=CARTESIAN_POINT ( 'NONE',  ( 5.075566108724594017, -4.332661967060489339, -17.09624963492156269 ) ) ;
#67416=ORIENTED_EDGE ( 'NONE', *, *, #71716, .F. ) ;
#67425=CARTESIAN_POINT ( 'NONE',  ( -9.920059540012950094, -3.000000000000003109, -96.33176891503234174 ) ) ;
#67443=CARTESIAN_POINT ( 'NONE',  ( -17.49999999999995381, 48.00000000000000000, 62.61753806507839215 ) ) ;
#67484=VERTEX_POINT ( 'NONE', #31102 ) ;
#67493=CARTESIAN_POINT ( 'NONE',  ( 19.49642740850473999, 49.99975891507487091, 59.99140731955566963 ) ) ;
#67500=CARTESIAN_POINT ( 'NONE',  ( -11.47300386045560749, -4.941189186712652059, -12.56866361833190915 ) ) ;
#67504=CARTESIAN_POINT ( 'NONE',  ( -5.243676916559595114, 9.267627703000917094, -29.53296413887904848 ) ) ;
#67519=FACE_OUTER_BOUND ( 'NONE', #8524, .T. ) ;
#67520=CARTESIAN_POINT ( 'NONE',  ( -7.081808430652881903, 41.46696591259760112, -58.88886595218312436 ) ) ;
#67540=CARTESIAN_POINT ( 'NONE',  ( -9.596002107492989097, -5.000000000000002665, -77.62543935900905012 ) ) ;
#67551=CARTESIAN_POINT ( 'NONE',  ( -4.852941176470586093, 40.00000000000132871, -70.80672828634229177 ) ) ;
#67562=CARTESIAN_POINT ( 'NONE',  ( 28.08715220166955007, 18.64284798592788306, 26.23039857546442732 ) ) ;
#67589=CARTESIAN_POINT ( 'NONE',  ( -7.500000000000006217, 39.99999999999122480, -59.88032989330939415 ) ) ;
#67604=CARTESIAN_POINT ( 'NONE',  ( 79.13121736040859844, 42.00000000000000000, -45.60838156035022450 ) ) ;
#67610=EDGE_LOOP ( 'NONE', ( #32733, #14180, #62436, #67885 ) ) ;
#67612=CARTESIAN_POINT ( 'NONE',  ( -5.921510830615929422, 40.83857583775533584, 64.79874045254685200 ) ) ;
#67630=CARTESIAN_POINT ( 'NONE',  ( -9.999999999999989342, 49.99999999999999289, -83.69100306251235111 ) ) ;
#67635=CARTESIAN_POINT ( 'NONE',  ( -7.316989450287470831, 41.06054039135568701, -70.27554050036877697 ) ) ;
#67671=CARTESIAN_POINT ( 'NONE',  ( 5.383907448094620740, 41.54392475608550939, -58.58678525159944428 ) ) ;
#67692=CARTESIAN_POINT ( 'NONE',  ( 5.367391215540106231, 43.24496486319787181, -60.11082976391321608 ) ) ;
#67718=CARTESIAN_POINT ( 'NONE',  ( -6.676660803729373761, 41.76849044449239301, -59.12256534660619423 ) ) ;
#67722=ADVANCED_FACE ( 'NONE', ( #102702 ), #92873, .T. ) ;
#67727=CARTESIAN_POINT ( 'NONE',  ( 17.50000000000002842, 50.00000000000000000, 63.82142195508322402 ) ) ;
#67748=CARTESIAN_POINT ( 'NONE',  ( 39.04923757937011430, 50.00000000002003731, 52.30342408740191473 ) ) ;
#67771=CARTESIAN_POINT ( 'NONE',  ( 24.97083012527267343, 41.55031761159468573, -72.99854779811836636 ) ) ;
#67788=CARTESIAN_POINT ( 'NONE',  ( -9.596002107488990518, 50.00000000000000000, -92.37456064098950037 ) ) ;
#67790=VERTEX_POINT ( 'NONE', #23943 ) ;
#67802=EDGE_CURVE ( 'NONE', #24664, #70585, #20046, .T. ) ;
#67841=( BOUNDED_SURFACE ( )  B_SPLINE_SURFACE ( 2, 3, ( 
 ( #77325, #4496, #44431, #37433 ),
 ( #3438, #95114, #79439, #44974 ),
 ( #52502, #11503, #3969, #28277 ) ),
 .UNSPECIFIED., .F., .F., .F. ) 
 B_SPLINE_SURFACE_WITH_KNOTS ( ( 3, 3 ),
 ( 4, 4 ),
 ( 0.000000000000000000, 1.000000000000000000 ),
 ( -0.05487404235502676975, -0.006958263022644777668 ),
 .UNSPECIFIED. ) 
 GEOMETRIC_REPRESENTATION_ITEM ( )  RATIONAL_B_SPLINE_SURFACE ( (
 ( 1.000000000000000000, 1.000000000000000000, 1.000000000000000000, 1.000000000000000000),
 ( 1.857142857142858317, 1.857142857142858317, 1.857142857142858317, 1.857142857142858317),
 ( 1.000000000000000000, 1.000000000000000000, 1.000000000000000000, 1.000000000000000000) ) ) 
 REPRESENTATION_ITEM ( '' )  SURFACE ( )  );
#67842=CARTESIAN_POINT ( 'NONE',  ( -14.33580413386536812, 42.00000000000000000, -89.41414995615788541 ) ) ;
#67851=B_SPLINE_CURVE_WITH_KNOTS ( 'NONE', 3,
 ( #86954, #79361, #5482, #70221 ),
 .UNSPECIFIED., .F., .F.,
 ( 4, 4 ),
 ( 0.000000000000000000, 1.000000000000000000 ),
 .UNSPECIFIED. ) ;
#67885=ORIENTED_EDGE ( 'NONE', *, *, #77241, .T. ) ;
#67889=CARTESIAN_POINT ( 'NONE',  ( 0.000000000000000000, -79.93083296558610584, -85.00000000000000000 ) ) ;
#67892=CARTESIAN_POINT ( 'NONE',  ( 79.13121736037263076, 42.00000000000000000, 45.60838156036771096 ) ) ;
#67894=B_SPLINE_SURFACE_WITH_KNOTS ( 'NONE', 3, 3, ( 
 ( #33404, #9089, #74878, #84059, #10160, #100758, #41999, #75962 ),
 ( #17741, #26927, #59800, #2594, #68419, #18834, #101313, #51678 ),
 ( #84599, #966, #66816, #99705, #25876, #58732, #50601, #91631 ),
 ( #83516, #9616, #28511, #93215, #13335, #61395, #68958, #93751 ),
 ( #4738, #45214, #86736, #78088, #30095, #4207, #11743, #12811 ),
 ( #94284, #54313, #19903, #20450, #102903, #53291, #19379, #85123 ),
 ( #44680, #20973, #37136, #70539, #103949, #45725, #52210, #86212 ),
 ( #37677, #87260, #46261, #78607, #38198, #103430, #3682, #79147 ),
 ( #29067, #29579, #61937, #11207, #52746, #62451, #94827, #71058 ),
 ( #95342, #70002, #27994, #12284, #53807, #101829, #21478, #5273 ) ),
 .UNSPECIFIED., .F., .F., .F.,
 ( 4, 2, 2, 2, 4 ),
 ( 4, 2, 2, 4 ),
 ( 0.000000000000000000, 0.1250000000000000000, 0.2500000000000000000, 0.5000000000000000000, 1.000000000000000000 ),
 ( 0.000000000000000000, 0.2500000000000000000, 0.5000000000000000000, 1.000000000000000000 ),
 .UNSPECIFIED. ) ;
#67901=CARTESIAN_POINT ( 'NONE',  ( 6.810575959914616284, 41.35122729146528542, -58.50275608815579176 ) ) ;
#67902=CARTESIAN_POINT ( 'NONE',  ( -5.500000000000007994, 42.00000000000000000, -72.67206406577980715 ) ) ;
#67911=CARTESIAN_POINT ( 'NONE',  ( -1.719443193057841768, -4.999999999999999112, -17.47055129847369770 ) ) ;
#67944=CARTESIAN_POINT ( 'NONE',  ( -5.499265899526136536, -3.000000000000002665, -99.22427370006747083 ) ) ;
#67945=CARTESIAN_POINT ( 'NONE',  ( -12.57956330988036164, -3.000000000000003109, -93.28077019085830557 ) ) ;
#67993=SURFACE_STYLE_USAGE ( .BOTH. , #98361 ) ;
#68003=( BOUNDED_SURFACE ( )  B_SPLINE_SURFACE ( 2, 3, ( 
 ( #44485, #67692, #45024, #13681, #61745, #20786, #62790, #46074, #77909, #4017 ),
 ( #80010, #88128, #21825, #54662, #30977, #70874, #46591, #103244, #78422, #79490 ),
 ( #78957, #71386, #6120, #5601, #14209, #21294, #102710, #38524, #104286, #29389 ) ),
 .UNSPECIFIED., .F., .F., .F. ) 
 B_SPLINE_SURFACE_WITH_KNOTS ( ( 3, 3 ),
 ( 4, 2, 2, 2, 4 ),
 ( 0.000000000000000000, 1.000000000000000000 ),
 ( 0.2013554496957829509, 0.2052093776119387758, 0.2375733647630427492, 0.2537553583385947498, 0.2699373519141466948 ),
 .UNSPECIFIED. ) 
 GEOMETRIC_REPRESENTATION_ITEM ( )  RATIONAL_B_SPLINE_SURFACE ( (
 ( 1.000000000000000000, 1.000000000000000000, 1.000000000000000000, 1.000000000000000000, 1.000000000000000000, 1.000000000000000000, 1.000000000000000000, 1.000000000000000000, 1.000000000000000000, 1.000000000000000000),
 ( 1.857142857142858317, 1.857142857142858317, 1.857142857142858317, 1.857142857142858317, 1.857142857142858317, 1.857142857142858317, 1.857142857142857428, 1.857142857142857428, 1.857142857142858317, 1.857142857142858317),
 ( 1.000000000000000000, 1.000000000000000000, 1.000000000000000000, 1.000000000000000000, 1.000000000000000000, 1.000000000000000000, 1.000000000000000000, 1.000000000000000000, 1.000000000000000000, 1.000000000000000000) ) ) 
 REPRESENTATION_ITEM ( '' )  SURFACE ( )  );
#68031=ORIENTED_EDGE ( 'NONE', *, *, #64030, .F. ) ;
#68036=CARTESIAN_POINT ( 'NONE',  ( -7.500000000000007105, 40.28750026290749275, -59.87155394325278479 ) ) ;
#68095=CARTESIAN_POINT ( 'NONE',  ( -7.500000000000005329, -5.250000000000004441, -68.91429205785459544 ) ) ;
#68101=CARTESIAN_POINT ( 'NONE',  ( 18.92174722983540391, 48.90933038775173003, 62.13887004286578275 ) ) ;
#68130=CARTESIAN_POINT ( 'NONE',  ( 55.21757201740613397, 40.83935004233791943, 34.80653877613059421 ) ) ;
#68151=CARTESIAN_POINT ( 'NONE',  ( -6.145467200818548470, 49.99999999999999289, -77.00333157709850695 ) ) ;
#68154=ORIENTED_EDGE ( 'NONE', *, *, #37050, .T. ) ;
#68186=CARTESIAN_POINT ( 'NONE',  ( -17.53271835666959788, 45.00000000000000711, 63.43174741287191409 ) ) ;
#68236=CARTESIAN_POINT ( 'NONE',  ( 9.999999999999998224, 47.99999999999999289, -86.30899693899574743 ) ) ;
#68243=CARTESIAN_POINT ( 'NONE',  ( 28.89099332390834363, 48.00000000000000000, 58.53034795347323893 ) ) ;
#68250=CARTESIAN_POINT ( 'NONE',  ( -6.346112372205309882, 41.86049372390779411, -59.13213685944749898 ) ) ;
#68258=CARTESIAN_POINT ( 'NONE',  ( -5.309984767906265724, -5.000000000000680345, -15.43787989249558734 ) ) ;
#68280=CARTESIAN_POINT ( 'NONE',  ( 6.996268247851322286, 41.79455473942780230, -69.25931863577100955 ) ) ;
#68281=ADVANCED_FACE ( 'NONE', ( #53877 ), #95869, .T. ) ;
#68283=CARTESIAN_POINT ( 'NONE',  ( -62.91825180719953892, 50.00000000000000000, 6.605622457240398759 ) ) ;
#68296=CARTESIAN_POINT ( 'NONE',  ( -23.07257312862554599, 18.64284798593020298, 30.73399254005029135 ) ) ;
#68309=CARTESIAN_POINT ( 'NONE',  ( 43.89937922080078891, 39.34350223877356001, -47.75665600345389805 ) ) ;
#68325=CARTESIAN_POINT ( 'NONE',  ( 12.13034742782427955, 48.00000000000000000, -93.82352941176471006 ) ) ;
#68327=CARTESIAN_POINT ( 'NONE',  ( -10.48543666094594684, 50.00000000000000000, -78.95657223723274853 ) ) ;
#68341=EDGE_CURVE ( 'NONE', #81898, #91293, #85739, .T. ) ;
#68397=ORIENTED_EDGE ( 'NONE', *, *, #20611, .T. ) ;
#68413=FACE_OUTER_BOUND ( 'NONE', #54119, .T. ) ;
#68414=CARTESIAN_POINT ( 'NONE',  ( -6.764423789826284228, 41.48989065997112391, -70.49176070234911151 ) ) ;
#68419=CARTESIAN_POINT ( 'NONE',  ( -6.873632436824210323, 41.52279939058548308, -58.77795267647356781 ) ) ;
#68437=CARTESIAN_POINT ( 'NONE',  ( -19.32152200341433357, 18.64316884707570310, 33.52312678237270660 ) ) ;
#68445=CARTESIAN_POINT ( 'NONE',  ( 7.006861261201393631, 41.19339584001859578, -58.48462847601448544 ) ) ;
#68446=CARTESIAN_POINT ( 'NONE',  ( -7.500000000000007994, 40.00000000000000000, -71.41947339646975479 ) ) ;
#68466=CARTESIAN_POINT ( 'NONE',  ( 7.432466292033693023, 40.29241581942148542, -70.20618918290337263 ) ) ;
#68532=CARTESIAN_POINT ( 'NONE',  ( -1.308996937483428269, -3.000000000000002665, -75.00000000000001421 ) ) ;
#68540=CARTESIAN_POINT ( 'NONE',  ( 18.00094660900708377, -4.332661967061082642, 2.683237397146490011 ) ) ;
#68552=ADVANCED_FACE ( 'NONE', ( #45563 ), #10483, .T. ) ;
#68557=EDGE_LOOP ( 'NONE', ( #15455, #61519, #14780, #25635, #74884, #75989, #11807, #28312, #36711, #78911, #66807, #90964 ) ) ;
#68563=CARTESIAN_POINT ( 'NONE',  ( 16.52731600354976749, 43.98685737190850631, -87.77869701378344303 ) ) ;
#68565=CARTESIAN_POINT ( 'NONE',  ( 6.827804075408431927, -2.999999999999529265, -71.19745151638494463 ) ) ;
#68575=CARTESIAN_POINT ( 'NONE',  ( -7.500000000000003553, 7.934965735923709573, -31.00258070019285839 ) ) ;
#68579=MECHANICAL_DESIGN_GEOMETRIC_PRESENTATION_REPRESENTATION('',(#97799),#59966);
#68590=CARTESIAN_POINT ( 'NONE',  ( -19.08521797759478744, 49.65371826308247449, 61.76473638255668419 ) ) ;
#68591=CARTESIAN_POINT ( 'NONE',  ( 4.966176485634620441, 41.64999999999997726, -70.47555195150160046 ) ) ;
#68594=CARTESIAN_POINT ( 'NONE',  ( -7.500000000000006217, 39.99999999999122480, -59.88032989330939415 ) ) ;
#68604=CARTESIAN_POINT ( 'NONE',  ( 5.233596130300162130, 8.457361458019045486, -28.79146962302072055 ) ) ;
#68607=CARTESIAN_POINT ( 'NONE',  ( 3.140345045834405546, -5.000000000000000000, -16.11513581654612537 ) ) ;
#68626=ADVANCED_FACE ( 'NONE', ( #8788 ), #69102, .T. ) ;
#68627=CARTESIAN_POINT ( 'NONE',  ( -4.966176470918042263, 41.64999999999998437, -70.47555194646970733 ) ) ;
#68643=CARTESIAN_POINT ( 'NONE',  ( 7.996316163938711696, -5.000000000000000000, 6.145999768513703110 ) ) ;
#68677=CARTESIAN_POINT ( 'NONE',  ( 55.65414010178471926, 42.00000000000000000, 72.41885610124163009 ) ) ;
#68684=CARTESIAN_POINT ( 'NONE',  ( 61.99203922365963138, 40.83832228034810186, -19.76974671391372596 ) ) ;
#68696=CARTESIAN_POINT ( 'NONE',  ( 8.169585525225409484, 39.99999999999999289, -72.41994148081866456 ) ) ;
#68717=CARTESIAN_POINT ( 'NONE',  ( 6.924711585765388477, 40.92328497145224020, -70.90711766198887744 ) ) ;
#68728=CARTESIAN_POINT ( 'NONE',  ( -6.890281280090280625, 41.03680257558234246, -70.85895802555796763 ) ) ;
#68732=ORIENTED_EDGE ( 'NONE', *, *, #58862, .F. ) ;
#68740=CARTESIAN_POINT ( 'NONE',  ( -18.19227789368855852, 45.00000000000000711, 62.45676960188954752 ) ) ;
#68750=CARTESIAN_POINT ( 'NONE',  ( 5.411617511166468830, 41.81753644224158251, -58.91471485095114247 ) ) ;
#68777=CARTESIAN_POINT ( 'NONE',  ( 11.87025963472306422, -4.834378162015144476, -12.56279239310862472 ) ) ;
#68783=CARTESIAN_POINT ( 'NONE',  ( 7.996668423981797780, 47.99999999999999289, -78.85453280025083700 ) ) ;
#68795=CARTESIAN_POINT ( 'NONE',  ( -6.492510984469592294, 41.78432685485347520, -59.03546988472429291 ) ) ;
#68826=( LENGTH_UNIT ( ) NAMED_UNIT ( * ) SI_UNIT ( .MILLI., .METRE. ) );
#68829=CARTESIAN_POINT ( 'NONE',  ( 6.335691922401378129, 41.93068719163046154, -69.89754162678619309 ) ) ;
#68830=CARTESIAN_POINT ( 'NONE',  ( 54.34415824577756382, 50.00000000000000000, -32.38913437803500983 ) ) ;
#68863=MECHANICAL_DESIGN_GEOMETRIC_PRESENTATION_REPRESENTATION('',(#8532),#10232);
#68872=CARTESIAN_POINT ( 'NONE',  ( 1.570796324980112679, 50.00000000000000000, -97.00000000000000000 ) ) ;
#68881=CARTESIAN_POINT ( 'NONE',  ( -6.145467199749145237, -3.000000000000002665, -92.99666842398180222 ) ) ;
#68914=CARTESIAN_POINT ( 'NONE',  ( 14.62196750106410015, 42.00000000000002132, -88.48477917736602194 ) ) ;
#68915=CARTESIAN_POINT ( 'NONE',  ( 6.106896958092508321, -4.373166921188613721, -16.80698729315718865 ) ) ;
#68952=CARTESIAN_POINT ( 'NONE',  ( -6.335691858987115843, 41.93068706802236534, -69.89754241407730717 ) ) ;
#68958=CARTESIAN_POINT ( 'NONE',  ( -6.810576809588133607, 41.35122479108419213, -58.50275420946741889 ) ) ;
#68965=CARTESIAN_POINT ( 'NONE',  ( -12.13034742782427955, 48.00000000000000000, -93.82352941176471006 ) ) ;
#68975=CARTESIAN_POINT ( 'NONE',  ( 7.040971602393473638, 41.74416448739698637, -59.82830749617803434 ) ) ;
#68976=CARTESIAN_POINT ( 'NONE',  ( -19.32152200348980742, 18.64316884709133504, -33.52312678235660570 ) ) ;
#68984=CARTESIAN_POINT ( 'NONE',  ( 6.670526534797884821, 41.45458331230783244, -58.55661123927227862 ) ) ;
#68990=FILL_AREA_STYLE ('',( #102399 ) ) ;
#69002=CARTESIAN_POINT ( 'NONE',  ( 17.50000000000002842, 45.00000000000000711, 64.09953197936602010 ) ) ;
#69003=CARTESIAN_POINT ( 'NONE',  ( 7.274972994441586849, 40.00000000291657187, -70.77553163430461325 ) ) ;
#69024=CARTESIAN_POINT ( 'NONE',  ( 5.499265899522581158, -4.999999999985523580, -99.22427370007513048 ) ) ;
#69063=CARTESIAN_POINT ( 'NONE',  ( -7.996668422906619611, -3.000000000000002665, -78.85453279917568636 ) ) ;
#69066=ORIENTED_EDGE ( 'NONE', *, *, #103844, .F. ) ;
#69070=CARTESIAN_POINT ( 'NONE',  ( 7.549954993183454199, -4.999999999999999112, -15.49602501671512833 ) ) ;
#69093=CARTESIAN_POINT ( 'NONE',  ( 6.931554132376503752, -2.999999999999883649, -71.13906995425703883 ) ) ;
#69099=ADVANCED_FACE ( 'NONE', ( #13558 ), #83557, .F. ) ;
#69102=( BOUNDED_SURFACE ( )  B_SPLINE_SURFACE ( 2, 3, ( 
 ( #89728, #64396, #25552, #65445 ),
 ( #23963, #90248, #72467, #57328 ),
 ( #74049, #48706, #25005, #57859 ) ),
 .UNSPECIFIED., .F., .F., .F. ) 
 B_SPLINE_SURFACE_WITH_KNOTS ( ( 3, 3 ),
 ( 4, 4 ),
 ( 0.000000000000000000, 1.000000000000000000 ),
 ( 0.01818793032717390401, 0.02264331519860534464 ),
 .UNSPECIFIED. ) 
 GEOMETRIC_REPRESENTATION_ITEM ( )  RATIONAL_B_SPLINE_SURFACE ( (
 ( 1.000000000000000000, 1.000000000000000000, 1.000000000000000000, 1.000000000000000000),
 ( 1.857142857142858317, 1.857142857142858317, 1.857142857142858317, 1.857142857142858317),
 ( 1.000000000000000000, 1.000000000000000000, 1.000000000000000000, 1.000000000000000000) ) ) 
 REPRESENTATION_ITEM ( '' )  SURFACE ( )  );
#69120=CARTESIAN_POINT ( 'NONE',  ( -18.96017730465335305, 49.36529653577810706, 62.00134825986546616 ) ) ;
#69121=CARTESIAN_POINT ( 'NONE',  ( -7.173661105156260653, 41.42016048193522693, -58.97621011332057606 ) ) ;
#69135=CARTESIAN_POINT ( 'NONE',  ( 5.299529629523134666, 19.77438493592522306, -39.01802436143358221 ) ) ;
#69141=FILL_AREA_STYLE ('',( #60524 ) ) ;
#69184=STYLED_ITEM ( 'NONE', ( #32688 ), #74164 ) ;
#69206=CARTESIAN_POINT ( 'NONE',  ( 55.65414010180120385, 42.00000000000000000, -72.41885610122511707 ) ) ;
#69216=CARTESIAN_POINT ( 'NONE',  ( -28.75499683032297327, 40.83805150464743861, 58.36934873979967620 ) ) ;
#69225=CARTESIAN_POINT ( 'NONE',  ( -8.169585525225413036, 39.99999999999999289, -72.41994148081866456 ) ) ;
#69234=CARTESIAN_POINT ( 'NONE',  ( -7.374560640988130800, 50.00000000000000000, -94.59600210748763516 ) ) ;
#69248=CARTESIAN_POINT ( 'NONE',  ( 7.036764705882354143, 40.00000000373363207, -71.06385277390853616 ) ) ;
#69259=CARTESIAN_POINT ( 'NONE',  ( -6.960057398333500345, 40.00000000008189716, -71.11869238929787684 ) ) ;
#69298=ADVANCED_FACE ( 'NONE', ( #105072 ), #62491, .F. ) ;
#69305=CARTESIAN_POINT ( 'NONE',  ( 7.150000000000005684, 41.64999999999999147, -68.91429206202190016 ) ) ;
#69312=CARTESIAN_POINT ( 'NONE',  ( 1.308996938995747872, 48.00000000000001421, -95.00000000000000000 ) ) ;
#69315=CARTESIAN_POINT ( 'NONE',  ( 6.145467199749145237, -3.000000000000003109, -92.99666842398180222 ) ) ;
#69324=CARTESIAN_POINT ( 'NONE',  ( -6.916167714701083824, 41.81554662627394237, -59.83173445090647391 ) ) ;
#69347=CARTESIAN_POINT ( 'NONE',  ( 52.56483885390523625, -79.93083296558610584, -38.23529411764706509 ) ) ;
#69358=CARTESIAN_POINT ( 'NONE',  ( -53.52139369739177255, 50.00000000000000000, 33.73130704865319274 ) ) ;
#69379=CARTESIAN_POINT ( 'NONE',  ( 30.61794937107824310, 40.99878234165733204, -65.44843078843095441 ) ) ;
#69383=VERTEX_POINT ( 'NONE', #45250 ) ;
#69384=ORIENTED_EDGE ( 'NONE', *, *, #22910, .T. ) ;
#69387=( LENGTH_UNIT ( ) NAMED_UNIT ( * ) SI_UNIT ( .MILLI., .METRE. ) );
#69394=CARTESIAN_POINT ( 'NONE',  ( 9.596002107491598210, 50.00000000000000000, -77.62543935901993564 ) ) ;
#69395=ADVANCED_FACE ( 'NONE', ( #4782 ), #78128, .F. ) ;
#69406=CARTESIAN_POINT ( 'NONE',  ( -7.996668423981797780, -3.000000000000003109, -91.14546719974914879 ) ) ;
#69411=CARTESIAN_POINT ( 'NONE',  ( -7.036764705882381676, 40.00000000007575807, -71.06385277390852195 ) ) ;
#69422=CARTESIAN_POINT ( 'NONE',  ( -5.171269539170080698, 1.677304854198049089, -22.62158602869747526 ) ) ;
#69430=( BOUNDED_CURVE ( )  B_SPLINE_CURVE ( 2, ( #104923, #81666, #38092 ),
 .UNSPECIFIED., .F., .F. ) 
 B_SPLINE_CURVE_WITH_KNOTS ( ( 3, 3 ),
 ( 0.000000000000000000, 1.000000000000000000 ),
 .UNSPECIFIED. ) 
 CURVE ( )  GEOMETRIC_REPRESENTATION_ITEM ( )  RATIONAL_B_SPLINE_CURVE ( ( 1.000000000000000000, 1.857142857142858317, 1.000000000000000000 ) ) 
 REPRESENTATION_ITEM ( '' )  );
#69440=CARTESIAN_POINT ( 'NONE',  ( -17.50570437742704044, 50.00000000000000711, 63.41904368646399348 ) ) ;
#69454=CARTESIAN_POINT ( 'NONE',  ( 2.078747088351101002, 50.00000000000000711, -97.99984157184401568 ) ) ;
#69459=CARTESIAN_POINT ( 'NONE',  ( 6.061808134801299985, 49.99999999999999289, -95.47796581436244878 ) ) ;
#69465=ORIENTED_EDGE ( 'NONE', *, *, #18520, .F. ) ;
#69474=CARTESIAN_POINT ( 'NONE',  ( -5.406990715186140051, 41.99999999999999289, -69.18631391233250838 ) ) ;
#69478=CARTESIAN_POINT ( 'NONE',  ( -16.21528977622788403, -5.000000000000000000, -2.627527450084738536 ) ) ;
#69482=LINE ( 'NONE', #22550, #89548 ) ;
#69484=ORIENTED_EDGE ( 'NONE', *, *, #61183, .F. ) ;
#69494=( NAMED_UNIT ( * ) PLANE_ANGLE_UNIT ( ) SI_UNIT ( $, .RADIAN. ) );
#69497=CARTESIAN_POINT ( 'NONE',  ( 37.36680950587120975, 18.64316884708630084, 10.04205104290988437 ) ) ;
#69508=CARTESIAN_POINT ( 'NONE',  ( 5.659804915025486771, 41.67004157394842423, -58.69865591471064192 ) ) ;
#69527=CARTESIAN_POINT ( 'NONE',  ( 7.493258622341705255, 40.28998690653781267, -69.65507372783751805 ) ) ;
#69530=CARTESIAN_POINT ( 'NONE',  ( 0.000000000000000000, -79.93083296558610584, -85.00000000000000000 ) ) ;
#69538=ORIENTED_EDGE ( 'NONE', *, *, #52450, .F. ) ;
#69547=CARTESIAN_POINT ( 'NONE',  ( 15.17227823171759837, -5.000000000000002665, -86.54073391195457532 ) ) ;
#69551=EDGE_CURVE ( 'NONE', #8947, #93003, #31484, .T. ) ;
#69563=ORIENTED_EDGE ( 'NONE', *, *, #15608, .T. ) ;
#69565=CARTESIAN_POINT ( 'NONE',  ( -17.50000000000003553, 51.60805965402929729, 62.32523305737346675 ) ) ;
#69597=CARTESIAN_POINT ( 'NONE',  ( -3.328192429499065685, -5.000000000000000000, 16.34245136408155830 ) ) ;
#69620=CARTESIAN_POINT ( 'NONE',  ( 7.500000017879060010, -5.000000000005163869, -69.80246344212856968 ) ) ;
#69641=CARTESIAN_POINT ( 'NONE',  ( -18.91882844845346767, 48.67754231730402381, 62.16217783403399721 ) ) ;
#69642=CARTESIAN_POINT ( 'NONE',  ( 6.661997535587873998, 40.29425722526258369, -71.19925417846640414 ) ) ;
#69657=CARTESIAN_POINT ( 'NONE',  ( 5.105411401488612277, -2.846505860404147104, -18.47274186656556338 ) ) ;
#69662=CARTESIAN_POINT ( 'NONE',  ( -11.99999999999999467, -5.000000000000002665, -83.42920367502566137 ) ) ;
#69691=CARTESIAN_POINT ( 'NONE',  ( 7.996135855217748833, -5.000000000000000000, -6.145819459791736605 ) ) ;
#69695=ORIENTED_EDGE ( 'NONE', *, *, #4269, .F. ) ;
#69700=SURFACE_STYLE_FILL_AREA ( #38406 ) ;
#69703=CARTESIAN_POINT ( 'NONE',  ( -4.707696486725459373, 48.00000000000000000, -99.43546650845934209 ) ) ;
#69710=CARTESIAN_POINT ( 'NONE',  ( 19.48249511158978464, 49.99632329422010457, 60.25369351552480168 ) ) ;
#69713=FILL_AREA_STYLE ('',( #4434 ) ) ;
#69715=CARTESIAN_POINT ( 'NONE',  ( 34.58711029377568735, 42.66036566261906415, -62.95058470269599127 ) ) ;
#69718=ORIENTED_EDGE ( 'NONE', *, *, #6613, .T. ) ;
#69720=EDGE_CURVE ( 'NONE', #27940, #78362, #85529, .T. ) ;
#69727=CARTESIAN_POINT ( 'NONE',  ( 59.23741894013591036, 42.00000000000000711, 7.754160006506985781 ) ) ;
#69734=CARTESIAN_POINT ( 'NONE',  ( -14.79739047843293598, 40.83920300364216160, 63.36299633484923532 ) ) ;
#69750=CARTESIAN_POINT ( 'NONE',  ( -5.036189802309416486, 49.99999999999999289, -76.26213611588271135 ) ) ;
#69779=CARTESIAN_POINT ( 'NONE',  ( -6.743821053489263306, 40.92373723432427113, -71.01439601632299059 ) ) ;
#69820=CARTESIAN_POINT ( 'NONE',  ( 12.29798915171414819, -4.463815859616105719, -12.75153713776963293 ) ) ;
#69824=CARTESIAN_POINT ( 'NONE',  ( 7.500000000000007105, 40.00000000000000000, -65.90297133634214788 ) ) ;
#69830=CARTESIAN_POINT ( 'NONE',  ( 7.996668423981797780, 48.00000000000000711, -91.14546719974913458 ) ) ;
#69846=CARTESIAN_POINT ( 'NONE',  ( -6.592587276917421413, 41.82481063595618309, -59.20696655526094787 ) ) ;
#69877=CARTESIAN_POINT ( 'NONE',  ( 6.804095789962234520, 41.75280167785350471, -69.96721248597626186 ) ) ;
#69901=CARTESIAN_POINT ( 'NONE',  ( 23.97277878003368201, 41.62145744130984326, -74.34290485744733701 ) ) ;
#69910=FACE_OUTER_BOUND ( 'NONE', #23628, .T. ) ;
#69920=FILL_AREA_STYLE_COLOUR ( '', #96905 ) ;
#69943=FILL_AREA_STYLE_COLOUR ( '', #48514 ) ;
#69945=CARTESIAN_POINT ( 'NONE',  ( -5.346335122799986905, 32.51462932279844864, -50.48019096095612923 ) ) ;
#69951=CARTESIAN_POINT ( 'NONE',  ( -6.890281280090280625, 41.03680257558234246, -70.85895802555796763 ) ) ;
#69960=CARTESIAN_POINT ( 'NONE',  ( -18.84132143639387280, 50.00000000000000000, 60.80075852822654525 ) ) ;
#69997=CARTESIAN_POINT ( 'NONE',  ( -6.546995956212704471, 41.93635053412784686, -69.23592160050631605 ) ) ;
#70001=CARTESIAN_POINT ( 'NONE',  ( 11.77492727325709332, -4.999999999999999112, -11.45403612798945403 ) ) ;
#70002=CARTESIAN_POINT ( 'NONE',  ( -5.415855499685822139, 41.85405045957928394, -58.97635199008218621 ) ) ;
#70020=CARTESIAN_POINT ( 'NONE',  ( 6.951447288752834019, 41.73217225470716585, -59.36631759480937376 ) ) ;
#70021=CARTESIAN_POINT ( 'NONE',  ( 51.76085035121451483, 41.99999999999999289, 29.83308852632746522 ) ) ;
#70052=CARTESIAN_POINT ( 'NONE',  ( -11.89158881072656193, -4.825170694069168320, -76.89278924248901603 ) ) ;
#70053=( LENGTH_UNIT ( ) NAMED_UNIT ( * ) SI_UNIT ( .MILLI., .METRE. ) );
#70069=CARTESIAN_POINT ( 'NONE',  ( 2.751706330279339863, -5.000000000000015987, -99.99999999999998579 ) ) ;
#70070=CARTESIAN_POINT ( 'NONE',  ( 17.17069302877290582, -4.333298119783758118, 5.126212997540350536 ) ) ;
#70083=CARTESIAN_POINT ( 'NONE',  ( -7.126148247341459019, 41.12758119229484066, -58.55282700859728351 ) ) ;
#70116=CARTESIAN_POINT ( 'NONE',  ( -6.648792466258459655, -5.000000000000000000, 15.29529797603510488 ) ) ;
#70144=CARTESIAN_POINT ( 'NONE',  ( 18.96461344042381469, 49.39013151286044234, 61.98979294430989739 ) ) ;
#70155=CARTESIAN_POINT ( 'NONE',  ( -12.50000000000000355, -79.93083296558610584, -76.70843802411151557 ) ) ;
#70168=CARTESIAN_POINT ( 'NONE',  ( 6.200188411027975022, 41.06054039277635326, -71.07396429817178785 ) ) ;
#70170=CARTESIAN_POINT ( 'NONE',  ( 12.50000000000000711, -4.999999999999999112, -80.60844091781802945 ) ) ;
#70181=CARTESIAN_POINT ( 'NONE',  ( 5.222379818299239140, 7.098635799589327888, -27.55850616374455697 ) ) ;
#70186=CARTESIAN_POINT ( 'NONE',  ( 5.036189802310023111, -5.000000000000002665, -76.26213611588336505 ) ) ;
#70187=SURFACE_STYLE_USAGE ( .BOTH. , #52939 ) ;
#70209=CARTESIAN_POINT ( 'NONE',  ( 12.13034742782427955, -79.93083296558610584, -93.82352941176471006 ) ) ;
#70217=CARTESIAN_POINT ( 'NONE',  ( 2.583889972060055218, -5.000000000000000000, 9.742892617415389367 ) ) ;
#70218=CARTESIAN_POINT ( 'NONE',  ( 6.061808134833448491, -5.000000000000000000, -74.52203418564995729 ) ) ;
#70221=CARTESIAN_POINT ( 'NONE',  ( 5.363597346073513350, 41.33266196706048845, -58.39526881795627844 ) ) ;
#70229=( LENGTH_UNIT ( ) NAMED_UNIT ( * ) SI_UNIT ( .MILLI., .METRE. ) );
#70237=CARTESIAN_POINT ( 'NONE',  ( 17.50000000000007105, 48.00000000000153477, 62.61753806507839926 ) ) ;
#70242=CARTESIAN_POINT ( 'NONE',  ( 25.59175815610272764, 43.61275438026441975, -75.31714932479673053 ) ) ;
#70253=CARTESIAN_POINT ( 'NONE',  ( -1.233923992984923027E-14, 18.64316884711714195, -38.36535705883633085 ) ) ;
#70261=CARTESIAN_POINT ( 'NONE',  ( -54.95213656779772293, 38.95432885865245254, -32.68837454861606773 ) ) ;
#70273=CARTESIAN_POINT ( 'NONE',  ( 1.735558044530975508, 39.99999999999999289, -69.74083754113327416 ) ) ;
#70294=CARTESIAN_POINT ( 'NONE',  ( -5.036189803708997381, 48.00000000000000711, -76.26213611645745516 ) ) ;
#70309=CARTESIAN_POINT ( 'NONE',  ( -6.804948495083388949, 41.03925908421396684, -70.91872536974180719 ) ) ;
#70331=CARTESIAN_POINT ( 'NONE',  ( -12.50000000000000000, 20.38384220063782593, -37.91620629977019519 ) ) ;
#70341=CARTESIAN_POINT ( 'NONE',  ( 7.130799530010651921, 41.48519058599254805, -59.01258828833805836 ) ) ;
#70362=CARTESIAN_POINT ( 'NONE',  ( -14.93248505786663038, -4.333298119783897562, 9.906141972585356115 ) ) ;
#70373=CARTESIAN_POINT ( 'NONE',  ( 60.62677696744211175, 49.99999999997998401, 24.18439665018642870 ) ) ;
#70378=CARTESIAN_POINT ( 'NONE',  ( -6.611591191889651498, 41.87945138500480624, -59.42330386243895646 ) ) ;
#70387=CARTESIAN_POINT ( 'NONE',  ( 19.36108815078635814, 50.00000000000000711, 60.09752357988048033 ) ) ;
#70399=CARTESIAN_POINT ( 'NONE',  ( 59.92186310548196815, 49.99999999999997868, -19.49309254038931272 ) ) ;
#70411=CARTESIAN_POINT ( 'NONE',  ( 6.746994761561826870, 41.86978728249054882, -69.53909782334804390 ) ) ;
#70433=( GEOMETRIC_REPRESENTATION_CONTEXT ( 3 ) GLOBAL_UNCERTAINTY_ASSIGNED_CONTEXT ( ( #35406 ) ) GLOBAL_UNIT_ASSIGNED_CONTEXT ( ( #81083, #74580, #56803 ) ) REPRESENTATION_CONTEXT ( 'NONE', 'WORKASPACE' ) );
#70445=LINE ( 'NONE', #30534, #35600 ) ;
#70493=LINE ( 'NONE', #63473, #41347 ) ;
#70495=CARTESIAN_POINT ( 'NONE',  ( -37.55250343708862459, 42.26547160929953151, -58.87384313933568336 ) ) ;
#70496=CARTESIAN_POINT ( 'NONE',  ( -17.64199176884268283, 50.00000000000000000, 62.53729709305390116 ) ) ;
#70497=CARTESIAN_POINT ( 'NONE',  ( 18.91791044776121211, 47.00000000000000000, 62.18611311450883505 ) ) ;
#70512=CARTESIAN_POINT ( 'NONE',  ( -14.75116209839011994, 43.55504285526384933, -90.22050492866908655 ) ) ;
#70518=CARTESIAN_POINT ( 'NONE',  ( 7.360438360688435822, 50.00000000000000711, -94.60993813358487614 ) ) ;
#70523=ORIENTED_EDGE ( 'NONE', *, *, #105401, .T. ) ;
#70531=CARTESIAN_POINT ( 'NONE',  ( -6.441911206406983226, 41.95837094207923457, -69.50559752220233634 ) ) ;
#70539=CARTESIAN_POINT ( 'NONE',  ( -6.249702485612488978, 41.65323702329418865, -58.70056700059317478 ) ) ;
#70542=ADVANCED_FACE ( 'NONE', ( #32599 ), #25001, .T. ) ;
#70561=CARTESIAN_POINT ( 'NONE',  ( -36.40416150969235787, 41.99999999991774757, -47.37019975554808582 ) ) ;
#70563=B_SPLINE_SURFACE_WITH_KNOTS ( 'NONE', 3, 3, ( 
 ( #23476, #63403, #32087, #64963, #39117, #38082, #70938, #103831 ),
 ( #29976, #26152, #57920, #34762, #34224, #41747, #50356, #90839 ),
 ( #90301, #91897, #713, #8312, #89778, #82739, #66556, #74634 ),
 ( #16410, #16957, #25063, #25613, #41215, #49834, #49290, #91378 ),
 ( #99434, #58473, #98903, #82195, #191, #9903, #74101, #42813 ),
 ( #33154, #8842, #66024, #67635, #17496, #33683, #83270, #9360 ),
 ( #50887, #26668, #42273, #75164, #75708, #83792, #59008, #1255 ),
 ( #100512, #18022, #67097, #99981, #24538, #1803, #15882, #106470 ),
 ( #7776, #48757, #81651, #40681, #73567, #32628, #65501, #98390 ),
 ( #57388, #94026, #93509, #51429, #44417, #36889, #102650, #11491 ) ),
 .UNSPECIFIED., .F., .F., .F.,
 ( 4, 2, 2, 2, 4 ),
 ( 4, 2, 2, 4 ),
 ( 0.000000000000000000, 0.1250000000000000000, 0.2500000000000000000, 0.5000000000000000000, 1.000000000000000000 ),
 ( 0.000000000000000000, 0.2500000000000000000, 0.5000000000000000000, 1.000000000000000000 ),
 .UNSPECIFIED. ) ;
#70585=VERTEX_POINT ( 'NONE', #15583 ) ;
#70591=CARTESIAN_POINT ( 'NONE',  ( -12.07109306393920178, -4.718911993881638622, -76.83903857454983211 ) ) ;
#70604=CARTESIAN_POINT ( 'NONE',  ( -8.831401106173711213, -5.000000000000002665, -94.83329464149440469 ) ) ;
#70611=SURFACE_STYLE_USAGE ( .BOTH. , #52286 ) ;
#70619=CARTESIAN_POINT ( 'NONE',  ( 0.000000000000000000, -79.93083296558610584, -85.00000000000000000 ) ) ;
#70637=ORIENTED_EDGE ( 'NONE', *, *, #12175, .F. ) ;
#70649=CARTESIAN_POINT ( 'NONE',  ( 13.20528892216484707, -4.332661967058641928, 12.52414413171604046 ) ) ;
#70657=EDGE_CURVE ( 'NONE', #53673, #102845, #29138, .T. ) ;
#70673=CARTESIAN_POINT ( 'NONE',  ( 18.94211536943317142, 49.24611979230877523, 62.05162962396204307 ) ) ;
#70701=CARTESIAN_POINT ( 'NONE',  ( 5.582554291377552325, 41.37363159368051413, -70.85834491557551473 ) ) ;
#70717=CARTESIAN_POINT ( 'NONE',  ( -9.797174393178825657E-16, -3.000000000000000000, 8.000000000000000000 ) ) ;
#70719=CARTESIAN_POINT ( 'NONE',  ( 0.000000000000000000, -5.000000000000002665, -73.00000000000001421 ) ) ;
#70721=FILL_AREA_STYLE_COLOUR ( '', #100038 ) ;
#70746=FACE_OUTER_BOUND ( 'NONE', #62034, .T. ) ;
#70759=CARTESIAN_POINT ( 'NONE',  ( -39.50046859269861699, 39.85910268592828487, -53.63619651269492294 ) ) ;
#70782=CARTESIAN_POINT ( 'NONE',  ( -38.36535705883633085, 18.64316884711714195, 5.022013495247505510 ) ) ;
#70789=CARTESIAN_POINT ( 'NONE',  ( -64.71212909754572706, 39.42531715955912830, 6.807929623798474772 ) ) ;
#70807=CARTESIAN_POINT ( 'NONE',  ( 2.617478844989858722, 48.00000000000000000, -94.73972676610448218 ) ) ;
#70814=CARTESIAN_POINT ( 'NONE',  ( 4.852941176470595863, 39.99999999999999289, -70.80672828634229177 ) ) ;
#70815=CARTESIAN_POINT ( 'NONE',  ( -16.52732684424166010, 43.98685724163156863, -87.77868211029608858 ) ) ;
#70847=CARTESIAN_POINT ( 'NONE',  ( -18.28710009642425760, 45.00000000000000711, 62.41242308437181663 ) ) ;
#70849=( BOUNDED_SURFACE ( )  B_SPLINE_SURFACE ( 2, 3, ( 
 ( #34921, #36000, #60778, #84510, #77481, #42986, #68327, #52654, #43517, #101745, #1433, #1972, #67788, #44047, #101222, #93667, #20364, #68872, #9528, #10599, #27913, #19818, #3592, #36529, #11661, #61303, #44591, #26839, #69394, #75873, #19299, #102277, #85039, #34394 ),
 ( #28425, #59710, #94195, #18743, #53205, #2508, #100675, #27379, #42441, #52123, #67269, #75331, #60259, #18192, #100148, #10076, #26315, #76937, #3050, #92587, #51049, #93125, #83966, #59176, #51591, #76394, #11121, #79591, #29496, #94743, #102818, #22458, #72036, #80114 ),
 ( #22978, #62896, #38627, #45127, #63436, #21920, #55301, #88228, #61846, #12196, #62372, #6218, #13252, #20892, #71491, #104389, #21394, #30539, #13781, #95263, #5700, #95787, #4656, #53726, #54231, #96330, #86655, #12725, #54769, #78004, #28980, #39154, #14309, #46176 ) ),
 .UNSPECIFIED., .F., .T., .F. ) 
 B_SPLINE_SURFACE_WITH_KNOTS ( ( 3, 3 ),
 ( 4, 2, 2, 2, 2, 2, 2, 2, 2, 2, 2, 2, 2, 2, 2, 2, 4 ),
 ( 0.000000000000000000, 1.000000000000000000 ),
 ( -3.141592653589793116, -2.748893571891068976, -2.356194490192344837, -1.963495408493620697, -1.570796326794896558, -1.178097245096172418, -0.7853981633974482790, -0.3926990816987241395, 0.000000000000000000, 0.3926990816987241395, 0.7853981633974482790, 1.178097245096172418, 1.570796326794896558, 1.963495408493620697, 2.356194490192344837, 2.748893571891068976, 3.141592653589793116 ),
 .UNSPECIFIED. ) 
 GEOMETRIC_REPRESENTATION_ITEM ( )  RATIONAL_B_SPLINE_SURFACE ( (
 ( 1.000000000000000000, 1.000000000000000000, 1.000000000000000000, 1.000000000000000000, 1.000000000000000000, 1.000000000000000000, 1.000000000000000000, 1.000000000000000000, 1.000000000000000000, 1.000000000000000000, 1.000000000000000000, 1.000000000000000000, 1.000000000000000000, 1.000000000000000000, 1.000000000000000000, 1.000000000000000000, 1.000000000000000000, 1.000000000000000000, 1.000000000000000000, 1.000000000000000000, 1.000000000000000000, 1.000000000000000000, 1.000000000000000000, 1.000000000000000000, 1.000000000000000000, 1.000000000000000000, 1.000000000000000000, 1.000000000000000000, 1.000000000000000000, 1.000000000000000000, 1.000000000000000000, 1.000000000000000000, 1.000000000000000000, 1.000000000000000000),
 ( 1.857142857142858317, 1.857142857142858317, 1.857142857142858317, 1.857142857142858317, 1.857142857142858317, 1.857142857142858317, 1.857142857142858317, 1.857142857142858317, 1.857142857142858317, 1.857142857142858317, 1.857142857142858317, 1.857142857142858317, 1.857142857142858317, 1.857142857142858317, 1.857142857142858317, 1.857142857142858317, 1.857142857142858317, 1.857142857142858317, 1.857142857142858317, 1.857142857142858317, 1.857142857142858317, 1.857142857142858317, 1.857142857142858317, 1.857142857142858317, 1.857142857142858317, 1.857142857142858317, 1.857142857142858317, 1.857142857142858317, 1.857142857142858317, 1.857142857142858317, 1.857142857142858317, 1.857142857142858317, 1.857142857142858317, 1.857142857142858317),
 ( 1.000000000000000000, 1.000000000000000000, 1.000000000000000000, 1.000000000000000000, 1.000000000000000000, 1.000000000000000000, 1.000000000000000000, 1.000000000000000000, 1.000000000000000000, 1.000000000000000000, 1.000000000000000000, 1.000000000000000000, 1.000000000000000000, 1.000000000000000000, 1.000000000000000000, 1.000000000000000000, 1.000000000000000000, 1.000000000000000000, 1.000000000000000000, 1.000000000000000000, 1.000000000000000000, 1.000000000000000000, 1.000000000000000000, 1.000000000000000000, 1.000000000000000000, 1.000000000000000000, 1.000000000000000000, 1.000000000000000000, 1.000000000000000000, 1.000000000000000000, 1.000000000000000000, 1.000000000000000000, 1.000000000000000000, 1.000000000000000000) ) ) 
 REPRESENTATION_ITEM ( '' )  SURFACE ( )  );
#70868=CARTESIAN_POINT ( 'NONE',  ( 0.000000000000000000, 50.00000000000000000, -97.00000000000000000 ) ) ;
#70869=CARTESIAN_POINT ( 'NONE',  ( 7.090506028190232790, 41.24768140130692728, -58.61601156502441512 ) ) ;
#70874=CARTESIAN_POINT ( 'NONE',  ( 7.500000000000001776, 13.44157116919690331, -32.95552552993890316 ) ) ;
#70883=CARTESIAN_POINT ( 'NONE',  ( 5.500000000000006217, 42.00000000000000000, -62.89165061482969321 ) ) ;
#70893=CARTESIAN_POINT ( 'NONE',  ( 1.262844703064978993E-15, -3.000000000000002665, -95.00000000000000000 ) ) ;
#70898=CARTESIAN_POINT ( 'NONE',  ( -51.78317192863611496, 49.99999999999999289, 39.73656039226784742 ) ) ;
#70902=CARTESIAN_POINT ( 'NONE',  ( -14.91271302809441401, 41.98564543112699710, -86.62215342991694911 ) ) ;
#70903=CARTESIAN_POINT ( 'NONE',  ( -5.935764392945439560, 41.97455565604287386, -59.37421952392686819 ) ) ;
#70905=CARTESIAN_POINT ( 'NONE',  ( 12.04168909130320841, -4.749806419314886341, -76.84810691751602008 ) ) ;
#70920=CARTESIAN_POINT ( 'NONE',  ( 59.10635875623282232, 49.99999999999999289, -21.83939464513134610 ) ) ;
#70938=CARTESIAN_POINT ( 'NONE',  ( -7.036764705886677795, 40.29466777512107001, -71.06385277390548083 ) ) ;
#70965=PRESENTATION_STYLE_ASSIGNMENT (( #62364 ) ) ;
#70975=ADVANCED_FACE ( 'NONE', ( #42938 ), #102769, .T. ) ;
#70977=PRESENTATION_STYLE_ASSIGNMENT (( #5189 ) ) ;
#70996=CARTESIAN_POINT ( 'NONE',  ( -5.235346568409651624, 8.628330344405153340, -28.94746872473582400 ) ) ;
#71014=CARTESIAN_POINT ( 'NONE',  ( -19.02605628674608340, 50.00000000000000000, 60.55087752146327773 ) ) ;
#71040=CARTESIAN_POINT ( 'NONE',  ( 6.764423792815447811, 41.48989066009205118, -70.49176070406230110 ) ) ;
#71052=SURFACE_SIDE_STYLE ('',( #37670 ) ) ;
#71053=CARTESIAN_POINT ( 'NONE',  ( -6.629186135610700248, 41.56975587227380942, -70.49374930908771830 ) ) ;
#71057=CARTESIAN_POINT ( 'NONE',  ( 6.523983739925002467, -5.000000000000001776, 15.07216758675048318 ) ) ;
#71058=CARTESIAN_POINT ( 'NONE',  ( -5.666914945001757964, 41.34312461251444404, -58.37679809223642025 ) ) ;
#71076=CARTESIAN_POINT ( 'NONE',  ( 5.469234054728515204, 41.99717949937266326, -59.59612150530382735 ) ) ;
#71086=MECHANICAL_DESIGN_GEOMETRIC_PRESENTATION_REPRESENTATION('',(#7314),#62546);
#71101=DIRECTION ( 'NONE',  ( 0.000000000000000000, 0.000000000000000000, 1.000000000000000000 ) ) ;
#71107=MECHANICAL_DESIGN_GEOMETRIC_PRESENTATION_REPRESENTATION('',(#10796),#19493);
#71112=CARTESIAN_POINT ( 'NONE',  ( -12.32841007366266162, -4.394465204955733562, -76.76276077223093353 ) ) ;
#71133=PLANE ( 'NONE',  #20700 ) ;
#71138=DIRECTION ( 'NONE',  ( 0.000000000000000000, 1.000000000000000000, 0.000000000000000000 ) ) ;
#71163=VERTEX_POINT ( 'NONE', #25056 ) ;
#71191=CARTESIAN_POINT ( 'NONE',  ( 19.45753456193933673, 49.98217452750294143, 60.55466515883400547 ) ) ;
#71224=CARTESIAN_POINT ( 'NONE',  ( 18.61015277268172952, 45.00000000000002842, 62.28407730500863693 ) ) ;
#71237=CARTESIAN_POINT ( 'NONE',  ( 1.308996937480706890, -4.999999999999988454, -95.00000000000001421 ) ) ;
#71244=ORIENTED_EDGE ( 'NONE', *, *, #9406, .T. ) ;
#71267=SURFACE_STYLE_FILL_AREA ( #54531 ) ;
#71272=PRESENTATION_STYLE_ASSIGNMENT (( #6000 ) ) ;
#71281=CARTESIAN_POINT ( 'NONE',  ( 6.951447288752834019, 41.73217225470716585, -59.36631759480938086 ) ) ;
#71292=CARTESIAN_POINT ( 'NONE',  ( 26.76898821255671379, 43.52124955778052140, -73.69872557157349036 ) ) ;
#71307=EDGE_LOOP ( 'NONE', ( #23624, #34593, #93117, #48721, #58991, #60132, #84832 ) ) ;
#71308=CARTESIAN_POINT ( 'NONE',  ( -63.73076471685384803, 38.95251052932829339, 0.7990814525311284999 ) ) ;
#71327=CARTESIAN_POINT ( 'NONE',  ( -6.145467200826166376, 48.00000000000000000, -92.99666842290478996 ) ) ;
#71339=CARTESIAN_POINT ( 'NONE',  ( 8.716845791011509803, -5.000000000000000000, -16.74192973251932415 ) ) ;
#71366=APPLICATION_CONTEXT ( 'automotive_design' ) ;
#71373=CARTESIAN_POINT ( 'NONE',  ( 5.500000000000641265, 42.00000000000000000, -59.88032989331720302 ) ) ;
#71380=CARTESIAN_POINT ( 'NONE',  ( 7.409230219490164693, 40.77747305847753267, -58.95054515628400083 ) ) ;
#71386=CARTESIAN_POINT ( 'NONE',  ( 7.500000000000007105, 41.91230289050422186, -61.59623549333881698 ) ) ;
#71399=CARTESIAN_POINT ( 'NONE',  ( 7.500000000000007105, 40.00000000000000000, -70.16688272716299934 ) ) ;
#71408=CARTESIAN_POINT ( 'NONE',  ( 64.91565662652978119, 40.83906611471883963, 6.815324757212413154 ) ) ;
#71412=CARTESIAN_POINT ( 'NONE',  ( 61.09659575456475977, 50.00000000000000000, -16.41787579823443366 ) ) ;
#71448=CARTESIAN_POINT ( 'NONE',  ( 5.787483263666111100, 41.99999999999999289, -68.91429206946564534 ) ) ;
#71456=CARTESIAN_POINT ( 'NONE',  ( -6.916167714701083824, 41.81554662627394237, -59.83173445090647391 ) ) ;
#71491=CARTESIAN_POINT ( 'NONE',  ( -5.036189802313092656, 48.00000000000000000, -93.73786388412078452 ) ) ;
#71513=CARTESIAN_POINT ( 'NONE',  ( 10.00000000000000000, -5.000000000000000000, 2.617993873628172263 ) ) ;
#71516=CARTESIAN_POINT ( 'NONE',  ( -5.284247479666474234, 16.54466108722069251, -36.10555915917339576 ) ) ;
#71531=FILL_AREA_STYLE ('',( #61890 ) ) ;
#71532=CARTESIAN_POINT ( 'NONE',  ( -17.69721706678098627, 50.00000000000000711, 62.38211090070038267 ) ) ;
#71538=CARTESIAN_POINT ( 'NONE',  ( 17.50000000000004619, 50.30551795521390801, 63.70247084374984325 ) ) ;
#71548=CARTESIAN_POINT ( 'NONE',  ( -14.36708347031724564, 43.38383075969758806, -90.74852574445671394 ) ) ;
#71580=CARTESIAN_POINT ( 'NONE',  ( -6.913779242700421435, 41.73441082398074542, -59.30275289623196500 ) ) ;
#71595=CARTESIAN_POINT ( 'NONE',  ( 6.232496355896457452, 41.83455062734740437, -59.02481358918409171 ) ) ;
#71624=CARTESIAN_POINT ( 'NONE',  ( -12.39938211290231784, -4.333194019920661333, -12.81742571336049075 ) ) ;
#71648=CARTESIAN_POINT ( 'NONE',  ( -2.617993873628327250, -5.000000000000000000, 10.00000000000000000 ) ) ;
#71661=ORIENTED_EDGE ( 'NONE', *, *, #43505, .T. ) ;
#71670=AXIS2_PLACEMENT_3D ( 'NONE', #69530, #94342, #61988 ) ;
#71687=CARTESIAN_POINT ( 'NONE',  ( 9.340818716798185979E-16, -4.999999999999999112, -8.000000000000000000 ) ) ;
#71694=CARTESIAN_POINT ( 'NONE',  ( -52.27951051746360633, 48.00000000000000711, 38.96734372144650393 ) ) ;
#71706=CARTESIAN_POINT ( 'NONE',  ( 18.91820918444131649, 48.57558852673482619, 62.17047227842536472 ) ) ;
#71716=EDGE_CURVE ( 'NONE', #58911, #44820, #74016, .T. ) ;
#71754=CARTESIAN_POINT ( 'NONE',  ( 4.916373759799321341, -3.000000000000000444, -6.397334739185440711 ) ) ;
#71758=CARTESIAN_POINT ( 'NONE',  ( -9.999999999999996447, -3.000000000000002665, -86.30899693747677759 ) ) ;
#71768=CARTESIAN_POINT ( 'NONE',  ( -1.590636543732056873, 50.00000000000000711, -96.99986829839870950 ) ) ;
#71769=CARTESIAN_POINT ( 'NONE',  ( -34.55014207014404093, 42.66529688316376223, -63.00140760762604231 ) ) ;
#71780=CARTESIAN_POINT ( 'NONE',  ( 7.439123282901347167, 41.00341550150766068, -68.91429205944716330 ) ) ;
#71818=CARTESIAN_POINT ( 'NONE',  ( 25.63492787469831313, 43.60956991405247862, -75.25780077383848266 ) ) ;
#71828=CARTESIAN_POINT ( 'NONE',  ( 23.57730434123481800, 18.64316884710268596, -30.67950393663962672 ) ) ;
#71833=CARTESIAN_POINT ( 'NONE',  ( -52.56491209535032993, 39.42572890908716943, -38.23519342730719472 ) ) ;
#71852=CARTESIAN_POINT ( 'NONE',  ( 7.996668422911924701, 48.00000000000000000, -91.14546720081904141 ) ) ;
#71859=ORIENTED_EDGE ( 'NONE', *, *, #81424, .T. ) ;
#71870=CARTESIAN_POINT ( 'NONE',  ( 8.599968422084343089, -5.000000000000000888, -16.55615795282379921 ) ) ;
#71875=SURFACE_STYLE_USAGE ( .BOTH. , #62743 ) ;
#71899=CARTESIAN_POINT ( 'NONE',  ( 6.974441890915084485, 41.03925908523778077, -70.79755109270119817 ) ) ;
#71910=CARTESIAN_POINT ( 'NONE',  ( -12.50000000000000355, 27.18132204066968427, -44.72105335469841947 ) ) ;
#71922=CARTESIAN_POINT ( 'NONE',  ( 7.126148245860624009, 41.12758397993106030, -58.55282951229288102 ) ) ;
#71943=CARTESIAN_POINT ( 'NONE',  ( 5.500000000000007994, 42.00000000000000000, -71.41947339647144588 ) ) ;
#71944=VERTEX_POINT ( 'NONE', #42958 ) ;
#71951=CARTESIAN_POINT ( 'NONE',  ( 39.04923757959249286, 40.83906611472210102, 52.30342408726538395 ) ) ;
#71956=CARTESIAN_POINT ( 'NONE',  ( 55.22048556082879145, 50.00000000002004441, 34.80214219306057544 ) ) ;
#71976=VERTEX_POINT ( 'NONE', #19274 ) ;
#72021=VERTEX_POINT ( 'NONE', #103840 ) ;
#72036=CARTESIAN_POINT ( 'NONE',  ( 1.308996937480704004, 49.99999999999999289, -75.00000000000001421 ) ) ;
#72070=STYLED_ITEM ( 'NONE', ( #4638 ), #42818 ) ;
#72078=EDGE_CURVE ( 'NONE', #21912, #67484, #72308, .T. ) ;
#72081=CARTESIAN_POINT ( 'NONE',  ( 17.50000000000003908, 51.99573851567223670, 60.30773471722763190 ) ) ;
#72088=CARTESIAN_POINT ( 'NONE',  ( -7.498343863768531570, -2.970317092013120774, -20.23009517154971348 ) ) ;
#72090=CARTESIAN_POINT ( 'NONE',  ( 7.500000000000006217, 39.99999999999942446, -59.88032989331673406 ) ) ;
#72110=ORIENTED_EDGE ( 'NONE', *, *, #3335, .T. ) ;
#72111=CARTESIAN_POINT ( 'NONE',  ( 4.852941176470595863, -5.000000000000002665, -70.80672828634229177 ) ) ;
#72137=CARTESIAN_POINT ( 'NONE',  ( 6.503370466877179012, 41.93912984867880311, -59.84719185825785104 ) ) ;
#72184=MECHANICAL_DESIGN_GEOMETRIC_PRESENTATION_REPRESENTATION('',(#91146),#59679);
#72197=CARTESIAN_POINT ( 'NONE',  ( 2.094395098902538166, -3.000000000000000000, -8.000000000000000000 ) ) ;
#72198=DIRECTION ( 'NONE',  ( 0.000000000000000000, 0.000000000000000000, 1.000000000000000000 ) ) ;
#72225=VERTEX_POINT ( 'NONE', #18034 ) ;
#72243=CARTESIAN_POINT ( 'NONE',  ( -65.20309930813586163, 47.99999999999999289, 0.3961530819213011090 ) ) ;
#72286=CARTESIAN_POINT ( 'NONE',  ( 18.91791044776121211, 45.00000000000000711, 62.18611311450882795 ) ) ;
#72301=CARTESIAN_POINT ( 'NONE',  ( 6.145467200819017428, -3.000000000000002665, -77.00333157708807619 ) ) ;
#72308=B_SPLINE_CURVE_WITH_KNOTS ( 'NONE', 3,
 ( #54744, #104919, #88203, #96305, #4631, #38090, #79565, #46667, #47187, #62872 ),
 .UNSPECIFIED., .F., .F.,
 ( 4, 2, 2, 2, 4 ),
 ( 0.000000000000000000, 0.2500000000000000000, 0.5000000000000000000, 0.7500000000000000000, 1.000000000000000000 ),
 .UNSPECIFIED. ) ;
#72313=CARTESIAN_POINT ( 'NONE',  ( 7.014891834159853623, -4.207085196949424066, -17.12005312236325594 ) ) ;
#72337=CARTESIAN_POINT ( 'NONE',  ( -9.432319653624512412, -5.000000000000000888, -70.68463330168729897 ) ) ;
#72353=CARTESIAN_POINT ( 'NONE',  ( 8.737863884121400915, -4.999999999998638422, -90.03618980231146907 ) ) ;
#72356=CARTESIAN_POINT ( 'NONE',  ( 7.500000000000005329, 9.833333333333344584, -71.71180648257555390 ) ) ;
#72359=CARTESIAN_POINT ( 'NONE',  ( 5.500000000000006217, 42.00000000000000000, -62.89165061903125320 ) ) ;
#72370=CARTESIAN_POINT ( 'NONE',  ( 61.55604228310126302, 38.95379169962407673, -16.52177172830128526 ) ) ;
#72389=CARTESIAN_POINT ( 'NONE',  ( 1.308996937483426715, 48.00000000000000000, -95.00000000000000000 ) ) ;
#72390=CARTESIAN_POINT ( 'NONE',  ( -12.13034742782427777, 41.99999999999999289, -93.82352941176471006 ) ) ;
#72396=CARTESIAN_POINT ( 'NONE',  ( -14.33580415456969703, 41.99999999999998579, -89.41414988892334748 ) ) ;
#72399=ORIENTED_EDGE ( 'NONE', *, *, #9311, .T. ) ;
#72406=CARTESIAN_POINT ( 'NONE',  ( 8.749920771053334434, -5.000000000000000000, -16.79831961264161677 ) ) ;
#72419=ORIENTED_EDGE ( 'NONE', *, *, #57618, .F. ) ;
#72429=CARTESIAN_POINT ( 'NONE',  ( -18.65899211044941097, 45.00000000000001421, 62.26487979851452081 ) ) ;
#72434=CARTESIAN_POINT ( 'NONE',  ( -7.491624054469464333, 40.33174201206623621, -59.48414770601905133 ) ) ;
#72450=CARTESIAN_POINT ( 'NONE',  ( 35.10078947236149105, 18.64284798592602144, -15.64789144403509091 ) ) ;
#72464=MECHANICAL_DESIGN_GEOMETRIC_PRESENTATION_REPRESENTATION('',(#44922),#38100);
#72467=CARTESIAN_POINT ( 'NONE',  ( 13.07034999569633626, 42.28767565851803312, -92.53123953979158500 ) ) ;
#72480=CARTESIAN_POINT ( 'NONE',  ( 28.00203968317441294, 50.00000000000000000, 56.72941417029700517 ) ) ;
#72484=EDGE_CURVE ( 'NONE', #77528, #90268, #4130, .T. ) ;
#72491=SURFACE_STYLE_FILL_AREA ( #57352 ) ;
#72494=CARTESIAN_POINT ( 'NONE',  ( 18.53506029635388686, 50.00000000000000711, 61.21187092669564578 ) ) ;
#72516=CARTESIAN_POINT ( 'NONE',  ( 5.787518022136032947, 41.99999999999999289, -59.87256586542197567 ) ) ;
#72522=CARTESIAN_POINT ( 'NONE',  ( -6.645513941704877858, 41.91298746401114528, -59.84148600730080858 ) ) ;
#72529=ORIENTED_EDGE ( 'NONE', *, *, #7126, .F. ) ;
#72541=CARTESIAN_POINT ( 'NONE',  ( -11.69514296590343427, -5.000000000000000000, -81.87740575804689058 ) ) ;
#72561=( NAMED_UNIT ( * ) PLANE_ANGLE_UNIT ( ) SI_UNIT ( $, .RADIAN. ) );
#72578=CARTESIAN_POINT ( 'NONE',  ( -4.175893272573466319, -3.000000000000000000, -7.137815226411295733 ) ) ;
#72605=CARTESIAN_POINT ( 'NONE',  ( 17.50000000000000355, 51.30660076970968930, 62.83706383107325166 ) ) ;
#72613=ORIENTED_EDGE ( 'NONE', *, *, #27391, .F. ) ;
#72614=CARTESIAN_POINT ( 'NONE',  ( -7.499999907820173561, -3.000141485250358730, -20.99866594742747949 ) ) ;
#72619=B_SPLINE_CURVE_WITH_KNOTS ( 'NONE', 3,
 ( #83707, #2797, #100430, #25530 ),
 .UNSPECIFIED., .F., .F.,
 ( 4, 4 ),
 ( 0.4999999999999988898, 1.000000000000000000 ),
 .UNSPECIFIED. ) ;
#72637=SURFACE_STYLE_FILL_AREA ( #39761 ) ;
#72639=CIRCLE ( 'NONE', #103671, 8.000000000000000000 ) ;
#72643=CARTESIAN_POINT ( 'NONE',  ( 7.036764705882352366, 40.00000000373363207, -71.06385277390853616 ) ) ;
#72662=ORIENTED_EDGE ( 'NONE', *, *, #52751, .T. ) ;
#72664=CARTESIAN_POINT ( 'NONE',  ( 6.492511067189947305, 41.78432740739263096, -59.03547063838888675 ) ) ;
#72666=ADVANCED_FACE ( 'NONE', ( #89665 ), #79167, .T. ) ;
#72714=CARTESIAN_POINT ( 'NONE',  ( 0.000000000000000000, -4.999999999999998224, 8.000000000000000000 ) ) ;
#72718=ORIENTED_EDGE ( 'NONE', *, *, #38944, .T. ) ;
#72720=CARTESIAN_POINT ( 'NONE',  ( -10.50000000000000711, -5.000000000000000000, -55.73109925765190553 ) ) ;
#72738=CARTESIAN_POINT ( 'NONE',  ( -4.852941176470586093, 40.00000000000132871, -70.80672828634229177 ) ) ;
#72760=VECTOR ( 'NONE', #74117, 1000.000000000000000 ) ;
#72787=CARTESIAN_POINT ( 'NONE',  ( 5.898965727403031600, 41.68848182032888872, -58.70906957313534491 ) ) ;
#72808=CARTESIAN_POINT ( 'NONE',  ( -7.673189737795076404, -4.999999999999999112, -15.67457516869437129 ) ) ;
#72812=CARTESIAN_POINT ( 'NONE',  ( 9.235395886531431551E-16, -3.000000000000000000, -8.000000000000000000 ) ) ;
#72816=FACE_OUTER_BOUND ( 'NONE', #7362, .T. ) ;
#72829=CARTESIAN_POINT ( 'NONE',  ( 6.615712822706482754, -4.357054607612469432, -16.81429077417679707 ) ) ;
#72837=CARTESIAN_POINT ( 'NONE',  ( 7.251642494156181229, 41.54835750584383192, -68.91429206127320128 ) ) ;
#72845=( BOUNDED_SURFACE ( )  B_SPLINE_SURFACE ( 2, 3, ( 
 ( #68325, #4119, #11658, #27911 ),
 ( #93665, #52652, #61843, #94193 ),
 ( #101219, #85583, #44589, #77478 ) ),
 .UNSPECIFIED., .F., .F., .F. ) 
 B_SPLINE_SURFACE_WITH_KNOTS ( ( 3, 3 ),
 ( 4, 4 ),
 ( 0.000000000000000000, 1.000000000000000000 ),
 ( -0.06873863542433759910, 1.530452813897690353E-17 ),
 .UNSPECIFIED. ) 
 GEOMETRIC_REPRESENTATION_ITEM ( )  RATIONAL_B_SPLINE_SURFACE ( (
 ( 1.000000000000000000, 1.000000000000000000, 1.000000000000000000, 1.000000000000000000),
 ( 1.857142857142858317, 1.857142857142858317, 1.857142857142858317, 1.857142857142858317),
 ( 1.000000000000000000, 1.000000000000000000, 1.000000000000000000, 1.000000000000000000) ) ) 
 REPRESENTATION_ITEM ( '' )  SURFACE ( )  );
#72866=CARTESIAN_POINT ( 'NONE',  ( 9.596002107493083244, -5.000000000000002665, -77.62543935902139935 ) ) ;
#72885=CARTESIAN_POINT ( 'NONE',  ( -55.40281771843035585, 38.95363459860563182, 31.50562541889846102 ) ) ;
#72910=FILL_AREA_STYLE ('',( #46534 ) ) ;
#72945=CARTESIAN_POINT ( 'NONE',  ( 7.168070102805851995, 40.56150966784696976, -70.87151302692181787 ) ) ;
#72948=CARTESIAN_POINT ( 'NONE',  ( -7.380470314495000572, 40.84001257084522507, -58.87769989985683594 ) ) ;
#72955=CARTESIAN_POINT ( 'NONE',  ( -56.15634551241206651, 50.00000000000000000, 28.58296655959290433 ) ) ;
#72965=CARTESIAN_POINT ( 'NONE',  ( 7.423110160291532367, 40.85353811916601785, -59.12022462436053161 ) ) ;
#72979=CARTESIAN_POINT ( 'NONE',  ( 14.55921722940514229, 43.46947890857538255, -90.48438549608371773 ) ) ;
#73008=CARTESIAN_POINT ( 'NONE',  ( 7.063836239582370169, 41.16939439637754816, -58.51215209214867485 ) ) ;
#73073=ORIENTED_EDGE ( 'NONE', *, *, #75294, .F. ) ;
#73075=CARTESIAN_POINT ( 'NONE',  ( -7.439122753854266357, 41.00341855746702180, -68.91429205792265122 ) ) ;
#73085=( NAMED_UNIT ( * ) PLANE_ANGLE_UNIT ( ) SI_UNIT ( $, .RADIAN. ) );
#73116=CARTESIAN_POINT ( 'NONE',  ( 17.50000000000104805, 48.96861188084124450, 62.56461476143844891 ) ) ;
#73125=CARTESIAN_POINT ( 'NONE',  ( -7.340594533191627136, -3.410200195908305254, -18.44125947282421407 ) ) ;
#73129=ADVANCED_FACE ( 'NONE', ( #79857 ), #38375, .T. ) ;
#73151=CARTESIAN_POINT ( 'NONE',  ( 64.32759900501075379, 49.99999999999999289, -11.06576400629166912 ) ) ;
#73174=CARTESIAN_POINT ( 'NONE',  ( 14.91270732344407257, 41.98564553269472555, -86.62216337287246404 ) ) ;
#73175=CARTESIAN_POINT ( 'NONE',  ( 5.908324287552553677, 41.91795896428032364, -59.12627191402334148 ) ) ;
#73216=CARTESIAN_POINT ( 'NONE',  ( -12.45393346519286837, -3.927217745177864927, -76.72514752459275655 ) ) ;
#73231=CARTESIAN_POINT ( 'NONE',  ( -4.175893272574851878, -3.000000000000000000, 7.137815226409915503 ) ) ;
#73232=CARTESIAN_POINT ( 'NONE',  ( 5.500000036871884213, 42.00000000000000000, -68.91429207046176941 ) ) ;
#73233=( NAMED_UNIT ( * ) PLANE_ANGLE_UNIT ( ) SI_UNIT ( $, .RADIAN. ) );
#73253=B_SPLINE_CURVE_WITH_KNOTS ( 'NONE', 3,
 ( #6853, #7375, #40288, #65095, #16012, #22554, #81785, #55394, #68296, #41876, #61689, #10046, #58612, #99035, #10571, #74765, #43487, #25201, #84478, #53567, #74242, #26805, #76363, #75845, #844, #1941, #51562, #42953, #59143, #92026, #2476, #33282, #318, #66153 ),
 .UNSPECIFIED., .F., .F.,
 ( 4, 2, 2, 2, 2, 2, 2, 2, 2, 2, 2, 2, 2, 2, 2, 2, 4 ),
 ( 0.4999999999999275579, 0.5312499999999320544, 0.5624999999999366063, 0.5937499999999411582, 0.6249999999999455991, 0.6562499999999501510, 0.6874999999999547029, 0.7187499999999592548, 0.7499999999999638067, 0.7812499999999682476, 0.8124999999999727995, 0.8437499999999773515, 0.8749999999999817923, 0.9062499999999864553, 0.9374999999999908962, 0.9687499999999953371, 1.000000000000000000 ),
 .UNSPECIFIED. ) ;
#73257=CARTESIAN_POINT ( 'NONE',  ( 4.852941176470592310, -3.000000000000002665, -70.80672828634229177 ) ) ;
#73284=CARTESIAN_POINT ( 'NONE',  ( -49.01201108414407059, 47.99999999999999289, 43.00492839360019559 ) ) ;
#73328=MECHANICAL_DESIGN_GEOMETRIC_PRESENTATION_REPRESENTATION('',(#4436),#78505);
#73330=CARTESIAN_POINT ( 'NONE',  ( 17.89029056138539531, 45.00000000000001421, 62.64214772316259427 ) ) ;
#73333=EDGE_CURVE ( 'NONE', #57232, #56205, #41358, .T. ) ;
#73336=CARTESIAN_POINT ( 'NONE',  ( -9.500000000000000000, -5.000000000000000000, -20.99851272547259384 ) ) ;
#73340=CARTESIAN_POINT ( 'NONE',  ( 6.990291106834063406, -3.000000000000000444, -4.028951842967194885 ) ) ;
#73347=CARTESIAN_POINT ( 'NONE',  ( 65.02775738911797987, 48.00000000000000711, -4.794983377755723808 ) ) ;
#73354=CARTESIAN_POINT ( 'NONE',  ( 7.092880029127421437, -4.030086327928861678, -17.38322132479146376 ) ) ;
#73366=EDGE_CURVE ( 'NONE', #37125, #18823, #80717, .T. ) ;
#73368=CARTESIAN_POINT ( 'NONE',  ( -60.62677696757947388, 40.83906611472935566, 24.18439664997239191 ) ) ;
#73371=CARTESIAN_POINT ( 'NONE',  ( -17.49999999999997868, 49.46308821774191955, 63.99046601235075826 ) ) ;
#73385=CARTESIAN_POINT ( 'NONE',  ( -33.29153341846981817, 40.67237416681741990, -61.88034040721849749 ) ) ;
#73391=CARTESIAN_POINT ( 'NONE',  ( 6.145467200816499442, -5.000000000008177459, -92.99666842292330671 ) ) ;
#73397=CARTESIAN_POINT ( 'NONE',  ( 4.852941176470593199, 44.25000000000000000, -70.80672828634229177 ) ) ;
#73415=CARTESIAN_POINT ( 'NONE',  ( 14.51107877698349569, 38.95396704606918803, 62.06021138805395765 ) ) ;
#73417=( GEOMETRIC_REPRESENTATION_CONTEXT ( 3 ) GLOBAL_UNCERTAINTY_ASSIGNED_CONTEXT ( ( #63408 ) ) GLOBAL_UNIT_ASSIGNED_CONTEXT ( ( #32657, #80630, #33180 ) ) REPRESENTATION_CONTEXT ( 'NONE', 'WORKASPACE' ) );
#73475=CARTESIAN_POINT ( 'NONE',  ( 6.733158597025957093, 41.46658730117229652, -70.54360491111089004 ) ) ;
#73480=CARTESIAN_POINT ( 'NONE',  ( -16.66584972143294863, 38.95383793067399125, 62.01418705518651819 ) ) ;
#73484=CARTESIAN_POINT ( 'NONE',  ( -56.71108403266729425, 50.00000000000000711, 27.46636503440964105 ) ) ;
#73489=( BOUNDED_CURVE ( )  B_SPLINE_CURVE ( 2, ( #58247, #499, #84126, #41534, #24847 ),
 .UNSPECIFIED., .F., .F. ) 
 B_SPLINE_CURVE_WITH_KNOTS ( ( 3, 2, 3 ),
 ( 0.000000000000000000, 0.9999561054434824570, 1.000000000000000000 ),
 .UNSPECIFIED. ) 
 CURVE ( )  GEOMETRIC_REPRESENTATION_ITEM ( )  RATIONAL_B_SPLINE_CURVE ( ( 1.000000000000000000, 1.857142857142858317, 1.000000000000000000, 1.000000000000000000, 1.000000000000000000 ) ) 
 REPRESENTATION_ITEM ( '' )  );
#73510=CARTESIAN_POINT ( 'NONE',  ( 13.44497361249347556, 42.85008855513920878, -92.01621721121948383 ) ) ;
#73558=CARTESIAN_POINT ( 'NONE',  ( -12.50000000000000711, 18.64303733123573537, -36.27143273323382999 ) ) ;
#73567=CARTESIAN_POINT ( 'NONE',  ( -7.442703362271647194, 40.98154495329247737, -69.28862671947442209 ) ) ;
#73603=CARTESIAN_POINT ( 'NONE',  ( 12.50000000000000533, 41.05801042994118433, -71.24449801089164680 ) ) ;
#73611=B_SPLINE_CURVE_WITH_KNOTS ( 'NONE', 3,
 ( #73896, #56097, #65283, #49079 ),
 .UNSPECIFIED., .F., .F.,
 ( 4, 4 ),
 ( 0.000000000000000000, 1.000000000000000000 ),
 .UNSPECIFIED. ) ;
#73614=B_SPLINE_CURVE_WITH_KNOTS ( 'NONE', 3,
 ( #73336, #73879, #106774, #33999, #98157, #81959, #32924, #66326, #57684, #42048, #16178, #8615, #91678, #82512, #24311, #90607, #9664, #65799, #99209, #98676, #50643, #49605, #74932, #72808, #58782, #64738, #41517, #17794, #74403, #105715, #49064, #97614, #16716, #25373, #7539, #56627, #58229, #48535, #81426, #40456 ),
 .UNSPECIFIED., .F., .F.,
 ( 4, 1, 1, 1, 1, 1, 1, 2, 2, 1, 1, 1, 1, 1, 2, 2, 1, 1, 1, 1, 1, 1, 2, 2, 1, 1, 1, 2, 2, 4 ),
 ( 0.000000000000000000, 0.1250000000000340283, 0.1875000000000504874, 0.2187500000000587308, 0.2343750000000622558, 0.2421875000000639766, 0.2460937500000649203, 0.2480468750000653366, 0.2500000000000657252, 0.3750000000000667799, 0.4375000000000666689, 0.4687500000000665024, 0.4843750000000663913, 0.4921875000000663913, 0.4960937500000657252, 0.5000000000000650591, 0.6250000000000497380, 0.6875000000000424105, 0.7187500000000386358, 0.7343750000000368594, 0.7421875000000359712, 0.7460937500000354161, 0.7480468750000351941, 0.7500000000000349720, 0.8125000000000258682, 0.8437500000000213163, 0.8593750000000189848, 0.8671875000000177636, 0.8750000000000165423, 1.000000000000000000 ),
 .UNSPECIFIED. ) ;
#73616=CARTESIAN_POINT ( 'NONE',  ( 62.01418705508225315, 38.95383793066456946, 16.66584972136411480 ) ) ;
#73627=CARTESIAN_POINT ( 'NONE',  ( -8.922269033015549411, -5.000000000000000000, -5.219866590717671784 ) ) ;
#73659=CARTESIAN_POINT ( 'NONE',  ( 17.49999999999850431, 50.00907933620509027, 60.12834585265864007 ) ) ;
#73662=PRESENTATION_STYLE_ASSIGNMENT (( #45304 ) ) ;
#73669=CARTESIAN_POINT ( 'NONE',  ( -6.731961105522484168, -4.334285474471498034, -16.87634736350372222 ) ) ;
#73685=CONICAL_SURFACE ( 'NONE', #59948, 15.00000000000000178, 0.7292773806962717931 ) ;
#73695=CARTESIAN_POINT ( 'NONE',  ( 62.59524157948160905, 49.99999999997998401, 18.50207713769105311 ) ) ;
#73719=CARTESIAN_POINT ( 'NONE',  ( 15.51400478511171244, 41.97981636269011574, -85.80391510450277792 ) ) ;
#73721=CARTESIAN_POINT ( 'NONE',  ( 4.852941176470595863, 39.99999999999999289, -70.80672828634229177 ) ) ;
#73755=CARTESIAN_POINT ( 'NONE',  ( 5.430163322397451253, 41.93410894844108583, -59.17461580565397128 ) ) ;
#73767=ORIENTED_EDGE ( 'NONE', *, *, #72078, .F. ) ;
#73775=CARTESIAN_POINT ( 'NONE',  ( 8.000000000000000000, -3.000000000000000000, -2.094395098902536834 ) ) ;
#73781=CARTESIAN_POINT ( 'NONE',  ( -12.50000000000000711, -4.999999999999999112, -79.51734232575269345 ) ) ;
#73858=CARTESIAN_POINT ( 'NONE',  ( 6.542885630808934927, 41.77241054322398384, -59.03854290128418825 ) ) ;
#73879=CARTESIAN_POINT ( 'NONE',  ( -9.499963314427418482, -5.000000000000000000, -20.52065077656356351 ) ) ;
#73889=CARTESIAN_POINT ( 'NONE',  ( 52.56483885390523625, 48.00000000000000000, -38.23529411764706509 ) ) ;
#73896=CARTESIAN_POINT ( 'NONE',  ( 12.49955057316562090, -4.332870170068738425, -12.71907580248059233 ) ) ;
#73897=CARTESIAN_POINT ( 'NONE',  ( 7.101747359470889975, -4.047770588429576044, -17.37629258577385727 ) ) ;
#73898=CARTESIAN_POINT ( 'NONE',  ( -43.53427904077744159, 41.44002608692422029, -50.65026129109237019 ) ) ;
#73911=CARTESIAN_POINT ( 'NONE',  ( -17.49999999999842260, 50.02580020273055084, 60.61389435658627889 ) ) ;
#73926=CARTESIAN_POINT ( 'NONE',  ( -31.96306626099171311, 40.83985558186470399, -63.64673710329628165 ) ) ;
#73932=CARTESIAN_POINT ( 'NONE',  ( 5.036189802310023111, -5.000000000000002665, -76.26213611588336505 ) ) ;
#73933=CARTESIAN_POINT ( 'NONE',  ( -7.126148247341459019, 41.12758119229484066, -58.55282700859728351 ) ) ;
#73949=CARTESIAN_POINT ( 'NONE',  ( 11.20323936960019928, -5.000000000000000000, -78.29850497474416215 ) ) ;
#73994=CARTESIAN_POINT ( 'NONE',  ( 6.701893401236465486, 41.44328394225253476, -70.59544911815949320 ) ) ;
#74014=CARTESIAN_POINT ( 'NONE',  ( 6.856834870136921722, 41.38254192504039963, -70.56142689300520487 ) ) ;
#74016=CIRCLE ( 'NONE', #3432, 60.00000000000000000 ) ;
#74037=CARTESIAN_POINT ( 'NONE',  ( 7.416285617647480066, 41.02764994231083762, -59.17152657697691609 ) ) ;
#74049=CARTESIAN_POINT ( 'NONE',  ( 14.33580413386840213, 42.00000000000000000, -89.41414995614803729 ) ) ;
#74070=CARTESIAN_POINT ( 'NONE',  ( -6.195804093982627769, 41.59435685013754380, -70.65487364512668478 ) ) ;
#74078=CARTESIAN_POINT ( 'NONE',  ( 6.464976090918999496, 41.32133059754584536, -58.37832579531859523 ) ) ;
#74101=CARTESIAN_POINT ( 'NONE',  ( -7.321076910647204450, 40.29402652806530227, -70.66289162821402670 ) ) ;
#74106=ORIENTED_EDGE ( 'NONE', *, *, #86587, .T. ) ;
#74117=DIRECTION ( 'NONE',  ( 0.000000000000000000, 0.000000000000000000, 1.000000000000000000 ) ) ;
#74122=( LENGTH_UNIT ( ) NAMED_UNIT ( * ) SI_UNIT ( .MILLI., .METRE. ) );
#74160=MECHANICAL_DESIGN_GEOMETRIC_PRESENTATION_REPRESENTATION('',(#79332),#75940);
#74164=ADVANCED_FACE ( 'NONE', ( #53229 ), #51109, .T. ) ;
#74165=CARTESIAN_POINT ( 'NONE',  ( -7.137815226409941260, -3.000000000000000000, 4.175893272574811910 ) ) ;
#74190=CARTESIAN_POINT ( 'NONE',  ( 19.42937650476797629, 49.96296734528399242, 60.82359239913252225 ) ) ;
#74200=CARTESIAN_POINT ( 'NONE',  ( -7.014891834166682827, -4.207085196961300788, -17.12005312235260845 ) ) ;
#74217=UNCERTAINTY_MEASURE_WITH_UNIT (LENGTH_MEASURE( 1.000000000000000082E-05 ), #106532, 'distance_accuracy_value', 'NONE');
#74227=CARTESIAN_POINT ( 'NONE',  ( 11.91432047182400211, 48.00000000000000000, 64.17585289259234571 ) ) ;
#74242=CARTESIAN_POINT ( 'NONE',  ( -38.12216208879733870, 18.64284798593187631, -4.860317469385954325 ) ) ;
#74243=EDGE_LOOP ( 'NONE', ( #88950, #100219, #81353, #57964 ) ) ;
#74288=UNCERTAINTY_MEASURE_WITH_UNIT (LENGTH_MEASURE( 1.000000000000000082E-05 ), #25168, 'distance_accuracy_value', 'NONE');
#74311=SURFACE_STYLE_USAGE ( .BOTH. , #9569 ) ;
#74313=CARTESIAN_POINT ( 'NONE',  ( -17.49999999999997513, 49.62432460127385525, 63.94669766439164960 ) ) ;
#74315=CARTESIAN_POINT ( 'NONE',  ( -12.50000000000000711, -4.999999999999999112, -78.42624373368740009 ) ) ;
#74350=CARTESIAN_POINT ( 'NONE',  ( -7.069742149889167493, 41.66287055432060527, -69.58314084294492829 ) ) ;
#74370=CARTESIAN_POINT ( 'NONE',  ( 6.123233995736763324E-16, 48.00000000000000000, -75.00000000000001421 ) ) ;
#74373=CARTESIAN_POINT ( 'NONE',  ( 88.20421627925426833, 42.00000000000000000, 23.70422451874904013 ) ) ;
#74393=CARTESIAN_POINT ( 'NONE',  ( -5.075566108724573589, -4.332661967060489339, -17.09624963492156624 ) ) ;
#74398=ORIENTED_EDGE ( 'NONE', *, *, #93967, .T. ) ;
#74403=CARTESIAN_POINT ( 'NONE',  ( -7.454085080097326177, -5.000000000000000000, -15.56508920776378702 ) ) ;
#74413=SURFACE_STYLE_FILL_AREA ( #65274 ) ;
#74424=CARTESIAN_POINT ( 'NONE',  ( 9.499999896953584155, -5.000000000000023093, -20.99851281918370205 ) ) ;
#74427=CARTESIAN_POINT ( 'NONE',  ( -38.53974113589808326, 42.10961629870702438, -57.51661569422308418 ) ) ;
#74440=CARTESIAN_POINT ( 'NONE',  ( -17.49999999999739941, 49.76444793454294313, 62.19248936617950818 ) ) ;
#74456=CARTESIAN_POINT ( 'NONE',  ( -23.01262813884551761, 41.68868216767802437, -75.63873355076052007 ) ) ;
#74462=CARTESIAN_POINT ( 'NONE',  ( -7.374560640984191728, -5.000000000000002665, -75.40399789251388540 ) ) ;
#74487=CARTESIAN_POINT ( 'NONE',  ( 11.63000494888384395, 38.95405869521447784, 62.66525763215405220 ) ) ;
#74494=CARTESIAN_POINT ( 'NONE',  ( -4.205882352941162416, -5.000000000000000000, -72.69916451482997388 ) ) ;
#74553=CARTESIAN_POINT ( 'NONE',  ( -58.66291549205074318, 49.99999999999999289, -23.00456702330189174 ) ) ;
#74580=( NAMED_UNIT ( * ) PLANE_ANGLE_UNIT ( ) SI_UNIT ( $, .RADIAN. ) );
#74603=CARTESIAN_POINT ( 'NONE',  ( 5.420470438621123321, 41.88321586334136981, -59.04137885805280916 ) ) ;
#74620=VERTEX_POINT ( 'NONE', #34958 ) ;
#74630=CARTESIAN_POINT ( 'NONE',  ( 8.841337832402281549, 48.00000000000000711, -97.17444126923535919 ) ) ;
#74634=CARTESIAN_POINT ( 'NONE',  ( -7.176538178872569951, 40.00000000006200196, -70.93639620227449427 ) ) ;
#74677=CARTESIAN_POINT ( 'NONE',  ( 54.43501200703078524, 38.95383793069735390, -33.39731814189929082 ) ) ;
#74721=CARTESIAN_POINT ( 'NONE',  ( -6.542885568110277106, 41.77240995323538897, -59.03854211387476880 ) ) ;
#74754=CARTESIAN_POINT ( 'NONE',  ( 65.26738680890606759, 48.00000000000000000, 0.8120011905328435864 ) ) ;
#74765=CARTESIAN_POINT ( 'NONE',  ( -36.90124019533217137, 18.64284798593122616, 10.73407659158960747 ) ) ;
#74791=CARTESIAN_POINT ( 'NONE',  ( -6.642722259512091831, 41.46658730094534917, -70.60825968550385312 ) ) ;
#74802=B_SPLINE_CURVE_WITH_KNOTS ( 'NONE', 3,
 ( #20738, #94033, #44426, #68717, #101600, #36898, #61145, #77322 ),
 .UNSPECIFIED., .F., .F.,
 ( 4, 2, 2, 4 ),
 ( 0.000000000000000000, 0.5000000000000000000, 0.7500000000000000000, 1.000000000000000000 ),
 .UNSPECIFIED. ) ;
#74835=CARTESIAN_POINT ( 'NONE',  ( -17.49999999999997158, 48.72924342453988089, 64.08323380050735807 ) ) ;
#74837=CARTESIAN_POINT ( 'NONE',  ( -12.49999999999999822, -4.999999999999999112, -34.12705337364893410 ) ) ;
#74857=ORIENTED_EDGE ( 'NONE', *, *, #91013, .F. ) ;
#74878=CARTESIAN_POINT ( 'NONE',  ( -6.828042834505471781, 41.63841151066672808, -58.95291702778770571 ) ) ;
#74884=ORIENTED_EDGE ( 'NONE', *, *, #59223, .T. ) ;
#74899=CARTESIAN_POINT ( 'NONE',  ( -88.20421627925426833, 42.00000000000000000, -23.70422451879017345 ) ) ;
#74908=CARTESIAN_POINT ( 'NONE',  ( 6.784953749580444615, 41.67963532863181797, -59.00226812211813154 ) ) ;
#74932=CARTESIAN_POINT ( 'NONE',  ( -7.890153520192944470, -5.000000000000000000, -15.80729722286742067 ) ) ;
#74939=CARTESIAN_POINT ( 'NONE',  ( -7.996668422906619611, -3.000000000000002665, -78.85453279917568636 ) ) ;
#74942=CARTESIAN_POINT ( 'NONE',  ( -9.500000000000003553, -5.000000000000000000, -68.91429205785459544 ) ) ;
#74952=CARTESIAN_POINT ( 'NONE',  ( -2.751706330279349633, -3.000000000000002665, -100.0000000000000000 ) ) ;
#74970=CARTESIAN_POINT ( 'NONE',  ( -19.13866731017106204, 49.71730248559588006, 61.67331676225234105 ) ) ;
#74981=CARTESIAN_POINT ( 'NONE',  ( -24.58887437406745491, 41.57629742064543166, -73.51403340649437723 ) ) ;
#74987=CARTESIAN_POINT ( 'NONE',  ( 9.999999999999994671, -3.000000000000002665, -86.30899693747679180 ) ) ;
#75044=DIRECTION ( 'NONE',  ( 0.000000000000000000, 0.000000000000000000, 1.000000000000000000 ) ) ;
#75048=CARTESIAN_POINT ( 'NONE',  ( 6.757705285491359071, 41.35007050631321590, -70.67351639401239538 ) ) ;
#75063=CARTESIAN_POINT ( 'NONE',  ( 3.430943074671123583, -4.332661967060490227, -17.58450835315055016 ) ) ;
#75074=CARTESIAN_POINT ( 'NONE',  ( -1.727368016638141196E-09, 38.95322581935191408, 63.66965480466879512 ) ) ;
#75097=CARTESIAN_POINT ( 'NONE',  ( 7.347880794884118356E-15, 50.00000000000000000, -60.00000000000000000 ) ) ;
#75106=STYLED_ITEM ( 'NONE', ( #36805 ), #24876 ) ;
#75114=STYLED_ITEM ( 'NONE', ( #39147 ), #23817 ) ;
#75132=CARTESIAN_POINT ( 'NONE',  ( -59.23741894013591036, 42.00000000000000711, -7.754160006507100356 ) ) ;
#75142=SURFACE_SIDE_STYLE ('',( #9341 ) ) ;
#75144=ORIENTED_EDGE ( 'NONE', *, *, #66422, .F. ) ;
#75145=CARTESIAN_POINT ( 'NONE',  ( 15.01526275298277824, 41.97362047124263285, -85.67312571145951949 ) ) ;
#75164=CARTESIAN_POINT ( 'NONE',  ( -7.358394980812720476, 41.06696360374984067, -70.11548085267834551 ) ) ;
#75197=CARTESIAN_POINT ( 'NONE',  ( 12.50000000000000711, 39.74926845579918933, -65.00518738068748803 ) ) ;
#75212=CARTESIAN_POINT ( 'NONE',  ( -16.52732684424165654, 43.98685724163156863, -87.77868211029610279 ) ) ;
#75216=ORIENTED_EDGE ( 'NONE', *, *, #23275, .T. ) ;
#75231=CARTESIAN_POINT ( 'NONE',  ( -5.477641402353350841, 41.99667695465397088, -59.64144010652168504 ) ) ;
#75259=CARTESIAN_POINT ( 'NONE',  ( 5.500000036871884213, 42.00000000000000000, -68.91429207046176941 ) ) ;
#75274=CARTESIAN_POINT ( 'NONE',  ( 52.56483885390524335, 49.99999999999999289, -38.23529411764707220 ) ) ;
#75290=CARTESIAN_POINT ( 'NONE',  ( -7.500000000000007105, 39.99999999999998579, -68.91429205786793943 ) ) ;
#75291=CARTESIAN_POINT ( 'NONE',  ( 37.84772257691316355, 50.00000000000000000, 50.69408796163846631 ) ) ;
#75294=EDGE_CURVE ( 'NONE', #78094, #21685, #54042, .T. ) ;
#75311=ORIENTED_EDGE ( 'NONE', *, *, #19756, .T. ) ;
#75319=STYLED_ITEM ( 'NONE', ( #25231 ), #101388 ) ;
#75331=CARTESIAN_POINT ( 'NONE',  ( -8.737863884121393809, 49.99999999999999289, -90.03618980231146907 ) ) ;
#75349=UNCERTAINTY_MEASURE_WITH_UNIT (LENGTH_MEASURE( 1.000000000000000082E-05 ), #4103, 'distance_accuracy_value', 'NONE');
#75377=CARTESIAN_POINT ( 'NONE',  ( -17.49999999999997513, 49.01643442013767782, 64.05028169109587566 ) ) ;
#75391=CARTESIAN_POINT ( 'NONE',  ( 7.500000000000000888, -3.000671055698259870, -20.99923901233272971 ) ) ;
#75398=CARTESIAN_POINT ( 'NONE',  ( -14.81135389224447962, 41.99477687821654115, -87.54767125253117399 ) ) ;
#75446=CARTESIAN_POINT ( 'NONE',  ( 9.797174393178825657E-16, -5.000000000000000000, -8.000000000000000000 ) ) ;
#75450=MECHANICAL_DESIGN_GEOMETRIC_PRESENTATION_REPRESENTATION('',(#3165),#53065);
#75455=CARTESIAN_POINT ( 'NONE',  ( -7.500000000000008882, 42.00000000000000711, -70.16688272716517361 ) ) ;
#75465=CARTESIAN_POINT ( 'NONE',  ( -4.905843853654967113, -4.999999999999999112, -16.52456679617691293 ) ) ;
#75466=CARTESIAN_POINT ( 'NONE',  ( -5.036189803708995605, -3.000000000000002665, -76.26213611645742674 ) ) ;
#75493=SURFACE_STYLE_USAGE ( .BOTH. , #17811 ) ;
#75494=CARTESIAN_POINT ( 'NONE',  ( 8.857351009221135385, -3.000000000000003109, -97.18047212223504516 ) ) ;
#75514=CARTESIAN_POINT ( 'NONE',  ( -19.50000000000036593, 50.00000000000000711, 59.91915230424519478 ) ) ;
#75527=CARTESIAN_POINT ( 'NONE',  ( -5.420469775605654128, 41.88321586335170821, -59.04137891894603030 ) ) ;
#75546=ADVANCED_BREP_SHAPE_REPRESENTATION ( '', ( #54736, #10728 ), #93449 ) ;
#75557=( BOUNDED_SURFACE ( )  B_SPLINE_SURFACE ( 2, 3, ( 
 ( #101035, #19106, #4470, #10940, #29316, #11477, #45476, #43862 ),
 ( #60080, #102637, #51416, #92944, #10425, #44951, #51944, #35816 ),
 ( #69225, #37409, #43339, #94014, #70273, #76754, #36876, #68696 ) ),
 .UNSPECIFIED., .F., .F., .F. ) 
 B_SPLINE_SURFACE_WITH_KNOTS ( ( 3, 3 ),
 ( 4, 2, 2, 4 ),
 ( 0.000000000000000000, 1.000000000000000000 ),
 ( 5.707226654021456902, 5.953728167561664009, 6.612642446797508455, 6.859143960337715562 ),
 .UNSPECIFIED. ) 
 GEOMETRIC_REPRESENTATION_ITEM ( )  RATIONAL_B_SPLINE_SURFACE ( (
 ( 1.000000000000000000, 1.000000000000000000, 1.000000000000000000, 1.000000000000000000, 1.000000000000000000, 1.000000000000000000, 1.000000000000000000, 1.000000000000000000),
 ( 1.857142857142858317, 1.857142857142858317, 1.857142857142858317, 1.857142857142858317, 1.857142857142858317, 1.857142857142858317, 1.857142857142858317, 1.857142857142858317),
 ( 1.000000000000000000, 1.000000000000000000, 1.000000000000000000, 1.000000000000000000, 1.000000000000000000, 1.000000000000000000, 1.000000000000000000, 1.000000000000000000) ) ) 
 REPRESENTATION_ITEM ( '' )  SURFACE ( )  );
#75596=CARTESIAN_POINT ( 'NONE',  ( -6.931965282482035917, 41.62850913407595499, -59.01894715436439753 ) ) ;
#75609=CARTESIAN_POINT ( 'NONE',  ( 5.075566108724593128, -4.332661967060489339, -17.09624963492156269 ) ) ;
#75633=CARTESIAN_POINT ( 'NONE',  ( 15.30771400658271908, 18.64284798592852965, 35.25047262264993719 ) ) ;
#75649=CARTESIAN_POINT ( 'NONE',  ( -4.852941176470593199, 24.91666666666666430, -70.80672828634229177 ) ) ;
#75658=CARTESIAN_POINT ( 'NONE',  ( -7.500000000000000888, -3.000671055698259870, -20.99923901233272971 ) ) ;
#75674=CARTESIAN_POINT ( 'NONE',  ( 79.13121736037263076, 42.00000000000000000, 45.60838156036771096 ) ) ;
#75685=CARTESIAN_POINT ( 'NONE',  ( -64.33158975147043179, 40.83917765566846469, 9.759077203600947215 ) ) ;
#75703=CARTESIAN_POINT ( 'NONE',  ( -1.177401751624803428, 48.00000000000000711, -100.0000000000000142 ) ) ;
#75708=CARTESIAN_POINT ( 'NONE',  ( -7.392085442450220256, 40.93519827090806729, -70.13194593521265574 ) ) ;
#75713=ADVANCED_FACE ( 'NONE', ( #659 ), #91772, .T. ) ;
#75718=CARTESIAN_POINT ( 'NONE',  ( -5.062487338738201892, -5.000000000000000888, 8.716223939771381879 ) ) ;
#75747=CARTESIAN_POINT ( 'NONE',  ( -7.230783165911326194, -2.999999999999882760, -70.90935356276069967 ) ) ;
#75757=ADVANCED_FACE ( 'NONE', ( #82146 ), #40732, .T. ) ;
#75777=CARTESIAN_POINT ( 'NONE',  ( -5.454982624654864054, 41.97810475128825658, -59.40149861125610897 ) ) ;
#75779=SURFACE_STYLE_FILL_AREA ( #90912 ) ;
#75795=COLOUR_RGB ( '', 0.72549020, 0.75294118, 0.79215686) ;
#75796=CARTESIAN_POINT ( 'NONE',  ( 62.59524157943331346, 48.00000000000000000, 18.50207713769442819 ) ) ;
#75818=CARTESIAN_POINT ( 'NONE',  ( 4.408728476930471644E-15, 0.000000000000000000, -15.00000000000000178 ) ) ;
#75830=CARTESIAN_POINT ( 'NONE',  ( -5.405952399528404229, 41.79441213502661157, -58.87429169783612792 ) ) ;
#75833=VECTOR ( 'NONE', #5417, 1000.000000000000000 ) ;
#75845=CARTESIAN_POINT ( 'NONE',  ( -35.10078947235764701, 18.64284798593234171, -15.64789144405767729 ) ) ;
#75853=CARTESIAN_POINT ( 'NONE',  ( 0.000000000000000000, 0.000000000000000000, 60.00000000000000000 ) ) ;
#75859=CARTESIAN_POINT ( 'NONE',  ( 45.44999599557070269, 39.19940254507191213, -45.67500132316253314 ) ) ;
#75873=CARTESIAN_POINT ( 'NONE',  ( 7.374560640985523996, 50.00000000000000000, -75.40399789250294305 ) ) ;
#75916=SURFACE_STYLE_FILL_AREA ( #44634 ) ;
#75934=CIRCLE ( 'NONE', #60414, 8.000000000000000000 ) ;
#75937=CARTESIAN_POINT ( 'NONE',  ( -2.078747088351100114, 50.00000000000001421, -98.00015842815599854 ) ) ;
#75940=( GEOMETRIC_REPRESENTATION_CONTEXT ( 3 ) GLOBAL_UNCERTAINTY_ASSIGNED_CONTEXT ( ( #43995 ) ) GLOBAL_UNIT_ASSIGNED_CONTEXT ( ( #79333, #20095, #80920 ) ) REPRESENTATION_CONTEXT ( 'NONE', 'WORKASPACE' ) );
#75955=PLANE ( 'NONE',  #78895 ) ;
#75962=CARTESIAN_POINT ( 'NONE',  ( -7.126148247341457242, 41.12758119229482645, -58.55282700859728351 ) ) ;
#75979=CARTESIAN_POINT ( 'NONE',  ( -55.65414010186731986, 42.00000000000000000, 72.41885610124127481 ) ) ;
#75989=ORIENTED_EDGE ( 'NONE', *, *, #106727, .F. ) ;
#76023=CARTESIAN_POINT ( 'NONE',  ( 12.12626197893212243, -3.000000000000002665, -94.24800833403466527 ) ) ;
#76061=CARTESIAN_POINT ( 'NONE',  ( 2.617478844989858722, -3.000000000000002665, -75.26027323389553203 ) ) ;
#76064=CARTESIAN_POINT ( 'NONE',  ( 5.625019092414619948, 41.66287055497627989, -70.61600277306789053 ) ) ;
#76081=COLOUR_RGB ( '', 0.72549020, 0.75294118, 0.79215686) ;
#76093=CARTESIAN_POINT ( 'NONE',  ( 16.51905981272403423, 42.00139749746823981, -87.79004739960673476 ) ) ;
#76095=CARTESIAN_POINT ( 'NONE',  ( 5.096247963225427391, -4.999999999999998224, -73.00359695309825270 ) ) ;
#76106=( LENGTH_UNIT ( ) NAMED_UNIT ( * ) SI_UNIT ( .MILLI., .METRE. ) );
#76123=CARTESIAN_POINT ( 'NONE',  ( -7.500000000000006217, 40.19558924101049513, -59.64746548774058965 ) ) ;
#76124=CARTESIAN_POINT ( 'NONE',  ( 6.924711585765388477, 40.92328497145224020, -70.90711766198887744 ) ) ;
#76140=( NAMED_UNIT ( * ) SI_UNIT ( $, .STERADIAN. ) SOLID_ANGLE_UNIT ( ) );
#76178=SURFACE_STYLE_FILL_AREA ( #59493 ) ;
#76187=CARTESIAN_POINT ( 'NONE',  ( 19.09326099321046755, 49.66527553188159771, 61.75128748409139234 ) ) ;
#76203=CARTESIAN_POINT ( 'NONE',  ( -72.41885610115926397, 42.00000000000000000, -55.65414010186705696 ) ) ;
#76211=CARTESIAN_POINT ( 'NONE',  ( -56.10248074403467911, 40.83957962598827862, -33.37184059469758068 ) ) ;
#76231=CARTESIAN_POINT ( 'NONE',  ( -7.996668422907487361, 49.99999999999999289, -91.14546720082822162 ) ) ;
#76246=CARTESIAN_POINT ( 'NONE',  ( 4.872636759907720716, 41.00341855746686548, -70.74912513459382524 ) ) ;
#76291=ADVANCED_FACE ( 'NONE', ( #36184 ), #11846, .T. ) ;
#76327=CARTESIAN_POINT ( 'NONE',  ( 7.500000000000007105, 39.99999999999998579, -68.91429205785453860 ) ) ;
#76329=CARTESIAN_POINT ( 'NONE',  ( -5.880230824525982669, -4.999999999999742428, -15.32427097195931864 ) ) ;
#76346=UNCERTAINTY_MEASURE_WITH_UNIT (LENGTH_MEASURE( 1.000000000000000082E-05 ), #70229, 'distance_accuracy_value', 'NONE');
#76350=CARTESIAN_POINT ( 'NONE',  ( 5.406991766687864853, 42.00000000000000000, -69.18631089694002867 ) ) ;
#76352=CARTESIAN_POINT ( 'NONE',  ( -62.34828826644581312, 50.00000000000000000, -10.72527895994686986 ) ) ;
#76363=CARTESIAN_POINT ( 'NONE',  ( -36.68673791898479664, 18.64284798593215342, -11.44574982652938999 ) ) ;
#76369=( GEOMETRIC_REPRESENTATION_CONTEXT ( 3 ) GLOBAL_UNCERTAINTY_ASSIGNED_CONTEXT ( ( #28754 ) ) GLOBAL_UNIT_ASSIGNED_CONTEXT ( ( #93708, #34965, #86168 ) ) REPRESENTATION_CONTEXT ( 'NONE', 'WORKASPACE' ) );
#76377=CARTESIAN_POINT ( 'NONE',  ( 42.15373538487478555, 39.53920096513062532, -50.09085211413447070 ) ) ;
#76382=SURFACE_STYLE_FILL_AREA ( #43503 ) ;
#76394=CARTESIAN_POINT ( 'NONE',  ( 9.999999999999989342, 49.99999999999999289, -83.69100306251233690 ) ) ;
#76439=CARTESIAN_POINT ( 'NONE',  ( -19.25089800403961959, 49.99999999999999289, 60.24512152074786542 ) ) ;
#76478=FACE_BOUND ( 'NONE', #100945, .T. ) ;
#76492=ORIENTED_EDGE ( 'NONE', *, *, #37050, .F. ) ;
#76504=CARTESIAN_POINT ( 'NONE',  ( 7.099152780515114891, 41.70084721948487072, -59.82719249545999674 ) ) ;
#76505=ADVANCED_FACE ( 'NONE', ( #19219 ), #29257, .T. ) ;
#76506=CARTESIAN_POINT ( 'NONE',  ( 23.70422451876635250, 42.00000000000004263, -88.20421627930062414 ) ) ;
#76513=ORIENTED_EDGE ( 'NONE', *, *, #90136, .F. ) ;
#76515=CARTESIAN_POINT ( 'NONE',  ( 5.373715277452113526, 41.43915641971339170, -58.48990532576927848 ) ) ;
#76532=CARTESIAN_POINT ( 'NONE',  ( 7.036764705882358584, 40.00000000373366049, -71.06385277390856459 ) ) ;
#76550=CARTESIAN_POINT ( 'NONE',  ( -13.73780227957491284, -3.000000000000002665, -78.37846873786676838 ) ) ;
#76568=EDGE_CURVE ( 'NONE', #22777, #67117, #102160, .T. ) ;
#76570=CARTESIAN_POINT ( 'NONE',  ( -17.49999999999995381, 51.99573851567584626, 60.30773471724109669 ) ) ;
#76594=CARTESIAN_POINT ( 'NONE',  ( 7.996668422910687468, -3.000000000000002665, -91.14546720082027775 ) ) ;
#76622=CARTESIAN_POINT ( 'NONE',  ( 14.75116209840774850, 43.55504285524111907, -90.22050492864485705 ) ) ;
#76624=CARTESIAN_POINT ( 'NONE',  ( 19.49614903793134246, 49.99973670987868957, 59.99522355992422007 ) ) ;
#76633=CARTESIAN_POINT ( 'NONE',  ( -12.22950890273588165, -4.580576956129855049, -12.66933385000461065 ) ) ;
#76638=CARTESIAN_POINT ( 'NONE',  ( -7.500000000000006217, 31.97088361167177339, -52.67517300286423421 ) ) ;
#76647=CARTESIAN_POINT ( 'NONE',  ( -9.500000000000003553, -5.000000000000000000, -68.91429205785459544 ) ) ;
#76650=CARTESIAN_POINT ( 'NONE',  ( -19.19191325036121398, 49.76861282268819053, 61.57617224385840871 ) ) ;
#76651=CARTESIAN_POINT ( 'NONE',  ( -7.303354903313936219, 41.37531411535626802, -59.25981086040365398 ) ) ;
#76652=CARTESIAN_POINT ( 'NONE',  ( 5.209799036363110147, 40.00000000078713214, -70.92874456541859729 ) ) ;
#76666=CARTESIAN_POINT ( 'NONE',  ( 4.852941176470594975, -4.999999999999998224, -70.80672828634229177 ) ) ;
#76668=CARTESIAN_POINT ( 'NONE',  ( 6.784953749580444615, 41.67963532863181797, -59.00226812211813154 ) ) ;
#76698=DIRECTION ( 'NONE',  ( 0.000000000000000000, 1.000000000000000000, 0.000000000000000000 ) ) ;
#76699=CARTESIAN_POINT ( 'NONE',  ( 5.062272329166140672, -5.000000000000001776, 8.716576110310610304 ) ) ;
#76735=( LENGTH_UNIT ( ) NAMED_UNIT ( * ) SI_UNIT ( .MILLI., .METRE. ) );
#76742=CARTESIAN_POINT ( 'NONE',  ( 39.08472187170780643, 40.83956871101882058, 52.27844079319547177 ) ) ;
#76754=CARTESIAN_POINT ( 'NONE',  ( 6.019162162300498053, 39.99999999999999289, -71.20548073448658499 ) ) ;
#76763=CARTESIAN_POINT ( 'NONE',  ( 11.99999999999999467, 50.00000000000000000, -86.57079632498522415 ) ) ;
#76775=CARTESIAN_POINT ( 'NONE',  ( -8.737863883542573262, 48.00000000000000711, -79.96381019629099285 ) ) ;
#76787=CARTESIAN_POINT ( 'NONE',  ( -6.565380407527345419, 40.29402549571846492, -71.20315154365353294 ) ) ;
#76799=CARTESIAN_POINT ( 'NONE',  ( -17.83514733193546320, 45.00000000000000711, 62.69713390834871802 ) ) ;
#76818=ORIENTED_EDGE ( 'NONE', *, *, #23728, .T. ) ;
#76837=CARTESIAN_POINT ( 'NONE',  ( 11.06459909230147254, -4.984765618719626090, -12.57729599004233911 ) ) ;
#76845=CARTESIAN_POINT ( 'NONE',  ( -8.480908980008681652, -4.333298119783866476, 15.78559285099031761 ) ) ;
#76850=CARTESIAN_POINT ( 'NONE',  ( 7.500000000000005329, -3.000000000000000000, -52.94236561372729000 ) ) ;
#76854=CARTESIAN_POINT ( 'NONE',  ( -60.62677696746903422, 48.00000000000000000, 24.18439665018601303 ) ) ;
#76866=CARTESIAN_POINT ( 'NONE',  ( -4.640047946013393876, -5.000000000000039968, -15.63625121056854184 ) ) ;
#76887=SURFACE_STYLE_USAGE ( .BOTH. , #27335 ) ;
#76889=CARTESIAN_POINT ( 'NONE',  ( 6.602502617004377683, 41.80321047191768002, -70.07543148703942393 ) ) ;
#76892=CARTESIAN_POINT ( 'NONE',  ( 5.774137037018601148, 50.00000000000000000, 63.00000000000000000 ) ) ;
#76894=B_SPLINE_CURVE_WITH_KNOTS ( 'NONE', 3,
 ( #76327, #20285, #93597, #53135 ),
 .UNSPECIFIED., .F., .F.,
 ( 4, 4 ),
 ( 0.000000000000000000, 1.000000000000000000 ),
 .UNSPECIFIED. ) ;
#76937=CARTESIAN_POINT ( 'NONE',  ( 1.308996937483428491, 49.99999999999999289, -95.00000000000001421 ) ) ;
#76946=CARTESIAN_POINT ( 'NONE',  ( 1.262844703064978993E-15, -3.000000000000002665, -95.00000000000000000 ) ) ;
#76964=ORIENTED_EDGE ( 'NONE', *, *, #86147, .F. ) ;
#76988=STYLED_ITEM ( 'NONE', ( #29444 ), #4960 ) ;
#77019=CARTESIAN_POINT ( 'NONE',  ( -4.966176470918028052, 41.64999999999999147, -70.47555194646973575 ) ) ;
#77042=FACE_OUTER_BOUND ( 'NONE', #91999, .T. ) ;
#77044=CARTESIAN_POINT ( 'NONE',  ( 6.690415142086856726, 41.73276191905608812, -59.04972836783017698 ) ) ;
#77045=CARTESIAN_POINT ( 'NONE',  ( 23.57730434123481800, 18.64316884710268596, -30.67950393663962672 ) ) ;
#77075=CARTESIAN_POINT ( 'NONE',  ( 7.493977565380718353, 40.56334570848421350, -69.29067317619599464 ) ) ;
#77095=CARTESIAN_POINT ( 'NONE',  ( 14.92100282753648344, -3.000000000000003109, -82.95543583085692774 ) ) ;
#77115=CARTESIAN_POINT ( 'NONE',  ( -17.49999999999991473, 51.99998113221733576, 59.93765433267815013 ) ) ;
#77146=CARTESIAN_POINT ( 'NONE',  ( 17.39901153685599411, -4.999999999999999112, 2.593512410380747646 ) ) ;
#77171=FACE_OUTER_BOUND ( 'NONE', #42555, .T. ) ;
#77173=CARTESIAN_POINT ( 'NONE',  ( 7.500000000000003553, -2.999999999999876099, -69.80246343544249044 ) ) ;
#77183=CARTESIAN_POINT ( 'NONE',  ( -7.499999999939189976, 33.41357786079682768, -51.06910100954272735 ) ) ;
#77188=CARTESIAN_POINT ( 'NONE',  ( -17.49999999999997513, 50.00000000000000000, 100.0000000000000000 ) ) ;
#77192=CARTESIAN_POINT ( 'NONE',  ( -9.500000000000005329, -5.000000000000000000, -52.94236561372726868 ) ) ;
#77194=CARTESIAN_POINT ( 'NONE',  ( -19.22370335506887429, 49.79722359267143617, 61.51281625664049102 ) ) ;
#77195=CARTESIAN_POINT ( 'NONE',  ( -7.409230666798462650, 40.77747091125806378, -58.95054567335854756 ) ) ;
#77196=CARTESIAN_POINT ( 'NONE',  ( 6.057904175366206623, 41.61856606260997893, -70.65344123640606711 ) ) ;
#77207=ORIENTED_EDGE ( 'NONE', *, *, #13899, .F. ) ;
#77236=CARTESIAN_POINT ( 'NONE',  ( 30.95568101991391430, 18.64284798592769476, 22.77427805268053262 ) ) ;
#77241=EDGE_CURVE ( 'NONE', #59690, #101469, #13646, .T. ) ;
#77246=CARTESIAN_POINT ( 'NONE',  ( 0.000000000000000000, -5.000000000000000000, 10.00000000000000000 ) ) ;
#77264=UNCERTAINTY_MEASURE_WITH_UNIT (LENGTH_MEASURE( 1.000000000000000082E-05 ), #2316, 'distance_accuracy_value', 'NONE');
#77283=CARTESIAN_POINT ( 'NONE',  ( -72.41885610115939187, 42.00000000000000000, 55.65414010178468374 ) ) ;
#77291=CARTESIAN_POINT ( 'NONE',  ( -49.76137878681610260, 40.83833847419749219, 41.92585938202696383 ) ) ;
#77307=CARTESIAN_POINT ( 'NONE',  ( -3.140974613990812792, 50.00000000000000000, -73.31232788067644890 ) ) ;
#77322=CARTESIAN_POINT ( 'NONE',  ( 6.701893401236465486, 41.44328394225253476, -70.59544911815949320 ) ) ;
#77325=CARTESIAN_POINT ( 'NONE',  ( -9.500000000000007105, -5.000000000000000000, -68.91429205785459544 ) ) ;
#77335=CARTESIAN_POINT ( 'NONE',  ( -4.933292134499193793, 41.54835750584372533, -70.57172791559196412 ) ) ;
#77355=ORIENTED_EDGE ( 'NONE', *, *, #32925, .T. ) ;
#77364=CARTESIAN_POINT ( 'NONE',  ( -18.10430355215808973, 43.96790572561079102, -85.61069757033331484 ) ) ;
#77387=CARTESIAN_POINT ( 'NONE',  ( -13.75294187979978666, -4.333298119783973945, -11.48770422822915727 ) ) ;
#77390=CARTESIAN_POINT ( 'NONE',  ( 2.617478843592800697, 48.00000000000000711, -75.26027323331685182 ) ) ;
#77391=COLOUR_RGB ( '', 0.08235294, 0.09019608, 0.10196078) ;
#77401=CARTESIAN_POINT ( 'NONE',  ( -7.099152841014172211, 41.70084716954765724, -59.82719248405098256 ) ) ;
#77411=CARTESIAN_POINT ( 'NONE',  ( 17.50213914152930883, 50.00000000000000000, 63.56338360167926282 ) ) ;
#77435=CARTESIAN_POINT ( 'NONE',  ( 7.125691916903466705, 41.67430808309654822, -69.26730091920677523 ) ) ;
#77437=CARTESIAN_POINT ( 'NONE',  ( -63.03617022294436367, 49.99999999995993250, -16.93907820454377244 ) ) ;
#77460=CARTESIAN_POINT ( 'NONE',  ( 18.91791044776121211, 46.94999999999998153, 62.18611311450882795 ) ) ;
#77473=SURFACE_SIDE_STYLE ('',( #20355 ) ) ;
#77478=CARTESIAN_POINT ( 'NONE',  ( 50.94745919686199898, 50.00000000000000000, -37.05882352941176805 ) ) ;
#77479=COLOUR_RGB ( '', 0.08235294, 0.09019608, 0.10196078) ;
#77481=CARTESIAN_POINT ( 'NONE',  ( -7.374560640982810611, 50.00000000000000000, -75.40399789251387119 ) ) ;
#77513=CARTESIAN_POINT ( 'NONE',  ( -7.036764705886677795, 40.29466777512107001, -71.06385277390548083 ) ) ;
#77528=VERTEX_POINT ( 'NONE', #82257 ) ;
#77534=EDGE_CURVE ( 'NONE', #10685, #78701, #84206, .T. ) ;
#77545=CARTESIAN_POINT ( 'NONE',  ( 1.590636543732056207, 50.00000000000000711, -97.00013170160131892 ) ) ;
#77561=CARTESIAN_POINT ( 'NONE',  ( -5.977866729378733091, 41.99823429243535600, -69.20734196604240651 ) ) ;
#77566=CARTESIAN_POINT ( 'NONE',  ( 8.012433108796550130, -5.000000000000000000, 14.34039711613852575 ) ) ;
#77567=CARTESIAN_POINT ( 'NONE',  ( -13.14242568365673414, 42.00000000000000000, -92.43215185528094935 ) ) ;
#77586=CARTESIAN_POINT ( 'NONE',  ( 30.67950393662592745, 18.64316884711713485, 23.57730434126678887 ) ) ;
#77601=CARTESIAN_POINT ( 'NONE',  ( -17.49999999999997513, 50.00000000000000000, -500000.0000000000582 ) ) ;
#77611=( BOUNDED_SURFACE ( )  B_SPLINE_SURFACE ( 2, 3, ( 
 ( #47817, #47296, #46254, #62972 ),
 ( #79140, #80193, #39237, #72111 ),
 ( #62445, #29061, #53801, #105020 ) ),
 .UNSPECIFIED., .F., .F., .F. ) 
 B_SPLINE_SURFACE_WITH_KNOTS ( ( 3, 3 ),
 ( 4, 4 ),
 ( 0.000000000000000000, 1.000000000000000000 ),
 ( 5.953728167561664009, 6.612642446797508455 ),
 .UNSPECIFIED. ) 
 GEOMETRIC_REPRESENTATION_ITEM ( )  RATIONAL_B_SPLINE_SURFACE ( (
 ( 1.000000000000000000, 1.000000000000000000, 1.000000000000000000, 1.000000000000000000),
 ( 1.857142857142858317, 1.857142857142858317, 1.857142857142858317, 1.857142857142858317),
 ( 1.000000000000000000, 1.000000000000000000, 1.000000000000000000, 1.000000000000000000) ) ) 
 REPRESENTATION_ITEM ( '' )  SURFACE ( )  );
#77614=CARTESIAN_POINT ( 'NONE',  ( 7.500000000000005329, 40.00000000029777425, -69.29143158580563977 ) ) ;
#77632=CARTESIAN_POINT ( 'NONE',  ( -12.12626197892902269, -5.000000000002062350, -94.24800833403607214 ) ) ;
#77656=CARTESIAN_POINT ( 'NONE',  ( -17.49999999999997158, 51.95328275803299789, 61.04403218099716355 ) ) ;
#77667=FILL_AREA_STYLE_COLOUR ( '', #78946 ) ;
#77675=CARTESIAN_POINT ( 'NONE',  ( 1.797870618340624782, 41.33266196706066609, -58.72278032361231936 ) ) ;
#77686=CARTESIAN_POINT ( 'NONE',  ( -16.64670748671521494, -5.000000000000000000, -1.019662339604523460 ) ) ;
#77707=CARTESIAN_POINT ( 'NONE',  ( 9.500000025475724641, -4.999999999999998224, -69.85526497429231085 ) ) ;
#77734=CARTESIAN_POINT ( 'NONE',  ( -18.91765097186078748, 48.32803790483924899, 62.18241277266358935 ) ) ;
#77736=CARTESIAN_POINT ( 'NONE',  ( 6.422424208505636223, 41.30029441423581460, -70.89074253712280438 ) ) ;
#77737=ADVANCED_FACE ( 'NONE', ( #20781 ), #60674, .F. ) ;
#77748=CARTESIAN_POINT ( 'NONE',  ( 5.183352296222792255, 2.622636543482688154, -23.48691144851825996 ) ) ;
#77749=CARTESIAN_POINT ( 'NONE',  ( 12.48579759839974734, -3.547635786644434575, -13.69895377872215114 ) ) ;
#77753=CARTESIAN_POINT ( 'NONE',  ( 9.596002107491598210, -5.000000000000002665, -92.37456064098007857 ) ) ;
#77763=SURFACE_STYLE_FILL_AREA ( #85876 ) ;
#77781=CARTESIAN_POINT ( 'NONE',  ( 6.061707334725029206, -5.000000000000000000, -95.47772246152658226 ) ) ;
#77805=CARTESIAN_POINT ( 'NONE',  ( 49.07844914649123069, 40.91359446734409744, -43.02828753854897315 ) ) ;
#77817=CARTESIAN_POINT ( 'NONE',  ( 37.36680950585426331, 18.64316884707256605, -10.04205104291870398 ) ) ;
#77825=CARTESIAN_POINT ( 'NONE',  ( 56.10245818848532195, 40.83957962279791332, -33.37187160345136050 ) ) ;
#77833=ORIENTED_EDGE ( 'NONE', *, *, #34685, .T. ) ;
#77840=CARTESIAN_POINT ( 'NONE',  ( 1.570796324976846403, 50.00000000000000000, -73.00000000000001421 ) ) ;
#77856=FILL_AREA_STYLE ('',( #63275 ) ) ;
#77869=CARTESIAN_POINT ( 'NONE',  ( -7.036764705886677795, 40.29466777512107001, -71.06385277390548083 ) ) ;
#77881=CARTESIAN_POINT ( 'NONE',  ( -17.78094014186206095, 45.00000000000000000, 62.75731298173543848 ) ) ;
#77908=B_SPLINE_CURVE_WITH_KNOTS ( 'NONE', 3,
 ( #99010, #66670, #23047, #3539, #27326, #67215, #100089, #51541, #50994, #10547, #44535, #52070 ),
 .UNSPECIFIED., .F., .F.,
 ( 4, 2, 2, 2, 2, 4 ),
 ( 0.000000000000000000, 0.2500336435762632314, 0.5000829980240025785, 0.7501323524717418145, 0.8751570296956115991, 1.000000000000000000 ),
 .UNSPECIFIED. ) ;
#77909=CARTESIAN_POINT ( 'NONE',  ( 5.121894999926677627, -2.681690743133432697, -18.64842307824732970 ) ) ;
#77914=CARTESIAN_POINT ( 'NONE',  ( 11.35794436181222089, -4.958956545026470764, -12.57307762860520661 ) ) ;
#77922=CARTESIAN_POINT ( 'NONE',  ( -12.49955057333833253, -4.332870170146376765, -12.71907580221295220 ) ) ;
#77924=CARTESIAN_POINT ( 'NONE',  ( 5.036189803708992052, 48.00000000000000711, -76.26213611645744095 ) ) ;
#77931=PRESENTATION_STYLE_ASSIGNMENT (( #44507 ) ) ;
#77937=CARTESIAN_POINT ( 'NONE',  ( -5.711455862418337581, 41.98245415718732687, -59.41190564724043099 ) ) ;
#77954=CARTESIAN_POINT ( 'NONE',  ( 19.50011280463133545, 50.00000000000000000, 59.90639435984937222 ) ) ;
#77964=CARTESIAN_POINT ( 'NONE',  ( 6.195804100829465533, 41.59435685053999521, -70.65487364791140124 ) ) ;
#77988=CARTESIAN_POINT ( 'NONE',  ( 40.91302753174524298, 39.68470576882931056, -51.74909898369087813 ) ) ;
#77998=CARTESIAN_POINT ( 'NONE',  ( 31.55411176397327466, 43.06427903709310812, -67.12026830634881946 ) ) ;
#78004=CARTESIAN_POINT ( 'NONE',  ( 6.145467200820246667, 48.00000000000000000, -77.00333157708931253 ) ) ;
#78032=CARTESIAN_POINT ( 'NONE',  ( -5.266678742591862417, 13.24337579848477375, -33.12418987319537678 ) ) ;
#78047=SURFACE_STYLE_USAGE ( .BOTH. , #53248 ) ;
#78064=LINE ( 'NONE', #5762, #44263 ) ;
#78083=CARTESIAN_POINT ( 'NONE',  ( -5.652563880857838896, 41.79847487344755308, -70.46163212616390581 ) ) ;
#78088=CARTESIAN_POINT ( 'NONE',  ( -6.568714509987131578, 41.61374477456796939, -58.74117337121824534 ) ) ;
#78094=VERTEX_POINT ( 'NONE', #20657 ) ;
#78105=CARTESIAN_POINT ( 'NONE',  ( 6.831363830528337289, 41.73171983268897378, -59.17722554277374059 ) ) ;
#78106=CARTESIAN_POINT ( 'NONE',  ( -47.37019975542479955, 42.00000000008224532, -36.40416150956886554 ) ) ;
#78128=CYLINDRICAL_SURFACE ( 'NONE', #15427, 60.00000000000000000 ) ;
#78134=CARTESIAN_POINT ( 'NONE',  ( 7.493949260784499522, 40.57568730855774675, -68.91429205858018747 ) ) ;
#78140=CARTESIAN_POINT ( 'NONE',  ( -11.17909359580129980, -4.978490734260999417, -77.11252404933959781 ) ) ;
#78154=CARTESIAN_POINT ( 'NONE',  ( -5.499265899522562506, -4.999999999985523580, -99.22427370007513048 ) ) ;
#78186=ORIENTED_EDGE ( 'NONE', *, *, #102106, .T. ) ;
#78204=CARTESIAN_POINT ( 'NONE',  ( 14.24124568368486088, -4.332661967059059371, -11.33228852115809637 ) ) ;
#78227=CARTESIAN_POINT ( 'NONE',  ( 19.49770126386425773, 49.99985876156954134, 59.97225932440124296 ) ) ;
#78235=( BOUNDED_CURVE ( )  B_SPLINE_CURVE ( 2, ( #9918, #728, #41758 ),
 .UNSPECIFIED., .F., .F. ) 
 B_SPLINE_CURVE_WITH_KNOTS ( ( 3, 3 ),
 ( 0.000000000000000000, 1.000000000000000000 ),
 .UNSPECIFIED. ) 
 CURVE ( )  GEOMETRIC_REPRESENTATION_ITEM ( )  RATIONAL_B_SPLINE_CURVE ( ( 1.000000000000000000, 1.428571428571427271, 1.428571428571429269 ) ) 
 REPRESENTATION_ITEM ( '' )  );
#78239=CARTESIAN_POINT ( 'NONE',  ( -7.500000000000001776, -4.015205788346293048, -20.09376801818934766 ) ) ;
#78251=CARTESIAN_POINT ( 'NONE',  ( -19.04051945834135040, 49.58720281916519212, 61.84160661372276024 ) ) ;
#78252=FACE_OUTER_BOUND ( 'NONE', #91426, .T. ) ;
#78253=CARTESIAN_POINT ( 'NONE',  ( 6.406311604196643472, 41.42610738297985762, -70.78720126776296695 ) ) ;
#78267=CARTESIAN_POINT ( 'NONE',  ( 5.221816652746770870, 7.032134607704920271, -27.49812609708854794 ) ) ;
#78269=CARTESIAN_POINT ( 'NONE',  ( -2.093983074874240291, -3.000000000000000444, -7.791781413346525298 ) ) ;
#78272=CARTESIAN_POINT ( 'NONE',  ( -7.996668422917848851, -4.999999999991826094, -91.14546720082944375 ) ) ;
#78321=CARTESIAN_POINT ( 'NONE',  ( 39.10169391268793504, 42.03037277983941067, -56.74405835323407388 ) ) ;
#78332=CARTESIAN_POINT ( 'NONE',  ( 36.40416150955762475, 42.00000000000001421, -47.37019975555940476 ) ) ;
#78339=CARTESIAN_POINT ( 'NONE',  ( 58.89336504995121402, 39.42406911483853804, -28.14246176607905525 ) ) ;
#78341=ORIENTED_EDGE ( 'NONE', *, *, #94786, .T. ) ;
#78355=CARTESIAN_POINT ( 'NONE',  ( -7.996668422912395435, 49.99999999999999289, -78.85453279917057046 ) ) ;
#78362=VERTEX_POINT ( 'NONE', #89044 ) ;
#78368=VERTEX_POINT ( 'NONE', #4949 ) ;
#78369=EDGE_CURVE ( 'NONE', #78737, #64826, #106345, .T. ) ;
#78373=CARTESIAN_POINT ( 'NONE',  ( -5.500000000000007105, 42.00000000000000000, -65.90297133655424489 ) ) ;
#78374=CARTESIAN_POINT ( 'NONE',  ( -12.50000000000000355, -3.000000000000001776, -76.70872284621019332 ) ) ;
#78379=VECTOR ( 'NONE', #61903, 1000.000000000000000 ) ;
#78387=CARTESIAN_POINT ( 'NONE',  ( -6.188824320863258954, 41.46400361745708807, -70.81766458224430494 ) ) ;
#78389=EDGE_LOOP ( 'NONE', ( #66654, #52242, #20863, #96007, #10135, #5780 ) ) ;
#78410=CARTESIAN_POINT ( 'NONE',  ( -12.50000000000000533, 27.17581705516544233, -44.71521942845799202 ) ) ;
#78414=ORIENTED_EDGE ( 'NONE', *, *, #24131, .T. ) ;
#78422=CARTESIAN_POINT ( 'NONE',  ( 7.500000000000000000, -2.376982511157178735, -18.31627213068316351 ) ) ;
#78435=B_SPLINE_CURVE_WITH_KNOTS ( 'NONE', 3,
 ( #102150, #19693, #53600, #52528 ),
 .UNSPECIFIED., .F., .F.,
 ( 4, 4 ),
 ( 0.000000000000000000, 1.000000000000000000 ),
 .UNSPECIFIED. ) ;
#78452=CARTESIAN_POINT ( 'NONE',  ( 23.38163988262877879, 50.00000000002003731, 60.94087333794557537 ) ) ;
#78454=ORIENTED_EDGE ( 'NONE', *, *, #94247, .F. ) ;
#78459=CARTESIAN_POINT ( 'NONE',  ( -5.441822498209519132, 41.96569345422851427, -59.31342656602353003 ) ) ;
#78467=CARTESIAN_POINT ( 'NONE',  ( 19.15405721169568309, 50.00000000000001421, 60.37683062052576588 ) ) ;
#78476=CARTESIAN_POINT ( 'NONE',  ( 62.09765651784079665, 49.99999999999999289, -11.13245139057254107 ) ) ;
#78485=CARTESIAN_POINT ( 'NONE',  ( 6.441910988235199476, 41.95837105961398095, -69.50559658456835166 ) ) ;
#78496=UNCERTAINTY_MEASURE_WITH_UNIT (LENGTH_MEASURE( 1.000000000000000082E-05 ), #97084, 'distance_accuracy_value', 'NONE');
#78505=( GEOMETRIC_REPRESENTATION_CONTEXT ( 3 ) GLOBAL_UNCERTAINTY_ASSIGNED_CONTEXT ( ( #100093 ) ) GLOBAL_UNIT_ASSIGNED_CONTEXT ( ( #39456, #22224, #14079 ) ) REPRESENTATION_CONTEXT ( 'NONE', 'WORKASPACE' ) );
#78521=PRESENTATION_STYLE_ASSIGNMENT (( #44044 ) ) ;
#78554=CARTESIAN_POINT ( 'NONE',  ( -5.280320895393596281, 15.76435391921249263, -35.40122979677870063 ) ) ;
#78581=( NAMED_UNIT ( * ) SI_UNIT ( $, .STERADIAN. ) SOLID_ANGLE_UNIT ( ) );
#78584=COLOUR_RGB ( '', 0.40784314, 0.44705882, 0.49803922) ;
#78588=CARTESIAN_POINT ( 'NONE',  ( 7.360624614871775329, 50.00000000000001421, -75.38987561219505551 ) ) ;
#78607=CARTESIAN_POINT ( 'NONE',  ( -5.898965146263452475, 41.68848200487053646, -58.70906998136139521 ) ) ;
#78619=EDGE_LOOP ( 'NONE', ( #54464, #96722, #106510, #78454 ) ) ;
#78623=CARTESIAN_POINT ( 'NONE',  ( -10.04205104296119622, 18.64316884715858080, 37.36680950591986772 ) ) ;
#78635=EDGE_LOOP ( 'NONE', ( #94395, #48987, #59288, #39795 ) ) ;
#78636=SURFACE_STYLE_USAGE ( .BOTH. , #52783 ) ;
#78654=CARTESIAN_POINT ( 'NONE',  ( -11.72777639069216526, -4.888764693000935857, -76.94183081657440937 ) ) ;
#78669=ADVANCED_FACE ( 'NONE', ( #4282 ), #25948, .T. ) ;
#78671=COLOUR_RGB ( '', 0.72549020, 0.75294118, 0.79215686) ;
#78700=( LENGTH_UNIT ( ) NAMED_UNIT ( * ) SI_UNIT ( .MILLI., .METRE. ) );
#78701=VERTEX_POINT ( 'NONE', #47903 ) ;
#78718=CARTESIAN_POINT ( 'NONE',  ( 16.28378713908861997, -4.332661967062005459, -8.128475758628217918 ) ) ;
#78721=ORIENTED_EDGE ( 'NONE', *, *, #105959, .T. ) ;
#78737=VERTEX_POINT ( 'NONE', #89975 ) ;
#78744=CARTESIAN_POINT ( 'NONE',  ( 19.31802113242206786, 49.87598122772962483, 61.28462200380675995 ) ) ;
#78770=CARTESIAN_POINT ( 'NONE',  ( -19.00015996940621932, 49.50625549542287018, 61.91457260680915198 ) ) ;
#78772=CARTESIAN_POINT ( 'NONE',  ( 6.097211899678556257, 40.29241764280718030, -71.16079434776209212 ) ) ;
#78775=CARTESIAN_POINT ( 'NONE',  ( 12.50000000000000711, -4.999999999999999112, -55.73109925765189843 ) ) ;
#78792=CARTESIAN_POINT ( 'NONE',  ( -6.043427762771337086, -5.000000000000002665, -74.51456333905269958 ) ) ;
#78808=CARTESIAN_POINT ( 'NONE',  ( -12.50000000000000355, 41.59226156894883530, -76.70843802411151557 ) ) ;
#78817=CARTESIAN_POINT ( 'NONE',  ( 7.412969500702210723, 41.14559805159964156, -68.91429205978418793 ) ) ;
#78823=CARTESIAN_POINT ( 'NONE',  ( 1.308371270545586329, -5.000000000000000888, -9.999872502480485537 ) ) ;
#78830=( NAMED_UNIT ( * ) SI_UNIT ( $, .STERADIAN. ) SOLID_ANGLE_UNIT ( ) );
#78836=CARTESIAN_POINT ( 'NONE',  ( 12.13034742782428133, 49.99999999999999289, -93.82352941176471006 ) ) ;
#78841=CARTESIAN_POINT ( 'NONE',  ( -42.32873853761031313, 39.51951600909762163, -49.85685020764661601 ) ) ;
#78846=FACE_OUTER_BOUND ( 'NONE', #44358, .T. ) ;
#78861=CARTESIAN_POINT ( 'NONE',  ( 33.52312678242137167, 18.64316884714798306, 19.32152200346563120 ) ) ;
#78869=CARTESIAN_POINT ( 'NONE',  ( 11.87333998996387230, 39.42593707198930986, 63.97654705930002450 ) ) ;
#78895=AXIS2_PLACEMENT_3D ( 'NONE', #67348, #52740, #101307 ) ;
#78901=DIRECTION ( 'NONE',  ( 0.000000000000000000, 0.000000000000000000, 1.000000000000000000 ) ) ;
#78907=SURFACE_STYLE_USAGE ( .BOTH. , #61700 ) ;
#78908=( NAMED_UNIT ( * ) PLANE_ANGLE_UNIT ( ) SI_UNIT ( $, .RADIAN. ) );
#78911=ORIENTED_EDGE ( 'NONE', *, *, #46736, .F. ) ;
#78915=CARTESIAN_POINT ( 'NONE',  ( -7.004291982367331748, 40.56179000230169862, -71.01843131766943884 ) ) ;
#78917=ORIENTED_EDGE ( 'NONE', *, *, #35018, .T. ) ;
#78919=VECTOR ( 'NONE', #2026, 1000.000000000000000 ) ;
#78933=MECHANICAL_DESIGN_GEOMETRIC_PRESENTATION_REPRESENTATION('',(#72070),#92706);
#78941=CARTESIAN_POINT ( 'NONE',  ( -12.50000000000000888, 38.67421576088683821, -61.60810543285763430 ) ) ;
#78946=COLOUR_RGB ( '', 0.66274510, 0.83137255, 0.94901961) ;
#78950=CARTESIAN_POINT ( 'NONE',  ( 7.384655732054108412, 41.09429998108713988, -59.07190378971382927 ) ) ;
#78957=CARTESIAN_POINT ( 'NONE',  ( 7.500000000000007105, 42.86855997971688481, -62.45407030448338048 ) ) ;
#78966=CARTESIAN_POINT ( 'NONE',  ( 7.500000000000007105, 42.00000000000000711, -70.16688272716297092 ) ) ;
#78968=ORIENTED_EDGE ( 'NONE', *, *, #68341, .F. ) ;
#78970=CARTESIAN_POINT ( 'NONE',  ( -16.50306599549761444, -4.333298119783954405, -6.982805419935155022 ) ) ;
#78982=CARTESIAN_POINT ( 'NONE',  ( -63.03617022295203753, 48.00000000000000000, -16.93907820454660396 ) ) ;
#78987=CARTESIAN_POINT ( 'NONE',  ( -6.847405770342755993, 41.77151253865379488, -59.31773377044793705 ) ) ;
#78989=CARTESIAN_POINT ( 'NONE',  ( 12.49723740359450730, -3.303264067465667697, -76.71011700628446306 ) ) ;
#79002=( GEOMETRIC_REPRESENTATION_CONTEXT ( 3 ) GLOBAL_UNCERTAINTY_ASSIGNED_CONTEXT ( ( #42954 ) ) GLOBAL_UNIT_ASSIGNED_CONTEXT ( ( #82482, #18303, #9635 ) ) REPRESENTATION_CONTEXT ( 'NONE', 'WORKASPACE' ) );
#79011=( NAMED_UNIT ( * ) SI_UNIT ( $, .STERADIAN. ) SOLID_ANGLE_UNIT ( ) );
#79067=ORIENTED_EDGE ( 'NONE', *, *, #60913, .T. ) ;
#79069=FILL_AREA_STYLE ('',( #69920 ) ) ;
#79075=EDGE_CURVE ( 'NONE', #36, #52979, #58611, .T. ) ;
#79106=CARTESIAN_POINT ( 'NONE',  ( -17.49999999999997513, 50.00000000000000000, 63.82142195434425958 ) ) ;
#79130=CARTESIAN_POINT ( 'NONE',  ( -10.50000000000000533, -5.000000000000000000, -55.73109922010478812 ) ) ;
#79140=CARTESIAN_POINT ( 'NONE',  ( -4.852941176470599416, -5.000000000000002665, -70.80672828634229177 ) ) ;
#79141=CARTESIAN_POINT ( 'NONE',  ( -5.342383608296940700, 41.79455473986575242, -70.44171442173730213 ) ) ;
#79147=CARTESIAN_POINT ( 'NONE',  ( -5.971402860190597295, 41.34845723532072270, -58.36201413431516727 ) ) ;
#79164=CARTESIAN_POINT ( 'NONE',  ( 57.69562748396144514, 41.99999999999999289, 15.50526908259264225 ) ) ;
#79167=B_SPLINE_SURFACE_WITH_KNOTS ( 'NONE', 3, 3, ( 
 ( #40573, #65386, #105831, #81017, #97730, #56740, #65912, #15764 ),
 ( #75, #57267, #16292, #49177, #98792, #8200, #48645, #41111 ),
 ( #26562, #75596, #36252, #27626, #2762, #60507, #58902, #59434 ),
 ( #100930, #85286, #18451, #17913, #76651, #99871, #26043, #91792 ),
 ( #51846, #67520, #69121, #50766, #10840, #83675, #19538, #1695 ),
 ( #9784, #42700, #92297, #11374, #35713, #93392, #51305, #34651 ),
 ( #84758, #2219, #43238, #100400, #84227, #52375, #44301, #68036 ),
 ( #35169, #10322, #43759, #77195, #59977, #92838, #76123, #27091 ) ),
 .UNSPECIFIED., .F., .F., .F.,
 ( 4, 2, 2, 4 ),
 ( 4, 2, 2, 4 ),
 ( 0.000000000000000000, 0.2500000000000000000, 0.5000000000000000000, 1.000000000000000000 ),
 ( 0.000000000000000000, 0.2500000000000000000, 0.5000000000000000000, 1.000000000000000000 ),
 .UNSPECIFIED. ) ;
#79171=B_SPLINE_CURVE_WITH_KNOTS ( 'NONE', 3,
 ( #42481, #24733, #74313, #66224, #50039, #91585, #7441, #17694, #25271, #75377, #74835, #57583, #50554 ),
 .UNSPECIFIED., .F., .F.,
 ( 4, 1, 1, 1, 1, 1, 2, 2, 4 ),
 ( 0.000000000000000000, 0.2499999999999372724, 0.3749999999999085731, 0.4374999999998958611, 0.4687499999998881450, 0.4843749999998855360, 0.4921874999998830380, 0.4999999999998806510, 1.000000000000000000 ),
 .UNSPECIFIED. ) ;
#79184=PRESENTATION_STYLE_ASSIGNMENT (( #78636 ) ) ;
#79228=SURFACE_SIDE_STYLE ('',( #54937 ) ) ;
#79286=CARTESIAN_POINT ( 'NONE',  ( 19.46591973412748189, 49.98735554868721920, 60.46518678595987950 ) ) ;
#79310=SURFACE_SIDE_STYLE ('',( #14030 ) ) ;
#79327=CARTESIAN_POINT ( 'NONE',  ( 5.221736196116609108, 7.022645827047127476, -27.48951043644760261 ) ) ;
#79331=CARTESIAN_POINT ( 'NONE',  ( -8.737863884125482983, -4.999999999994546585, -90.03618980230058355 ) ) ;
#79332=STYLED_ITEM ( 'NONE', ( #54502 ), #73129 ) ;
#79333=( LENGTH_UNIT ( ) NAMED_UNIT ( * ) SI_UNIT ( .MILLI., .METRE. ) );
#79361=CARTESIAN_POINT ( 'NONE',  ( -1.797870618176258484, 41.33266196706050977, -58.72278032362692102 ) ) ;
#79363=EDGE_CURVE ( 'NONE', #38992, #54340, #75934, .T. ) ;
#79364=CARTESIAN_POINT ( 'NONE',  ( -7.500000000000003553, -2.999999999999999112, -68.91429205785459544 ) ) ;
#79380=( LENGTH_UNIT ( ) NAMED_UNIT ( * ) SI_UNIT ( .MILLI., .METRE. ) );
#79383=CARTESIAN_POINT ( 'NONE',  ( 34.57001659430475371, 42.66264814753424872, -62.97408465421569446 ) ) ;
#79387=CARTESIAN_POINT ( 'NONE',  ( 5.500000000000641265, 42.00000000000000000, -59.88032989331720302 ) ) ;
#79396=CARTESIAN_POINT ( 'NONE',  ( 29.83308852632731245, 41.99999999995888089, 51.76085035125569789 ) ) ;
#79403=CARTESIAN_POINT ( 'NONE',  ( -65.06413854203213987, 39.42447728981473176, 0.8157412600678713988 ) ) ;
#79420=CARTESIAN_POINT ( 'NONE',  ( 7.996668422916345165, 49.99999999999455014, -91.14546720080639375 ) ) ;
#79427=SURFACE_STYLE_USAGE ( .BOTH. , #14671 ) ;
#79435=CARTESIAN_POINT ( 'NONE',  ( 8.901296169213878784, -5.000000000000000000, -17.06178707270185058 ) ) ;
#79439=CARTESIAN_POINT ( 'NONE',  ( -7.500000000055414340, -4.999999999944586548, -36.97043916959988508 ) ) ;
#79470=CARTESIAN_POINT ( 'NONE',  ( -12.50000000000000533, 34.72467956601219186, -53.96055213376253334 ) ) ;
#79482=CARTESIAN_POINT ( 'NONE',  ( 7.311443158282724397, 40.96482056676212125, -58.73188698012794617 ) ) ;
#79490=CARTESIAN_POINT ( 'NONE',  ( 7.500000000000000000, -6.192646671729328922, -14.54134196042664229 ) ) ;
#79510=CARTESIAN_POINT ( 'NONE',  ( 63.03617022303986772, 40.83906611471739012, -16.93907820431003586 ) ) ;
#79514=CARTESIAN_POINT ( 'NONE',  ( -63.03617022294436367, 49.99999999995993250, -16.93907820454377244 ) ) ;
#79536=SURFACE_SIDE_STYLE ('',( #94135 ) ) ;
#79550=CARTESIAN_POINT ( 'NONE',  ( 6.645514545840788934, 41.91298724924220664, -59.84148600294046361 ) ) ;
#79552=CARTESIAN_POINT ( 'NONE',  ( 17.50000000000002842, 50.00000000000000000, -500000.0000000000582 ) ) ;
#79565=CARTESIAN_POINT ( 'NONE',  ( 7.461258573462377974, 40.57432690845221401, -59.19360968028617975 ) ) ;
#79591=CARTESIAN_POINT ( 'NONE',  ( 8.737863884120029567, 49.99999999999999289, -79.96381019768851672 ) ) ;
#79609=CARTESIAN_POINT ( 'NONE',  ( 2.094395098902538610, -4.999999999999998224, -8.000000000000000000 ) ) ;
#79611=CARTESIAN_POINT ( 'NONE',  ( -5.075741750048029743, -4.332638003024074536, -17.09621982684887698 ) ) ;
#79626=CARTESIAN_POINT ( 'NONE',  ( -17.92908368763044891, 41.95109109384650736, -82.51357555118542564 ) ) ;
#79628=CARTESIAN_POINT ( 'NONE',  ( -19.17276608133135696, 49.99999999999999289, 60.35151560209396848 ) ) ;
#79631=CARTESIAN_POINT ( 'NONE',  ( -17.49999999999998579, 50.79875088428568120, 63.37001662960430082 ) ) ;
#79636=CARTESIAN_POINT ( 'NONE',  ( 17.50000000000002842, 48.58944628578559133, 64.09148194233368656 ) ) ;
#79672=( NAMED_UNIT ( * ) SI_UNIT ( $, .STERADIAN. ) SOLID_ANGLE_UNIT ( ) );
#79677=CARTESIAN_POINT ( 'NONE',  ( -10.73749782760683225, -5.000000000000000888, 12.43190307932432148 ) ) ;
#79743=DIRECTION ( 'NONE',  ( 0.000000000000000000, 1.000000000000000000, 0.000000000000000000 ) ) ;
#79747=CARTESIAN_POINT ( 'NONE',  ( 17.59386865953261392, -4.333298119783753677, 3.400962272007458598 ) ) ;
#79750=CARTESIAN_POINT ( 'NONE',  ( -5.219866590715411370, -5.000000000000000000, -8.922269033013266792 ) ) ;
#79779=FACE_OUTER_BOUND ( 'NONE', #2599, .T. ) ;
#79801=CARTESIAN_POINT ( 'NONE',  ( -65.02775738911799408, 48.00000000000000711, -4.794983377755789533 ) ) ;
#79809=CARTESIAN_POINT ( 'NONE',  ( -12.34835181856066555, -4.332967528434497062, -12.86601580078907148 ) ) ;
#79833=CARTESIAN_POINT ( 'NONE',  ( -19.44215914665673495, 49.97163196006100350, 60.69499804416638966 ) ) ;
#79840=( NAMED_UNIT ( * ) PLANE_ANGLE_UNIT ( ) SI_UNIT ( $, .RADIAN. ) );
#79856=CARTESIAN_POINT ( 'NONE',  ( -9.999999999999996447, -5.000000000000002665, -86.30899693747676338 ) ) ;
#79857=FACE_OUTER_BOUND ( 'NONE', #64784, .T. ) ;
#79865=CARTESIAN_POINT ( 'NONE',  ( 5.079306836895828070, -4.308466644845876381, -17.11871833148104471 ) ) ;
#79867=CARTESIAN_POINT ( 'NONE',  ( -33.84683838397652522, 42.75782337701531333, -63.96829032114721514 ) ) ;
#79870=ORIENTED_EDGE ( 'NONE', *, *, #10691, .F. ) ;
#79881=CARTESIAN_POINT ( 'NONE',  ( -55.22048556067662162, 40.83906611472863801, 34.80214219330362369 ) ) ;
#79884=CARTESIAN_POINT ( 'NONE',  ( -18.91772294110159081, 48.25776538900139911, 62.18609455222676274 ) ) ;
#79908=CARTESIAN_POINT ( 'NONE',  ( 34.55448620566968287, 42.66471839012794476, -62.99543540866341118 ) ) ;
#79925=CARTESIAN_POINT ( 'NONE',  ( -49.76159010805244520, 39.42507290984417523, 41.92561844419851980 ) ) ;
#79942=CARTESIAN_POINT ( 'NONE',  ( -9.999999999999996447, 48.00000000000000000, -83.69100306252323662 ) ) ;
#79943=DIRECTION ( 'NONE',  ( 0.000000000000000000, -0.000000000000000000, 1.000000000000000000 ) ) ;
#79957=CARTESIAN_POINT ( 'NONE',  ( 4.651269564039822946, -4.999999999999991118, -15.66707428873065311 ) ) ;
#79963=B_SPLINE_CURVE_WITH_KNOTS ( 'NONE', 3,
 ( #59554, #92422, #723, #91906, #42283, #33691, #66034, #66565, #1268, #83803, #25071, #57929, #90849, #10446, #75718, #34234, #67106, #49843 ),
 .UNSPECIFIED., .F., .F.,
 ( 4, 2, 2, 2, 2, 2, 2, 2, 4 ),
 ( 0.5000000000000000000, 0.5625000000000000000, 0.6250000000000000000, 0.6875000000000000000, 0.7500000000000000000, 0.8125000000000000000, 0.8750000000000001110, 0.9375000000000000000, 1.000000000000000000 ),
 .UNSPECIFIED. ) ;
#79993=ORIENTED_EDGE ( 'NONE', *, *, #39491, .F. ) ;
#79994=CARTESIAN_POINT ( 'NONE',  ( -12.50000000000000178, 39.23410961838661137, -63.25741677043061628 ) ) ;
#80010=CARTESIAN_POINT ( 'NONE',  ( 7.500000000000007105, 44.29449649216757479, -60.86453129175313137 ) ) ;
#80032=CARTESIAN_POINT ( 'NONE',  ( -28.89099332391479535, 50.00000000002003731, 58.53034795348396813 ) ) ;
#80036=EDGE_CURVE ( 'NONE', #88651, #78362, #65612, .T. ) ;
#80042=LINE ( 'NONE', #6690, #101151 ) ;
#80048=B_SPLINE_CURVE_WITH_KNOTS ( 'NONE', 3,
 ( #93888, #18973, #52350, #78227, #34623, #67493, #76624, #52894, #101450, #85262, #3818, #11345, #44278, #100373, #20045, #44821, #94434, #20594, #86352, #92271, #53938, #79286, #56042, #71191, #5916, #5408, #87923, #86871, #4878, #97056, #103565, #15076, #104086, #31300, #29716, #96545, #45866, #88454, #37277, #78744, #103048, #22677, #29204, #62590, #95474, #38843, #96014, #14529, #47961, #30771, #4342, #38330, #63657, #55514, #105158, #64187, #47438, #88976, #80329, #21619, #23201, #62078, #30226, #70144, #94966, #21105, #70673, #6443, #54449, #54992, #39379, #63112, #22141, #12945, #71706, #37814, #14002, #87402 ),
 .UNSPECIFIED., .F., .F.,
 ( 4, 1, 1, 1, 2, 2, 2, 2, 1, 2, 2, 2, 2, 1, 1, 1, 2, 2, 2, 2, 1, 1, 2, 2, 2, 2, 1, 2, 2, 2, 2, 1, 2, 2, 2, 2, 2, 2, 2, 1, 2, 2, 2, 2, 4 ),
 ( 0.000000000000000000, 0.007812500000051594146, 0.01171875000007735826, 0.01367187500009205137, 0.01464843750009946731, 0.01562500000010688325, 0.02343750000011152884, 0.02734375000011205620, 0.02929687500011102230, 0.03027343750010927023, 0.03125000000010751816, 0.06250000000006696033, 0.09375000000002639555, 0.1093750000000080352, 0.1171874999999988620, 0.1210937499999942824, 0.1230468749999939632, 0.1249999999999936301, 0.1875000000000501543, 0.2187500000000764111, 0.2343750000000898726, 0.2421875000000949796, 0.2460937500000979217, 0.2500000000001008083, 0.3125000000001723066, 0.3437500000002080558, 0.3593750000002235434, 0.3671875000002313150, 0.3750000000002390310, 0.4375000000002702838, 0.4687500000002808309, 0.4843750000002861045, 0.4921875000002899347, 0.5000000000002936540, 0.5625000000002762235, 0.5937500000002652323, 0.6250000000002541301, 0.6875000000002211564, 0.7187500000002028377, 0.7343750000001891820, 0.7421875000001824096, 0.7500000000001757483, 0.8750000000000874856, 0.9375000000000437428, 1.000000000000000000 ),
 .UNSPECIFIED. ) ;
#80054=EDGE_LOOP ( 'NONE', ( #72110, #89626, #63409, #46412, #25688, #59365 ) ) ;
#80076=ORIENTED_EDGE ( 'NONE', *, *, #64377, .F. ) ;
#80088=CARTESIAN_POINT ( 'NONE',  ( 6.645597273868374621, 41.91296976309556044, -68.91429206532015428 ) ) ;
#80097=CARTESIAN_POINT ( 'NONE',  ( -6.062025480882868855, -5.000000000000000000, -74.52240934977429276 ) ) ;
#80102=CARTESIAN_POINT ( 'NONE',  ( -52.56483885390523625, 40.83906611473335602, -38.23529411764706509 ) ) ;
#80114=CARTESIAN_POINT ( 'NONE',  ( 1.224646799147352073E-15, 49.99999999999999289, -75.00000000000001421 ) ) ;
#80135=CARTESIAN_POINT ( 'NONE',  ( 2.094395098902661623, -3.000000000000000000, 8.000000000000000000 ) ) ;
#80142=FILL_AREA_STYLE ('',( #62925 ) ) ;
#80155=CARTESIAN_POINT ( 'NONE',  ( -17.51806903888139644, 50.00000000000000711, 63.24379045937951815 ) ) ;
#80162=VERTEX_POINT ( 'NONE', #56409 ) ;
#80167=EDGE_CURVE ( 'NONE', #51961, #35975, #33201, .T. ) ;
#80181=CARTESIAN_POINT ( 'NONE',  ( 7.150000000000005684, 41.64999999999999147, -68.91429206202190016 ) ) ;
#80193=CARTESIAN_POINT ( 'NONE',  ( -1.724765290377670013, -5.000000000000002665, -69.73714729960835257 ) ) ;
#80218=CARTESIAN_POINT ( 'NONE',  ( 6.583804726435484866, 41.87230891639573116, -59.35876464016742915 ) ) ;
#80224=ORIENTED_EDGE ( 'NONE', *, *, #50497, .F. ) ;
#80269=CARTESIAN_POINT ( 'NONE',  ( 2.094395098902661623, -3.000000000000000000, 8.000000000000000000 ) ) ;
#80329=CARTESIAN_POINT ( 'NONE',  ( 19.02338435704004027, 49.55559105460935854, 61.87204836851903167 ) ) ;
#80354=CARTESIAN_POINT ( 'NONE',  ( -7.048357505843686255, 41.75164249415629314, -68.91429205804081448 ) ) ;
#80382=CARTESIAN_POINT ( 'NONE',  ( -5.036189802309444907, -5.000000000000002665, -76.26213611588271135 ) ) ;
#80393=CARTESIAN_POINT ( 'NONE',  ( 6.793650603637590990, -4.999999999999984901, -15.34177241507032896 ) ) ;
#80411=( BOUNDED_SURFACE ( )  B_SPLINE_SURFACE ( 2, 3, ( 
 ( #79865, #87982, #41010, #72829, #39438, #40472, #14587, #6501, #81444, #48554, #14062, #15136 ),
 ( #98177, #104679, #96070, #39955, #24329, #72313, #73354, #22201, #90090, #31875, #16194, #7039 ),
 ( #64758, #57176, #30830, #97114, #63715, #96604, #73897, #83487, #47497, #97633, #23797, #105218 ),
 ( #63176, #64241, #89565, #23255, #55052, #15661, #80928, #56099, #22735, #46967, #5972, #55574 ),
 ( #106253, #32414, #88511, #80393, #89034, #48018, #51204, #83576, #83063, #58800, #100299, #74424 ) ),
 .UNSPECIFIED., .F., .F., .T. ) 
 B_SPLINE_SURFACE_WITH_KNOTS ( ( 3, 2, 3 ),
 ( 4, 2, 2, 2, 2, 4 ),
 ( -0.01000000000000000021, 0.000000000000000000, 1.000000000000000000 ),
 ( 0.000000000000000000, 0.0009008737055280950992, 0.001801747411056190198, 0.003603494822112380397, 0.005405242233168570595, 0.007206989644224760794 ),
 .UNSPECIFIED. ) 
 GEOMETRIC_REPRESENTATION_ITEM ( )  RATIONAL_B_SPLINE_SURFACE ( (
 ( 1.000000000000000000, 1.000000000000000000, 1.000000000000000000, 1.000000000000000000, 1.000000000000000000, 1.000000000000000000, 1.000000000000000000, 1.000000000000000000, 1.000000000000000000, 1.000000000000000000, 1.000000000000000000, 1.000000000000000000),
 ( 1.000000000000000000, 1.000000000000000000, 1.000000000000000000, 1.000000000000000000, 1.000000000000000000, 1.000000000000000000, 1.000000000000000000, 1.000000000000000000, 1.000000000000000000, 1.000000000000000000, 1.000000000000000000, 1.000000000000000000),
 ( 1.000000000000000000, 1.000000000000000000, 1.000000000000000000, 1.000000000000000000, 1.000000000000000000, 1.000000000000000000, 1.000000000000000000, 1.000000000000000000, 1.000000000000000000, 1.000000000000000000, 1.000000000000000000, 1.000000000000000000),
 ( 1.857142857142858317, 1.857142857142858317, 1.857142857142858317, 1.857142857142858317, 1.857142857142858317, 1.857142857142858317, 1.857142857142858317, 1.857142857142858317, 1.857142857142858317, 1.857142857142858317, 1.857142857142858317, 1.857142857142858317),
 ( 1.000000000000000000, 1.000000000000000000, 1.000000000000000000, 1.000000000000000000, 1.000000000000000000, 1.000000000000000000, 1.000000000000000000, 1.000000000000000000, 1.000000000000000000, 1.000000000000000000, 1.000000000000000000, 1.000000000000000000) ) ) 
 REPRESENTATION_ITEM ( '' )  SURFACE ( )  );
#80415=VERTEX_POINT ( 'NONE', #90057 ) ;
#80432=CARTESIAN_POINT ( 'NONE',  ( -8.737863884124131175, -5.000000000000002665, -79.96381019768853093 ) ) ;
#80435=CARTESIAN_POINT ( 'NONE',  ( 7.500000000000005329, -5.250000000000004441, -68.91429205785459544 ) ) ;
#80436=MECHANICAL_DESIGN_GEOMETRIC_PRESENTATION_REPRESENTATION('',(#76988),#6374);
#80438=ORIENTED_EDGE ( 'NONE', *, *, #9403, .F. ) ;
#80445=CARTESIAN_POINT ( 'NONE',  ( -1.191759989000076070, -5.000000000000000000, -97.99990947982458067 ) ) ;
#80451=CARTESIAN_POINT ( 'NONE',  ( -31.42871867836007027, 39.42550727674528588, 56.97524511970465255 ) ) ;
#80467=MECHANICAL_DESIGN_GEOMETRIC_PRESENTATION_REPRESENTATION('',(#75319),#63255);
#80470=CARTESIAN_POINT ( 'NONE',  ( 5.036189802310016006, 50.00000000000001421, -93.73786388411662074 ) ) ;
#80482=CARTESIAN_POINT ( 'NONE',  ( 8.733056179379989459, -5.000000000000000000, -16.76938723918380703 ) ) ;
#80489=MECHANICAL_DESIGN_GEOMETRIC_PRESENTATION_REPRESENTATION('',(#65022),#104671);
#80507=CARTESIAN_POINT ( 'NONE',  ( 7.029557119109635543, 41.29102226339720261, -70.49405813111694385 ) ) ;
#80531=CARTESIAN_POINT ( 'NONE',  ( 30.50942973405924974, 18.64284798592565195, -23.36871039509505721 ) ) ;
#80560=CARTESIAN_POINT ( 'NONE',  ( 39.04923757937011430, 50.00000000002003731, 52.30342408740191473 ) ) ;
#80566=CARTESIAN_POINT ( 'NONE',  ( 12.15075205251924828, -4.649444361049084762, -76.81485639520219877 ) ) ;
#80585=AXIS2_PLACEMENT_3D ( 'NONE', #60834, #19879, #67328 ) ;
#80593=CARTESIAN_POINT ( 'NONE',  ( -12.50000000000000000, 3.927497713838737692, -21.92086582174311005 ) ) ;
#80599=CARTESIAN_POINT ( 'NONE',  ( 6.645597273868374621, 41.91296976309556044, -68.91429206532015428 ) ) ;
#80630=( NAMED_UNIT ( * ) PLANE_ANGLE_UNIT ( ) SI_UNIT ( $, .RADIAN. ) );
#80661=CARTESIAN_POINT ( 'NONE',  ( -2.094395098902536390, -3.000000000000000000, -8.000000000000000000 ) ) ;
#80681=( NAMED_UNIT ( * ) SI_UNIT ( $, .STERADIAN. ) SOLID_ANGLE_UNIT ( ) );
#80689=CARTESIAN_POINT ( 'NONE',  ( 17.50000000000256506, 49.16280683614454716, 62.52714020843568221 ) ) ;
#80699=CARTESIAN_POINT ( 'NONE',  ( -5.692357205181195035, -4.313020517848788593, -16.93296622887996961 ) ) ;
#80717=( BOUNDED_CURVE ( )  B_SPLINE_CURVE ( 2, ( #51737, #42056, #74942 ),
 .UNSPECIFIED., .F., .F. ) 
 B_SPLINE_CURVE_WITH_KNOTS ( ( 3, 3 ),
 ( 0.000000000000000000, 1.000000000000000000 ),
 .UNSPECIFIED. ) 
 CURVE ( )  GEOMETRIC_REPRESENTATION_ITEM ( )  RATIONAL_B_SPLINE_CURVE ( ( 1.000000000000000000, 1.857142857142858317, 1.000000000000000000 ) ) 
 REPRESENTATION_ITEM ( '' )  );
#80747=B_SPLINE_CURVE_WITH_KNOTS ( 'NONE', 3,
 ( #36276, #102560, #61588, #89437 ),
 .UNSPECIFIED., .F., .F.,
 ( 4, 4 ),
 ( 0.000000000000000000, 1.000000000000000000 ),
 .UNSPECIFIED. ) ;
#80751=CARTESIAN_POINT ( 'NONE',  ( 6.434574498933689490, 41.95046769211187865, -59.72043363588650067 ) ) ;
#80787=CARTESIAN_POINT ( 'NONE',  ( -12.42907082493785076, -4.067133856147437498, -76.73301493501935511 ) ) ;
#80805=CARTESIAN_POINT ( 'NONE',  ( -8.000000000000000000, -4.999999999999998224, 2.094395098902548824 ) ) ;
#80812=FILL_AREA_STYLE ('',( #15550 ) ) ;
#80884=CARTESIAN_POINT ( 'NONE',  ( 5.660419746013990228, 41.80469037513988440, -58.87109516261954667 ) ) ;
#80918=PRESENTATION_STYLE_ASSIGNMENT (( #16723 ) ) ;
#80920=( NAMED_UNIT ( * ) SI_UNIT ( $, .STERADIAN. ) SOLID_ANGLE_UNIT ( ) );
#80928=CARTESIAN_POINT ( 'NONE',  ( 7.579218993349996936, -5.000000000006481038, -17.00320663867185900 ) ) ;
#80955=CARTESIAN_POINT ( 'NONE',  ( 39.08667504521158520, 48.00000000000000000, -56.76470588235294912 ) ) ;
#80961=CARTESIAN_POINT ( 'NONE',  ( -6.043427762771337086, -5.000000000000002665, -74.51456333905269958 ) ) ;
#80974=CARTESIAN_POINT ( 'NONE',  ( -5.782971157185549771, -5.000000000000000000, -96.70384082256207137 ) ) ;
#81014=CARTESIAN_POINT ( 'NONE',  ( 9.087744254835127933, -4.999999999999999112, -17.48834560249285985 ) ) ;
#81017=CARTESIAN_POINT ( 'NONE',  ( -6.913779242700420546, 41.73441082398074542, -59.30275289623196500 ) ) ;
#81026=CARTESIAN_POINT ( 'NONE',  ( 8.641101172573151246, -5.000000000000001776, -72.37542516944607485 ) ) ;
#81039=CARTESIAN_POINT ( 'NONE',  ( 7.004291983109769859, 40.56179000455576045, -71.01843131752761451 ) ) ;
#81043=AXIS2_PLACEMENT_3D ( 'NONE', #77601, #5309, #52245 ) ;
#81049=CARTESIAN_POINT ( 'NONE',  ( -59.92177854689752792, 50.00000000000000711, -19.49351526723193473 ) ) ;
#81062=CARTESIAN_POINT ( 'NONE',  ( 36.68673791898589087, 18.64284798592620618, -11.44574982650785167 ) ) ;
#81083=( LENGTH_UNIT ( ) NAMED_UNIT ( * ) SI_UNIT ( .MILLI., .METRE. ) );
#81092=CARTESIAN_POINT ( 'NONE',  ( 23.38163988287269390, 40.83906611472318815, 60.94087333791210170 ) ) ;
#81158=ORIENTED_EDGE ( 'NONE', *, *, #26243, .F. ) ;
#81161=DIRECTION ( 'NONE',  ( 1.000000000000000000, 0.000000000000000000, -1.160749806054361473E-16 ) ) ;
#81189=CARTESIAN_POINT ( 'NONE',  ( 2.617993873628172263, -5.000000000000000000, -10.00000000000000000 ) ) ;
#81213=CARTESIAN_POINT ( 'NONE',  ( 17.50000000000003197, 51.95328275803498741, 61.04403218098684647 ) ) ;
#81222=CARTESIAN_POINT ( 'NONE',  ( -7.499997280422835644, -2.963001255690722147, -20.99866594762864480 ) ) ;
#81247=CARTESIAN_POINT ( 'NONE',  ( -60.62677696746903422, 48.00000000000000000, 24.18439665018601303 ) ) ;
#81275=CARTESIAN_POINT ( 'NONE',  ( 5.947848185899612616, 41.98179895519294291, -59.44139658209459043 ) ) ;
#81281=VERTEX_POINT ( 'NONE', #41654 ) ;
#81288=VERTEX_POINT ( 'NONE', #46439 ) ;
#81323=CARTESIAN_POINT ( 'NONE',  ( 52.56483885390523625, 40.83906611471594061, -38.23529411764706509 ) ) ;
#81353=ORIENTED_EDGE ( 'NONE', *, *, #16156, .F. ) ;
#81376=CARTESIAN_POINT ( 'NONE',  ( 0.000000000000000000, 0.000000000000000000, 15.00000000000000178 ) ) ;
#81404=CARTESIAN_POINT ( 'NONE',  ( 6.767547407775503565, 41.65232290981239771, -58.92985917264464035 ) ) ;
#81424=EDGE_CURVE ( 'NONE', #58869, #102845, #48182, .T. ) ;
#81426=CARTESIAN_POINT ( 'NONE',  ( -5.346098296770412261, -4.999999999999997335, -15.46179592075988474 ) ) ;
#81430=CARTESIAN_POINT ( 'NONE',  ( 6.397334739185443375, -3.000000000000000444, 4.916373759799320453 ) ) ;
#81435=CARTESIAN_POINT ( 'NONE',  ( 63.45785145800994798, 48.00000000000000000, -14.99006954567211380 ) ) ;
#81444=CARTESIAN_POINT ( 'NONE',  ( 7.334017076207792307, -3.381213663715690654, -18.44266608209203895 ) ) ;
#81457=CARTESIAN_POINT ( 'NONE',  ( -64.32759900502631467, 40.83906611473152992, -11.06576400653637116 ) ) ;
#81458=CARTESIAN_POINT ( 'NONE',  ( -6.907083948287215058, 41.55068305711947829, -58.85924204532965831 ) ) ;
#81460=CARTESIAN_POINT ( 'NONE',  ( -19.48979057729603426, 49.99890399319770751, 60.12824249908928209 ) ) ;
#81479=CARTESIAN_POINT ( 'NONE',  ( 9.739726766104318756, -5.000000000001365130, -87.61747884499031613 ) ) ;
#81491=CARTESIAN_POINT ( 'NONE',  ( 0.000000000000000000, 0.000000000000000000, 0.000000000000000000 ) ) ;
#81497=CARTESIAN_POINT ( 'NONE',  ( 62.81009128990557144, 38.95404459711129164, -10.81681776479946144 ) ) ;
#81503=CARTESIAN_POINT ( 'NONE',  ( -8.990409435379676850, -5.000000000000000000, -71.93151781322266913 ) ) ;
#81542=STYLED_ITEM ( 'NONE', ( #38356 ), #19013 ) ;
#81558=CARTESIAN_POINT ( 'NONE',  ( -63.67138272020815748, 38.95383793066860534, 8.334564508068538657 ) ) ;
#81561=CARTESIAN_POINT ( 'NONE',  ( -45.43592567508400748, 50.00000000000001421, 43.65922790991991320 ) ) ;
#81568=CARTESIAN_POINT ( 'NONE',  ( -7.500000000000000888, -3.000671055698259870, -20.99923901233272971 ) ) ;
#81570=ORIENTED_EDGE ( 'NONE', *, *, #1980, .T. ) ;
#81634=B_SPLINE_CURVE_WITH_KNOTS ( 'NONE', 3,
 ( #15719, #56146, #98230, #15184, #16791, #65869, #64291, #48073, #56698, #99276, #16248, #31929, #33523, #80974, #97689, #97162, #80445, #89621, #7610, #8159, #48605, #98748, #49134, #106305, #33001, #49678, #40529, #8690, #24385, #24903, #41064, #39488, #73949, #57756 ),
 .UNSPECIFIED., .F., .F.,
 ( 4, 2, 2, 2, 2, 2, 2, 2, 2, 2, 2, 2, 2, 2, 2, 2, 4 ),
 ( 0.000000000000000000, 0.06250000000000000000, 0.1250000000000000000, 0.1875000000000000000, 0.2500000000000000000, 0.3125000000000000000, 0.3750000000000000000, 0.4375000000000000000, 0.5000000000000000000, 0.5625000000000000000, 0.6250000000000000000, 0.6875000000000000000, 0.7500000000000000000, 0.8125000000000000000, 0.8750000000000000000, 0.9375000000000000000, 1.000000000000000000 ),
 .UNSPECIFIED. ) ;
#81638=EDGE_LOOP ( 'NONE', ( #50207, #36473, #1235, #49108 ) ) ;
#81640=CARTESIAN_POINT ( 'NONE',  ( -12.50000000000000711, 16.77477480092213824, -34.50590452214681392 ) ) ;
#81645=SURFACE_STYLE_FILL_AREA ( #48752 ) ;
#81651=CARTESIAN_POINT ( 'NONE',  ( -7.326726048548432679, 41.40616594562586528, -69.28044392950745589 ) ) ;
#81655=VERTEX_POINT ( 'NONE', #49609 ) ;
#81663=CARTESIAN_POINT ( 'NONE',  ( 6.075691126275640563, 41.99394904787047977, -68.91429206828460963 ) ) ;
#81666=CARTESIAN_POINT ( 'NONE',  ( 12.13034742782428310, 49.99999999999999289, -93.82352941176471006 ) ) ;
#81672=CARTESIAN_POINT ( 'NONE',  ( 1.517883041479706208E-15, -5.000000000000000888, -97.00000000000000000 ) ) ;
#81679=CARTESIAN_POINT ( 'NONE',  ( 37.47001334519036675, 40.63833030000166247, -58.98724826624130202 ) ) ;
#81688=CARTESIAN_POINT ( 'NONE',  ( -6.931554132363010545, -3.000000000000119904, -71.13906995426670221 ) ) ;
#81695=CARTESIAN_POINT ( 'NONE',  ( 17.50000000000004974, 48.00000000000341771, 64.09949417230997426 ) ) ;
#81709=CARTESIAN_POINT ( 'NONE',  ( -5.219866590718559962, -5.000000000000000000, 8.922269033012391048 ) ) ;
#81723=CARTESIAN_POINT ( 'NONE',  ( 6.338673411933466006, 41.81695763293575396, -59.02782193812689115 ) ) ;
#81726=SURFACE_STYLE_FILL_AREA ( #91974 ) ;
#81738=CARTESIAN_POINT ( 'NONE',  ( 17.49999999999544897, 49.80818831228071986, 62.14041309008325698 ) ) ;
#81747=CARTESIAN_POINT ( 'NONE',  ( -5.885102640077104041, -4.999999999999960920, -15.35622078683719849 ) ) ;
#81785=CARTESIAN_POINT ( 'NONE',  ( -17.34830914839865201, 18.64284798592992232, 34.29224544877759939 ) ) ;
#81788=CARTESIAN_POINT ( 'NONE',  ( 7.126148245860624009, 41.12758397993106740, -58.55282951229289523 ) ) ;
#81854=CARTESIAN_POINT ( 'NONE',  ( 7.137815226410160641, -3.000000000000000000, -4.175893272574602300 ) ) ;
#81870=CARTESIAN_POINT ( 'NONE',  ( 7.500000000000002665, 4.320742148886384193, -27.76523484934585895 ) ) ;
#81898=VERTEX_POINT ( 'NONE', #94344 ) ;
#81900=EDGE_CURVE ( 'NONE', #105469, #84646, #49523, .T. ) ;
#81937=CARTESIAN_POINT ( 'NONE',  ( 6.770722867741076456, 41.58070725240481380, -58.79856991761213436 ) ) ;
#81959=CARTESIAN_POINT ( 'NONE',  ( -9.384368963317969659, -5.000000000000000000, -18.81659302942708223 ) ) ;
#81994=CARTESIAN_POINT ( 'NONE',  ( -63.03617022304293727, 40.83906611473187809, -16.93907820429951983 ) ) ;
#81998=CARTESIAN_POINT ( 'NONE',  ( -19.35735956073961006, 49.90708382026840439, 61.17470024478767243 ) ) ;
#82002=CARTESIAN_POINT ( 'NONE',  ( -7.225703553025885739, -5.000000000000001776, -73.19314196553557395 ) ) ;
#82017=CARTESIAN_POINT ( 'NONE',  ( 2.617478844992707110, -5.000000000000015099, -94.73972676610841859 ) ) ;
#82022=CARTESIAN_POINT ( 'NONE',  ( 7.500000000000005329, 9.833333333333344584, -68.91429205785459544 ) ) ;
#82042=CARTESIAN_POINT ( 'NONE',  ( 54.08561378075543047, 38.95410943244764468, 34.09344903348132050 ) ) ;
#82055=PRESENTATION_STYLE_ASSIGNMENT (( #33019 ) ) ;
#82064=CARTESIAN_POINT ( 'NONE',  ( -11.08666809900981676, -4.983486105408843514, -12.57803232073183786 ) ) ;
#82102=CARTESIAN_POINT ( 'NONE',  ( 7.418912130467639088, 41.12212895980070471, -69.28711560576921613 ) ) ;
#82121=COLOUR_RGB ( '', 0.08235294, 0.09019608, 0.10196078) ;
#82124=CARTESIAN_POINT ( 'NONE',  ( 7.493767109741696686, 40.39058573922605433, -59.41312748714017289 ) ) ;
#82140=CARTESIAN_POINT ( 'NONE',  ( 13.85787468398986100, 43.09645778404858163, -91.44857208682125815 ) ) ;
#82146=FACE_OUTER_BOUND ( 'NONE', #47982, .T. ) ;
#82151=CARTESIAN_POINT ( 'NONE',  ( -1.448103213439668968, -5.000000000000000000, -72.00384268476057059 ) ) ;
#82167=PRESENTATION_STYLE_ASSIGNMENT (( #67993 ) ) ;
#82190=SURFACE_SIDE_STYLE ('',( #81645 ) ) ;
#82195=CARTESIAN_POINT ( 'NONE',  ( -7.204797958417223924, 41.05104878663154722, -70.50691237690513447 ) ) ;
#82221=CARTESIAN_POINT ( 'NONE',  ( -11.69538631874851653, -5.000000000000000000, -88.12269504201408665 ) ) ;
#82224=CARTESIAN_POINT ( 'NONE',  ( 17.50000000000002842, 45.00000000000000711, 100.0000000000000000 ) ) ;
#82228=CARTESIAN_POINT ( 'NONE',  ( 46.50260525563992076, 39.63181832368864832, -46.56948742080178505 ) ) ;
#82233=CARTESIAN_POINT ( 'NONE',  ( 12.50000000000000355, 27.22490228149561631, -44.76726718883759304 ) ) ;
#82238=CARTESIAN_POINT ( 'NONE',  ( -7.500000000000003553, -2.999999999998154365, -69.80246343544763477 ) ) ;
#82239=( LENGTH_UNIT ( ) NAMED_UNIT ( * ) SI_UNIT ( .MILLI., .METRE. ) );
#82246=CARTESIAN_POINT ( 'NONE',  ( 17.50000000000003553, 48.75234879777378438, 64.07562946667630399 ) ) ;
#82257=CARTESIAN_POINT ( 'NONE',  ( -4.852941176470586093, 40.00000000000132871, -70.80672828634229177 ) ) ;
#82300=CARTESIAN_POINT ( 'NONE',  ( -7.579218993349681632, -4.999999999985669241, -17.00320663868540905 ) ) ;
#82324=CARTESIAN_POINT ( 'NONE',  ( 64.32759900504497352, 48.00000000000000000, -11.06576400629120549 ) ) ;
#82364=CARTESIAN_POINT ( 'NONE',  ( -6.619572829881549936, 41.38254192478331106, -70.73105035172459054 ) ) ;
#82387=CARTESIAN_POINT ( 'NONE',  ( -13.88435755502521474, 42.00000000000000000, -90.88030988970933777 ) ) ;
#82418=SURFACE_SIDE_STYLE ('',( #41951 ) ) ;
#82461=CARTESIAN_POINT ( 'NONE',  ( 1.224646799147352073E-15, 49.99999999999999289, -75.00000000000001421 ) ) ;
#82482=( LENGTH_UNIT ( ) NAMED_UNIT ( * ) SI_UNIT ( .MILLI., .METRE. ) );
#82484=B_SPLINE_SURFACE_WITH_KNOTS ( 'NONE', 3, 3, ( 
 ( #102382, #61414, #78105, #53824, #70020, #29086, #52228, #86230 ),
 ( #77044, #21496, #85138, #45230, #4223, #95359, #13353, #76504 ),
 ( #102919, #61952, #60358, #86757, #2613, #12825, #93233, #68975 ),
 ( #28009, #45745, #93769, #19926, #85687, #56470, #63536, #89400 ),
 ( #72664, #6865, #31703, #80218, #6322, #14411, #105564, #5293 ),
 ( #62999, #88338, #23618, #95895, #31188, #105047, #55919, #7389 ),
 ( #71595, #97461, #38213, #47322, #104500, #22021, #80751, #72137 ),
 ( #103966, #73175, #14950, #39789, #81275, #64590, #15494, #64073 ),
 ( #48381, #40302, #96432, #88861, #47844, #32229, #46280, #22568 ),
 ( #106080, #96948, #23082, #65108, #30108, #71076, #98005, #39264 ) ),
 .UNSPECIFIED., .F., .F., .F.,
 ( 4, 2, 2, 2, 4 ),
 ( 4, 2, 2, 4 ),
 ( 0.000000000000000000, 0.1250000000000000000, 0.2500000000000000000, 0.5000000000000000000, 1.000000000000000000 ),
 ( 0.000000000000000000, 0.2500000000000000000, 0.5000000000000000000, 1.000000000000000000 ),
 .UNSPECIFIED. ) ;
#82491=CARTESIAN_POINT ( 'NONE',  ( 6.373568729748126493, 41.63985758277738114, -58.70717962065710793 ) ) ;
#82507=CARTESIAN_POINT ( 'NONE',  ( 17.63369058254861699, 45.00000000000000711, 63.00619685671904335 ) ) ;
#82512=CARTESIAN_POINT ( 'NONE',  ( -8.991848411656118145, -5.000000000000000000, -17.27917748744093629 ) ) ;
#82519=CARTESIAN_POINT ( 'NONE',  ( -9.739726766103894207, -3.000000000000002665, -82.38252115500876016 ) ) ;
#82548=ORIENTED_EDGE ( 'NONE', *, *, #8268, .T. ) ;
#82550=CARTESIAN_POINT ( 'NONE',  ( -19.48249511158732261, 49.99632329421929455, 60.25369351552990338 ) ) ;
#82563=CARTESIAN_POINT ( 'NONE',  ( -34.17192354664857845, 40.55982561316064050, -60.71114593581258845 ) ) ;
#82569=CARTESIAN_POINT ( 'NONE',  ( 1.308996937483426937, -5.000000000000002665, -75.00000000000001421 ) ) ;
#82591=CARTESIAN_POINT ( 'NONE',  ( 28.18312358715398247, 38.95287143380507899, 57.16470827993371984 ) ) ;
#82598=CARTESIAN_POINT ( 'NONE',  ( -9.432319653624512412, -5.000000000000000000, -70.68463330168729897 ) ) ;
#82651=CARTESIAN_POINT ( 'NONE',  ( 6.806778131844891000, 41.25019534418786549, -70.74215739200818120 ) ) ;
#82669=CARTESIAN_POINT ( 'NONE',  ( 38.34155876363057303, 18.64284798592657921, -2.616639027923388205 ) ) ;
#82737=CARTESIAN_POINT ( 'NONE',  ( -10.63258248847111531, 48.00000000000000000, -95.64586607611548175 ) ) ;
#82739=CARTESIAN_POINT ( 'NONE',  ( -7.168069589493909710, 40.56151012121110710, -70.87151392390727267 ) ) ;
#82774=CARTESIAN_POINT ( 'NONE',  ( 12.50000000000000711, 35.28456030440094793, -54.82782442755426189 ) ) ;
#82779=CARTESIAN_POINT ( 'NONE',  ( -7.421727621021489973, -3.000000000000118128, -70.37058875307404548 ) ) ;
#82787=CARTESIAN_POINT ( 'NONE',  ( -1.727368016638141196E-09, 38.95322581935191408, 63.66965480466879512 ) ) ;
#82792=VERTEX_POINT ( 'NONE', #78808 ) ;
#82809=SURFACE_STYLE_USAGE ( .BOTH. , #8909 ) ;
#82828=CARTESIAN_POINT ( 'NONE',  ( 19.01558148378777346, 49.54233067771700405, 61.88543008400887402 ) ) ;
#82862=CARTESIAN_POINT ( 'NONE',  ( -64.32759900504490247, 48.00000000000000000, -11.06576400629244361 ) ) ;
#82894=EDGE_CURVE ( 'NONE', #8448, #24875, #49315, .T. ) ;
#82900=CARTESIAN_POINT ( 'NONE',  ( -5.500000000000007994, 42.00000000000000000, -68.91429205818155879 ) ) ;
#82950=CARTESIAN_POINT ( 'NONE',  ( -12.50000000000000000, -3.000000000000000000, -9.904958390907868448 ) ) ;
#83012=PRESENTATION_STYLE_ASSIGNMENT (( #25894 ) ) ;
#83023=FACE_OUTER_BOUND ( 'NONE', #74243, .T. ) ;
#83037=ADVANCED_FACE ( 'NONE', ( #25393 ), #13304, .T. ) ;
#83039=CARTESIAN_POINT ( 'NONE',  ( 17.60121130357612174, 45.00000000000000000, 63.09853793600694871 ) ) ;
#83063=CARTESIAN_POINT ( 'NONE',  ( 9.256208135396892800, -5.000000000000000888, -17.97305361429082993 ) ) ;
#83080=CARTESIAN_POINT ( 'NONE',  ( -19.23735690889347794, 49.80931112121790250, 61.48632125443229057 ) ) ;
#83093=CARTESIAN_POINT ( 'NONE',  ( -19.56509672771084141, 41.86698933908479603, -80.29965057802650108 ) ) ;
#83122=CARTESIAN_POINT ( 'NONE',  ( 22.84345602534879660, 38.95245093555178073, 59.50021660759410480 ) ) ;
#83131=ORIENTED_EDGE ( 'NONE', *, *, #96302, .F. ) ;
#83136=DIRECTION ( 'NONE',  ( 0.000000000000000000, 1.000000000000000000, 0.000000000000000000 ) ) ;
#83201=CARTESIAN_POINT ( 'NONE',  ( 0.000000000000000000, 0.000000000000000000, 15.00000000000000178 ) ) ;
#83211=FILL_AREA_STYLE ('',( #32573 ) ) ;
#83228=VERTEX_POINT ( 'NONE', #9561 ) ;
#83240=CARTESIAN_POINT ( 'NONE',  ( 88.20421627925426833, 42.00000000000000000, 23.70422451874904013 ) ) ;
#83265=CARTESIAN_POINT ( 'NONE',  ( -12.34835181856066555, -4.332967528434497062, -12.86601580078907148 ) ) ;
#83270=CARTESIAN_POINT ( 'NONE',  ( -7.404343286415054237, 40.29318263988768223, -70.39067260838145046 ) ) ;
#83276=EDGE_LOOP ( 'NONE', ( #9887, #12017, #50079, #87461 ) ) ;
#83279=CARTESIAN_POINT ( 'NONE',  ( 4.966176485634622217, 41.64999999999998437, -70.47555195150158625 ) ) ;
#83315=CARTESIAN_POINT ( 'NONE',  ( 17.50000000000002487, 48.46901212408400283, 64.09337290743147264 ) ) ;
#83326=CARTESIAN_POINT ( 'NONE',  ( -7.439139359426217624, 41.00331351352566145, -59.84461297751296627 ) ) ;
#83340=EDGE_LOOP ( 'NONE', ( #79870, #72529, #56486, #102672 ) ) ;
#83356=CARTESIAN_POINT ( 'NONE',  ( -6.786616733794231138, 41.72678875807561383, -59.11526074045958268 ) ) ;
#83363=CARTESIAN_POINT ( 'NONE',  ( -5.882666732301543355, -4.999999999999851674, -15.34024587939825857 ) ) ;
#83368=( NAMED_UNIT ( * ) SI_UNIT ( $, .STERADIAN. ) SOLID_ANGLE_UNIT ( ) );
#83388=CARTESIAN_POINT ( 'NONE',  ( -50.94745919686192082, 50.00000000000000000, -37.05882352941185331 ) ) ;
#83472=DIRECTION ( 'NONE',  ( 0.000000000000000000, 1.000000000000000000, 0.000000000000000000 ) ) ;
#83474=CARTESIAN_POINT ( 'NONE',  ( 14.33580413386840213, 42.00000000000000000, -89.41414995614803729 ) ) ;
#83487=CARTESIAN_POINT ( 'NONE',  ( 7.270302578000916505, -3.659675574284731780, -18.03744543698569203 ) ) ;
#83501=ORIENTED_EDGE ( 'NONE', *, *, #16156, .T. ) ;
#83516=CARTESIAN_POINT ( 'NONE',  ( -6.542885568110277106, 41.77240995323538897, -59.03854211387476880 ) ) ;
#83527=CARTESIAN_POINT ( 'NONE',  ( 9.500000000000003553, -5.000000000000000000, -68.91429205785459544 ) ) ;
#83542=CARTESIAN_POINT ( 'NONE',  ( 5.398220238549152228, 41.68867471179443385, -58.74408635829322378 ) ) ;
#83543=CARTESIAN_POINT ( 'NONE',  ( -5.500000000000006217, 42.00000000000000000, -58.09827136975972905 ) ) ;
#83552=CARTESIAN_POINT ( 'NONE',  ( 1.719443193058131758, -4.999999999998633093, -17.47055129848030219 ) ) ;
#83553=CARTESIAN_POINT ( 'NONE',  ( -1.308996938995748982, -3.000000000000001776, -75.00000000000000000 ) ) ;
#83557=( BOUNDED_SURFACE ( )  B_SPLINE_SURFACE ( 2, 3, ( 
 ( #62155, #21700, #95048, #63737, #11973, #62672, #46476, #38923, #63200, #79364 ),
 ( #96091, #30854, #96620, #49102, #56666, #65835, #31385, #89059, #98715, #90111 ),
 ( #32437, #7058, #47522, #82002, #105757, #89590, #48042, #72337, #98197, #105241 ) ),
 .UNSPECIFIED., .F., .F., .F. ) 
 B_SPLINE_SURFACE_WITH_KNOTS ( ( 3, 3 ),
 ( 4, 2, 2, 2, 4 ),
 ( 0.000000000000000000, 1.000000000000000000 ),
 ( 0.000000000000000000, 0.001626978433639921342, 0.003253956867279842683, 0.004880935300919764241, 0.006507913734559685366 ),
 .UNSPECIFIED. ) 
 GEOMETRIC_REPRESENTATION_ITEM ( )  RATIONAL_B_SPLINE_SURFACE ( (
 ( 1.000000000000000000, 1.000000000000000000, 1.000000000000000000, 1.000000000000000000, 1.000000000000000000, 1.000000000000000000, 1.000000000000000000, 1.000000000000000000, 1.000000000000000000, 1.000000000000000000),
 ( 1.857142857142858317, 1.857142857142858317, 1.857142857142858317, 1.857142857142858317, 1.857142857142858317, 1.857142857142858317, 1.857142857142858317, 1.857142857142858317, 1.857142857142858317, 1.857142857142858317),
 ( 1.000000000000000000, 1.000000000000000000, 1.000000000000000000, 1.000000000000000000, 1.000000000000000000, 1.000000000000000000, 1.000000000000000000, 1.000000000000000000, 1.000000000000000000, 1.000000000000000000) ) ) 
 REPRESENTATION_ITEM ( '' )  SURFACE ( )  );
#83576=CARTESIAN_POINT ( 'NONE',  ( 9.060614273895151172, -4.999999999999968914, -17.33913672110647752 ) ) ;
#83579=CARTESIAN_POINT ( 'NONE',  ( -8.857351009234111672, -3.000000000000002665, -97.18047212222559494 ) ) ;
#83600=CARTESIAN_POINT ( 'NONE',  ( -17.49999999999841904, 48.26617306480387981, 62.61753806995410088 ) ) ;
#83610=CARTESIAN_POINT ( 'NONE',  ( 6.123233995736763324E-16, 48.00000000000000000, -95.00000000000000000 ) ) ;
#83612=CARTESIAN_POINT ( 'NONE',  ( -17.66057173557561910, 41.94261100565687883, -82.88176911731406449 ) ) ;
#83675=CARTESIAN_POINT ( 'NONE',  ( -7.417433415418480003, 41.15875677289866985, -59.49136428978601998 ) ) ;
#83702=CARTESIAN_POINT ( 'NONE',  ( -51.48757442383523397, 38.95383793070303113, -37.45149417477429665 ) ) ;
#83707=CARTESIAN_POINT ( 'NONE',  ( -1.841875822471433519E-14, -3.000000000000002665, -70.00227127314062159 ) ) ;
#83759=CARTESIAN_POINT ( 'NONE',  ( 17.50000000000002842, 50.00000000000000000, 100.0000000000000000 ) ) ;
#83762=CARTESIAN_POINT ( 'NONE',  ( -55.65414010186731986, 42.00000000000000000, 72.41885610124127481 ) ) ;
#83770=CARTESIAN_POINT ( 'NONE',  ( -23.30914976775985537, 40.83761692952442957, 60.74960289684516113 ) ) ;
#83788=CARTESIAN_POINT ( 'NONE',  ( -12.48743925095353191, -3.519139377062180607, -13.73189632760026058 ) ) ;
#83792=CARTESIAN_POINT ( 'NONE',  ( -7.445751637708186266, 40.55658532066092903, -70.17153985021506912 ) ) ;
#83803=CARTESIAN_POINT ( 'NONE',  ( -10.00012749751951446, -4.999999999999999112, 1.308371270542952658 ) ) ;
#83806=APPLICATION_CONTEXT ( 'automotive_design' ) ;
#83831=CARTESIAN_POINT ( 'NONE',  ( 12.50000000000000711, 34.80611260448990407, -54.08410186685180321 ) ) ;
#83850=EDGE_LOOP ( 'NONE', ( #55935, #52885, #34291, #22018, #78186, #71661 ) ) ;
#83868=MECHANICAL_DESIGN_GEOMETRIC_PRESENTATION_REPRESENTATION('',(#37339),#104501);
#83878=( NAMED_UNIT ( * ) PLANE_ANGLE_UNIT ( ) SI_UNIT ( $, .RADIAN. ) );
#83890=( BOUNDED_SURFACE ( )  B_SPLINE_SURFACE ( 2, 3, ( 
 ( #3326, #36273, #20093, #27647, #93410, #84777, #51863, #52395, #100952, #19560, #2240, #11395, #77753, #93936, #3864, #28704, #61585, #94479, #27109, #34668, #102012, #85308, #1715, #60001, #36796, #69662, #19024, #10862, #67540, #44320, #78792, #37326, #31354, #70719 ),
 ( #62123, #29242, #53980, #70186, #95013, #30277, #38373, #64233, #96591, #38890, #22727, #47484, #23246, #21148, #103611, #22190, #71237, #104132, #55564, #45392, #12462, #78272, #79331, #103093, #79856, #97105, #86918, #88500, #6494, #14578, #80382, #21664, #12989, #45915 ),
 ( #4926, #63164, #39426, #37858, #72301, #29760, #46956, #5964, #105207, #96060, #5452, #54501, #87445, #55040, #62635, #46442, #95523, #87972, #86396, #30820, #63706, #4385, #13523, #14052, #71758, #104667, #82519, #106781, #74939, #40464, #50144, #489, #25380, #32402 ) ),
 .UNSPECIFIED., .F., .T., .F. ) 
 B_SPLINE_SURFACE_WITH_KNOTS ( ( 3, 3 ),
 ( 4, 2, 2, 2, 2, 2, 2, 2, 2, 2, 2, 2, 2, 2, 2, 2, 4 ),
 ( 0.000000000000000000, 1.000000000000000000 ),
 ( 0.000000000000000000, 0.3926990816987241395, 0.7853981633974482790, 1.178097245096172418, 1.570796326794896558, 1.963495408493620697, 2.356194490192344837, 2.748893571891068976, 3.141592653589793116, 3.534291735288517255, 3.926990816987241395, 4.319689898685965090, 4.712388980384689674, 5.105088062083414258, 5.497787143782137953, 5.890486225480861648, 6.283185307179586232 ),
 .UNSPECIFIED. ) 
 GEOMETRIC_REPRESENTATION_ITEM ( )  RATIONAL_B_SPLINE_SURFACE ( (
 ( 1.000000000000000000, 1.000000000000000000, 1.000000000000000000, 1.000000000000000000, 1.000000000000000000, 1.000000000000000000, 1.000000000000000000, 1.000000000000000000, 1.000000000000000000, 1.000000000000000000, 1.000000000000000000, 1.000000000000000000, 1.000000000000000000, 1.000000000000000000, 1.000000000000000000, 1.000000000000000000, 1.000000000000000000, 1.000000000000000000, 1.000000000000000000, 1.000000000000000000, 1.000000000000000000, 1.000000000000000000, 1.000000000000000000, 1.000000000000000000, 1.000000000000000000, 1.000000000000000000, 1.000000000000000000, 1.000000000000000000, 1.000000000000000000, 1.000000000000000000, 1.000000000000000000, 1.000000000000000000, 1.000000000000000000, 1.000000000000000000),
 ( 1.857142857142858317, 1.857142857142858317, 1.857142857142858317, 1.857142857142858317, 1.857142857142858317, 1.857142857142858317, 1.857142857142858317, 1.857142857142858317, 1.857142857142858317, 1.857142857142858317, 1.857142857142858317, 1.857142857142858317, 1.857142857142858317, 1.857142857142858317, 1.857142857142858317, 1.857142857142858317, 1.857142857142858317, 1.857142857142858317, 1.857142857142858317, 1.857142857142858317, 1.857142857142858317, 1.857142857142858317, 1.857142857142858317, 1.857142857142858317, 1.857142857142858317, 1.857142857142858317, 1.857142857142858317, 1.857142857142858317, 1.857142857142858317, 1.857142857142858317, 1.857142857142858317, 1.857142857142858317, 1.857142857142858317, 1.857142857142858317),
 ( 1.000000000000000000, 1.000000000000000000, 1.000000000000000000, 1.000000000000000000, 1.000000000000000000, 1.000000000000000000, 1.000000000000000000, 1.000000000000000000, 1.000000000000000000, 1.000000000000000000, 1.000000000000000000, 1.000000000000000000, 1.000000000000000000, 1.000000000000000000, 1.000000000000000000, 1.000000000000000000, 1.000000000000000000, 1.000000000000000000, 1.000000000000000000, 1.000000000000000000, 1.000000000000000000, 1.000000000000000000, 1.000000000000000000, 1.000000000000000000, 1.000000000000000000, 1.000000000000000000, 1.000000000000000000, 1.000000000000000000, 1.000000000000000000, 1.000000000000000000, 1.000000000000000000, 1.000000000000000000, 1.000000000000000000, 1.000000000000000000) ) ) 
 REPRESENTATION_ITEM ( '' )  SURFACE ( )  );
#83901=CARTESIAN_POINT ( 'NONE',  ( 0.000000000000000000, -3.331654917651224235, 0.000000000000000000 ) ) ;
#83905=CARTESIAN_POINT ( 'NONE',  ( -4.852941176470598528, -3.000000000000002665, -70.80672828634229177 ) ) ;
#83915=UNCERTAINTY_MEASURE_WITH_UNIT (LENGTH_MEASURE( 1.000000000000000082E-05 ), #62526, 'distance_accuracy_value', 'NONE');
#83923=CARTESIAN_POINT ( 'NONE',  ( -11.54772599577038505, 50.00000000000000000, 62.20121126512094634 ) ) ;
#83935=UNCERTAINTY_MEASURE_WITH_UNIT (LENGTH_MEASURE( 1.000000000000000082E-05 ), #104781, 'distance_accuracy_value', 'NONE');
#83936=B_SPLINE_CURVE_WITH_KNOTS ( 'NONE', 3,
 ( #23878, #56722, #40030, #582, #89644, #66418, #15745, #65366, #48628, #106330, #24411, #90170, #82064, #10822, #84208, #43744, #2203, #67500, #101973, #42680, #52903, #28134, #26544, #93370, #17896, #60491, #35697, #76633, #51824, #85270 ),
 .UNSPECIFIED., .F., .F.,
 ( 4, 2, 2, 1, 1, 1, 2, 2, 2, 2, 2, 1, 2, 2, 2, 2, 4 ),
 ( 0.000000000000000000, 0.1249999999998845923, 0.1874999999998268885, 0.2187499999997968292, 0.2343749999997817579, 0.2421874999997729871, 0.2460937499997698230, 0.2499999999997666589, 0.3749999999998109290, 0.4374999999998330225, 0.4687499999998432365, 0.4843749999998492317, 0.4921874999998513966, 0.4999999999998535616, 0.6249999999998900879, 0.7499999999999267253, 1.000000000000000000 ),
 .UNSPECIFIED. ) ;
#83937=ORIENTED_EDGE ( 'NONE', *, *, #24170, .F. ) ;
#83955=ORIENTED_EDGE ( 'NONE', *, *, #24427, .F. ) ;
#83965=EDGE_LOOP ( 'NONE', ( #72613, #5818, #81570, #78917, #94836 ) ) ;
#83966=CARTESIAN_POINT ( 'NONE',  ( 8.737863884124120517, 49.99999999999999289, -90.03618980230058355 ) ) ;
#84044=ORIENTED_EDGE ( 'NONE', *, *, #104574, .F. ) ;
#84059=CARTESIAN_POINT ( 'NONE',  ( -6.907083948287215058, 41.55068305711947829, -58.85924204532965831 ) ) ;
#84084=CARTESIAN_POINT ( 'NONE',  ( 5.666915313784246067, 41.34312547834939977, -58.37679883534556069 ) ) ;
#84119=CIRCLE ( 'NONE', #104831, 60.00000000000000000 ) ;
#84126=CARTESIAN_POINT ( 'NONE',  ( 5.074712500031950846, -4.333244529504593601, -17.09696852381403431 ) ) ;
#84127=CARTESIAN_POINT ( 'NONE',  ( 11.46641754970693228, -3.000000000000002665, -75.26692388747142104 ) ) ;
#84128=CARTESIAN_POINT ( 'NONE',  ( -14.92666003045043510, -3.000000000000002665, -87.00284506551274433 ) ) ;
#84151=EDGE_CURVE ( 'NONE', #82792, #36789, #100709, .T. ) ;
#84175=CARTESIAN_POINT ( 'NONE',  ( 6.057904175366206623, 41.61856606260997893, -70.65344123640606711 ) ) ;
#84201=CARTESIAN_POINT ( 'NONE',  ( 7.421727621019012844, -2.999999999999999112, -70.37058875308096617 ) ) ;
#84206=( BOUNDED_CURVE ( )  B_SPLINE_CURVE ( 2, ( #34281, #67154, #8898 ),
 .UNSPECIFIED., .F., .F. ) 
 B_SPLINE_CURVE_WITH_KNOTS ( ( 3, 3 ),
 ( 0.000000000000000000, 1.000000000000000000 ),
 .UNSPECIFIED. ) 
 CURVE ( )  GEOMETRIC_REPRESENTATION_ITEM ( )  RATIONAL_B_SPLINE_CURVE ( ( 1.000000000000000000, 1.857142857142858317, 1.000000000000000000 ) ) 
 REPRESENTATION_ITEM ( '' )  );
#84208=CARTESIAN_POINT ( 'NONE',  ( -11.30963196869130449, -4.963880803831879795, -12.57418315201559800 ) ) ;
#84227=CARTESIAN_POINT ( 'NONE',  ( -7.423110184046854521, 40.85353637179369457, -59.12022309273985599 ) ) ;
#84229=CARTESIAN_POINT ( 'NONE',  ( 6.642722263319527087, 41.46658730130243953, -70.60825968728163105 ) ) ;
#84234=DIRECTION ( 'NONE',  ( 0.000000000000000000, 1.000000000000000000, 0.000000000000000000 ) ) ;
#84236=ORIENTED_EDGE ( 'NONE', *, *, #106117, .T. ) ;
#84281=ORIENTED_EDGE ( 'NONE', *, *, #91606, .F. ) ;
#84284=CARTESIAN_POINT ( 'NONE',  ( -4.852941176470593199, 44.25000000000000000, -70.80672828634229177 ) ) ;
#84295=CARTESIAN_POINT ( 'NONE',  ( -7.500000000000002665, 4.320742148886547618, -27.76523484934600816 ) ) ;
#84318=CARTESIAN_POINT ( 'NONE',  ( 2.971737004093363499, 40.83778713800185756, 64.99968649108126328 ) ) ;
#84336=CARTESIAN_POINT ( 'NONE',  ( -12.49701543487590705, -3.281887186806090373, -14.00878883702671018 ) ) ;
#84339=UNCERTAINTY_MEASURE_WITH_UNIT (LENGTH_MEASURE( 1.000000000000000082E-05 ), #55653, 'distance_accuracy_value', 'NONE');
#84387=CARTESIAN_POINT ( 'NONE',  ( 5.415856237588537958, 41.85405046271414875, -58.97635192936115800 ) ) ;
#84408=CARTESIAN_POINT ( 'NONE',  ( 10.50000000000000355, -5.000000000000000000, -34.12705335492802305 ) ) ;
#84412=PRESENTATION_STYLE_ASSIGNMENT (( #82809 ) ) ;
#84432=CARTESIAN_POINT ( 'NONE',  ( -43.69716417794982277, 48.00000000000000000, 48.48761666242421597 ) ) ;
#84445=CARTESIAN_POINT ( 'NONE',  ( 17.59235505452603832, 49.99999999999999289, 62.71843377526943897 ) ) ;
#84464=CARTESIAN_POINT ( 'NONE',  ( 7.069742150690448312, 41.66287055390499461, -69.58314084581829206 ) ) ;
#84465=CARTESIAN_POINT ( 'NONE',  ( -42.35263604938428017, 50.00000000000000000, 46.99568999588436924 ) ) ;
#84478=CARTESIAN_POINT ( 'NONE',  ( -38.38499389483345681, 18.64284798593159564, 1.874612472308246902 ) ) ;
#84491=CARTESIAN_POINT ( 'NONE',  ( 33.07092925538307782, 40.70022578739308727, -62.17362998248158590 ) ) ;
#84510=CARTESIAN_POINT ( 'NONE',  ( -6.043427762771305112, 50.00000000000000000, -74.51456333905269958 ) ) ;
#84520=PRODUCT ( '2. Holder', '2. Holder', '', ( #56794 ) ) ;
#84555=CARTESIAN_POINT ( 'NONE',  ( -19.32515916410156009, 49.99999999999999289, 60.14378497377332167 ) ) ;
#84599=CARTESIAN_POINT ( 'NONE',  ( -6.641837642500876271, 41.74662713182689089, -59.04567091375639620 ) ) ;
#84614=CARTESIAN_POINT ( 'NONE',  ( 79.13121736040859844, 42.00000000000000000, -45.60838156035022450 ) ) ;
#84631=( NAMED_UNIT ( * ) SI_UNIT ( $, .STERADIAN. ) SOLID_ANGLE_UNIT ( ) );
#84646=VERTEX_POINT ( 'NONE', #97025 ) ;
#84649=CARTESIAN_POINT ( 'NONE',  ( -12.10346316003903056, -4.692865865568782269, -76.82923406330107241 ) ) ;
#84663=CARTESIAN_POINT ( 'NONE',  ( -14.73122683063112603, -3.000000000000002665, -81.05502296678270113 ) ) ;
#84680=CARTESIAN_POINT ( 'NONE',  ( -17.49999999999995381, 51.97748320727993843, 60.75044042984304582 ) ) ;
#84699=CARTESIAN_POINT ( 'NONE',  ( -9.999999999999992895, -3.000000000000002665, -83.69100306252320820 ) ) ;
#84701=VERTEX_POINT ( 'NONE', #104053 ) ;
#84707=CARTESIAN_POINT ( 'NONE',  ( -3.631902923573203879, -4.332661967060489339, 17.83376356531591611 ) ) ;
#84732=CARTESIAN_POINT ( 'NONE',  ( 9.500000000000003553, -4.999999999999998224, -68.91429205785459544 ) ) ;
#84736=DIRECTION ( 'NONE',  ( 0.000000000000000000, 0.000000000000000000, 1.000000000000000000 ) ) ;
#84749=( GEOMETRIC_REPRESENTATION_CONTEXT ( 3 ) GLOBAL_UNCERTAINTY_ASSIGNED_CONTEXT ( ( #16144 ) ) GLOBAL_UNIT_ASSIGNED_CONTEXT ( ( #22431, #69494, #28532 ) ) REPRESENTATION_CONTEXT ( 'NONE', 'WORKASPACE' ) );
#84758=CARTESIAN_POINT ( 'NONE',  ( -7.090506018371190322, 41.24767894959148151, -58.61600934880981839 ) ) ;
#84759=CARTESIAN_POINT ( 'NONE',  ( 7.036764706176849238, 40.29466777802799271, -71.06385277369803077 ) ) ;
#84777=CARTESIAN_POINT ( 'NONE',  ( 9.596002107493083244, -5.000000000000002665, -77.62543935902139935 ) ) ;
#84817=CARTESIAN_POINT ( 'NONE',  ( -9.312033689600580644, 50.00000000000000000, -94.29807022305314490 ) ) ;
#84832=ORIENTED_EDGE ( 'NONE', *, *, #12483, .T. ) ;
#84840=CARTESIAN_POINT ( 'NONE',  ( -14.91271302809441401, 41.98564543112699710, -86.62215342991694911 ) ) ;
#84841=CARTESIAN_POINT ( 'NONE',  ( -59.23741894013591036, 42.00000000000000711, 7.754160006507077263 ) ) ;
#84848=CARTESIAN_POINT ( 'NONE',  ( 23.32150899776524966, 40.83761553963523028, 60.74500979864502881 ) ) ;
#84868=CARTESIAN_POINT ( 'NONE',  ( -12.50000000000000000, -3.000000000000003109, -14.34180675897363599 ) ) ;
#84869=EDGE_CURVE ( 'NONE', #24875, #8448, #6507, .T. ) ;
#84878=CARTESIAN_POINT ( 'NONE',  ( -8.737863883542575039, 48.00000000000000000, -90.03618980370900715 ) ) ;
#84893=CARTESIAN_POINT ( 'NONE',  ( -6.455412923701131511, 41.05104862138563249, -71.04266226920890404 ) ) ;
#84927=CARTESIAN_POINT ( 'NONE',  ( -29.08775742405871867, 43.32034978114150903, -70.51094494232118848 ) ) ;
#84940=CARTESIAN_POINT ( 'NONE',  ( 12.22950890273489755, -4.580576956131391597, -12.66933385000445611 ) ) ;
#84942=CARTESIAN_POINT ( 'NONE',  ( -7.500000000000003553, -3.000000000000000888, -36.97043916959992771 ) ) ;
#84946=CARTESIAN_POINT ( 'NONE',  ( -17.11334244688239536, -4.333298119783949964, -5.314533759433560434 ) ) ;
#84956=CARTESIAN_POINT ( 'NONE',  ( -50.94745919686192082, 50.00000000000000000, -37.05882352941185331 ) ) ;
#84957=SURFACE_SIDE_STYLE ('',( #18660 ) ) ;
#84995=CARTESIAN_POINT ( 'NONE',  ( 4.966176485634620441, 41.64999999999997726, -70.47555195150160046 ) ) ;
#84996=CARTESIAN_POINT ( 'NONE',  ( 58.76133767613618630, 50.00000000000000000, 23.44026136864407306 ) ) ;
#85039=CARTESIAN_POINT ( 'NONE',  ( 1.570796324976846403, 50.00000000000000000, -73.00000000000001421 ) ) ;
#85080=CARTESIAN_POINT ( 'NONE',  ( -48.44486512746869522, 38.95340677903534754, -41.63464568442791602 ) ) ;
#85101=CARTESIAN_POINT ( 'NONE',  ( 10.47796581435196472, 50.00000000000001421, -78.93819186518393849 ) ) ;
#85117=CARTESIAN_POINT ( 'NONE',  ( -6.921856738059537051, 41.59435685020018525, -70.13580383255585105 ) ) ;
#85119=CARTESIAN_POINT ( 'NONE',  ( 7.500000000000007105, 39.99999999999998579, -68.91429205785453860 ) ) ;
#85123=CARTESIAN_POINT ( 'NONE',  ( -6.578491659837745864, 41.30621945901641112, -58.38226164895504411 ) ) ;
#85138=CARTESIAN_POINT ( 'NONE',  ( 6.771436162406291537, 41.75941402238878197, -59.18670940897492727 ) ) ;
#85139=CARTESIAN_POINT ( 'NONE',  ( 37.36680950585426331, 18.64316884707256605, -10.04205104291870398 ) ) ;
#85147=CARTESIAN_POINT ( 'NONE',  ( 6.736687879933906942, 41.36687664139658693, -58.48851407026759830 ) ) ;
#85148=CARTESIAN_POINT ( 'NONE',  ( -7.500000000000008882, 42.00000000000000711, -72.67206406577980715 ) ) ;
#85154=( NAMED_UNIT ( * ) SI_UNIT ( $, .STERADIAN. ) SOLID_ANGLE_UNIT ( ) );
#85189=CARTESIAN_POINT ( 'NONE',  ( 9.937561876413942841, -5.000000000000002665, -76.56466736914200055 ) ) ;
#85228=CARTESIAN_POINT ( 'NONE',  ( 8.737863884125493641, -3.000000000000002665, -79.96381019769830800 ) ) ;
#85239=CARTESIAN_POINT ( 'NONE',  ( -7.012902693339047921, -4.999999999999998224, 16.13291991228729572 ) ) ;
#85262=CARTESIAN_POINT ( 'NONE',  ( 19.49496444267845519, 49.99961719514236336, 60.01447535217918983 ) ) ;
#85270=CARTESIAN_POINT ( 'NONE',  ( -12.34835181856066555, -4.332967528434497062, -12.86601580078907148 ) ) ;
#85273=( NAMED_UNIT ( * ) SI_UNIT ( $, .STERADIAN. ) SOLID_ANGLE_UNIT ( ) );
#85285=CARTESIAN_POINT ( 'NONE',  ( -19.07987706826217789, 49.64660923895987565, 61.77383235656444072 ) ) ;
#85286=CARTESIAN_POINT ( 'NONE',  ( -7.039599673380882550, 41.52217312180329856, -58.93052077570905567 ) ) ;
#85287=CARTESIAN_POINT ( 'NONE',  ( 5.273744720368365613, 41.55406131380648560, -70.69180554715100584 ) ) ;
#85308=CARTESIAN_POINT ( 'NONE',  ( -9.596002107494335576, -5.000000000000002665, -92.37456064099097830 ) ) ;
#85310=( GEOMETRIC_REPRESENTATION_CONTEXT ( 3 ) GLOBAL_UNCERTAINTY_ASSIGNED_CONTEXT ( ( #10953 ) ) GLOBAL_UNIT_ASSIGNED_CONTEXT ( ( #79380, #30325, #22242 ) ) REPRESENTATION_CONTEXT ( 'NONE', 'WORKASPACE' ) );
#85331=CARTESIAN_POINT ( 'NONE',  ( 17.34830914839334781, 18.64284798592843373, 34.29224544877874337 ) ) ;
#85349=CARTESIAN_POINT ( 'NONE',  ( 2.040829700809986047, 50.00000000000000000, -98.00000000000000000 ) ) ;
#85356=CARTESIAN_POINT ( 'NONE',  ( 18.97029851426021096, 49.42830426956580681, 61.97293826772167336 ) ) ;
#85376=CARTESIAN_POINT ( 'NONE',  ( -15.50526908257195835, 42.00000000000000000, -57.69562748404377572 ) ) ;
#85377=EDGE_CURVE ( 'NONE', #31057, #105843, #189, .T. ) ;
#85386=ADVANCED_FACE ( 'NONE', ( #6185 ), #70563, .T. ) ;
#85403=CARTESIAN_POINT ( 'NONE',  ( -10.48543666094731464, 50.00000000000000000, -91.04342776276725147 ) ) ;
#85414=CARTESIAN_POINT ( 'NONE',  ( -9.999999999999994671, 48.00000000000000000, -86.30899693899574743 ) ) ;
#85416=CARTESIAN_POINT ( 'NONE',  ( -5.500000000000006217, 42.00000000000000000, -59.88032989329961708 ) ) ;
#85422=ORIENTED_EDGE ( 'NONE', *, *, #67133, .T. ) ;
#85428=CARTESIAN_POINT ( 'NONE',  ( -4.852941176476488927, 40.28748004600674903, -70.80672828634432392 ) ) ;
#85461=CARTESIAN_POINT ( 'NONE',  ( -31.76732676843110781, 43.01778740796270029, -66.82714613718027863 ) ) ;
#85465=ADVANCED_FACE ( 'NONE', ( #38466 ), #20940, .T. ) ;
#85486=B_SPLINE_CURVE_WITH_KNOTS ( 'NONE', 3,
 ( #48715, #56266, #57335, #81092, #90258, #71951, #96769, #105383, #16360, #7730, #15302, #71408, #22376, #40113, #79510, #38543, #89203, #5620 ),
 .UNSPECIFIED., .F., .F.,
 ( 4, 2, 2, 2, 2, 2, 2, 2, 4 ),
 ( 0.5000000000001136868, 0.5625000000000994760, 0.6250000000000852651, 0.6875000000000711653, 0.7500000000000569544, 0.8125000000000427436, 0.8750000000000284217, 0.9375000000000142109, 1.000000000000000000 ),
 .UNSPECIFIED. ) ;
#85491=CARTESIAN_POINT ( 'NONE',  ( 6.123233995736763324E-16, 48.00000000000000000, -75.00000000000001421 ) ) ;
#85494=CARTESIAN_POINT ( 'NONE',  ( 8.737863883542575039, -3.000000000000003109, -90.03618980370902136 ) ) ;
#85497=CARTESIAN_POINT ( 'NONE',  ( -37.46929538816834793, 50.00000000000000000, -55.58823529411764497 ) ) ;
#85504=CARTESIAN_POINT ( 'NONE',  ( -5.767825830945890964, 42.00032026480481306, -59.73203846925512295 ) ) ;
#85514=EDGE_LOOP ( 'NONE', ( #89842, #102817, #3038, #5305, #98954, #47601 ) ) ;
#85528=EDGE_LOOP ( 'NONE', ( #38731, #2457 ) ) ;
#85529=B_SPLINE_CURVE_WITH_KNOTS ( 'NONE', 3,
 ( #14901, #29042, #20949, #103921, #62425, #38173, #22517, #13311, #30069, #12782, #94802, #96389, #47796, #71548, #70512 ),
 .UNSPECIFIED., .F., .F.,
 ( 4, 1, 1, 1, 1, 1, 1, 1, 2, 2, 4 ),
 ( 0.000000000000000000, 0.2500000000003557155, 0.3750000000005364043, 0.4375000000006320500, 0.4687500000006805667, 0.4843750000006981082, 0.4921875000007118750, 0.4960937500007114864, 0.4980468750007052692, 0.5000000000006989964, 1.000000000000000000 ),
 .UNSPECIFIED. ) ;
#85537=CARTESIAN_POINT ( 'NONE',  ( 5.788218731899625880, 41.97741539037772895, -69.85767741758428429 ) ) ;
#85539=CARTESIAN_POINT ( 'NONE',  ( 63.25915952246698026, 50.00000000000000000, 0.7870165385177050332 ) ) ;
#85550=UNCERTAINTY_MEASURE_WITH_UNIT (LENGTH_MEASURE( 1.000000000000000082E-05 ), #100301, 'distance_accuracy_value', 'NONE');
#85554=AXIS2_PLACEMENT_3D ( 'NONE', #70619, #102986, #94913 ) ;
#85564=CARTESIAN_POINT ( 'NONE',  ( 18.91791044776121211, 45.90000000000000568, 62.18611311450882795 ) ) ;
#85567=CARTESIAN_POINT ( 'NONE',  ( 23.97397358239886600, 41.62137230726112591, -74.34129542729060347 ) ) ;
#85583=CARTESIAN_POINT ( 'NONE',  ( 23.99113157954623432, 50.00000000000000000, -74.11764705887551941 ) ) ;
#85610=CARTESIAN_POINT ( 'NONE',  ( -5.293142421612902382, 18.41054814049272892, -37.78857195590732942 ) ) ;
#85625=CARTESIAN_POINT ( 'NONE',  ( 7.101747359470936161, -4.047770588429664862, -17.37629258577382885 ) ) ;
#85633=EDGE_LOOP ( 'NONE', ( #19345, #53951, #62897, #61970, #50046 ) ) ;
#85644=CARTESIAN_POINT ( 'NONE',  ( 4.046285834744535848, 49.99999999999999289, -97.52808355545833763 ) ) ;
#85664=CARTESIAN_POINT ( 'NONE',  ( -5.313746993492887150, 41.99394904787047977, -69.45902141694074317 ) ) ;
#85668=CARTESIAN_POINT ( 'NONE',  ( 15.92648127229067612, -5.000000000000000000, 4.023271965934163141 ) ) ;
#85669=CARTESIAN_POINT ( 'NONE',  ( -12.13034742782427777, 41.99999999999999289, -93.82352941176471006 ) ) ;
#85686=SURFACE_STYLE_USAGE ( .BOTH. , #105949 ) ;
#85687=CARTESIAN_POINT ( 'NONE',  ( 6.678340154126256145, 41.85887555562482021, -59.41504759784768908 ) ) ;
#85688=CARTESIAN_POINT ( 'NONE',  ( -1.905220702120325443E-14, 42.00000000000000711, -59.23741894013591036 ) ) ;
#85690=CARTESIAN_POINT ( 'NONE',  ( 0.000000000000000000, 50.00000000000000000, 0.000000000000000000 ) ) ;
#85698=CARTESIAN_POINT ( 'NONE',  ( 7.070595415630159586, 41.16321656043108135, -58.51508817460690182 ) ) ;
#85729=CARTESIAN_POINT ( 'NONE',  ( -14.75116205827941940, 43.55504283738518723, -90.22050498381219086 ) ) ;
#85739=B_SPLINE_CURVE_WITH_KNOTS ( 'NONE', 3,
 ( #100186, #66766, #86032, #36956, #16613, #99652, #99106, #25823, #18232, #9039 ),
 .UNSPECIFIED., .F., .F.,
 ( 4, 2, 2, 2, 4 ),
 ( 0.000000000000000000, 0.5000000000000000000, 0.7500000000000000000, 0.8750000000000000000, 1.000000000000000000 ),
 .UNSPECIFIED. ) ;
#85744=CARTESIAN_POINT ( 'NONE',  ( -15.17227823171696954, -5.000000000000002665, -86.54073391196325815 ) ) ;
#85745=CARTESIAN_POINT ( 'NONE',  ( 12.49986889690059222, -3.000000000000002665, -76.70852482682694529 ) ) ;
#85785=CARTESIAN_POINT ( 'NONE',  ( 7.439138809193584834, 41.00331669213974806, -59.84461289586582922 ) ) ;
#85794=EDGE_CURVE ( 'NONE', #78701, #67484, #33472, .T. ) ;
#85796=CARTESIAN_POINT ( 'NONE',  ( -9.479859806997659177, -5.000000000000000000, -13.37835090744192001 ) ) ;
#85817=CARTESIAN_POINT ( 'NONE',  ( 5.693345022498909280, -2.999999999999138467, -71.09407784968016131 ) ) ;
#85842=CARTESIAN_POINT ( 'NONE',  ( -19.16002095161153918, 49.73805339712912144, 61.63562287024812036 ) ) ;
#85843=FILL_AREA_STYLE_COLOUR ( '', #14343 ) ;
#85844=CARTESIAN_POINT ( 'NONE',  ( 6.040960808745679422, 41.48433375008082180, -70.81801795692170742 ) ) ;
#85858=CARTESIAN_POINT ( 'NONE',  ( 5.254776564415823081, 11.34081578130501811, -31.40351826358976695 ) ) ;
#85876=FILL_AREA_STYLE ('',( #52948 ) ) ;
#85891=CARTESIAN_POINT ( 'NONE',  ( 9.743117168495814440, -5.000000000000000000, 2.583982984168559316 ) ) ;
#85917=CARTESIAN_POINT ( 'NONE',  ( 34.86657997040038737, 42.62263848107266995, -62.56637741842270373 ) ) ;
#85929=CARTESIAN_POINT ( 'NONE',  ( -36.40416150961017649, 41.99999999999999289, 47.37019975558912677 ) ) ;
#85937=CARTESIAN_POINT ( 'NONE',  ( 65.26569490341492497, 40.83736746500258619, 0.7620991476189149516 ) ) ;
#85955=CARTESIAN_POINT ( 'NONE',  ( 11.68767211932355998, 50.00000000000000000, -88.14097461399491351 ) ) ;
#85981=CARTESIAN_POINT ( 'NONE',  ( -6.812288195523935386, 40.56150966584056761, -71.12586875364199557 ) ) ;
#85993=CARTESIAN_POINT ( 'NONE',  ( -17.58856438785635490, 45.00000000000000711, 63.14100056368219782 ) ) ;
#86028=CARTESIAN_POINT ( 'NONE',  ( 11.60416385448452203, -4.915838321100066466, -12.56281314056613674 ) ) ;
#86032=CARTESIAN_POINT ( 'NONE',  ( -7.069742149889169269, 41.66287055432060527, -69.58314084294495672 ) ) ;
#86043=CARTESIAN_POINT ( 'NONE',  ( 60.62677696746332145, 48.00000000000000000, 24.18439665019722540 ) ) ;
#86048=CARTESIAN_POINT ( 'NONE',  ( -6.294744146068734558, 41.94828263137729607, -59.44631356406647882 ) ) ;
#86071=CARTESIAN_POINT ( 'NONE',  ( 62.95715931499727702, 49.99999999999999289, 4.917584479073736858 ) ) ;
#86079=EDGE_LOOP ( 'NONE', ( #40020, #4523, #46692, #79067 ) ) ;
#86081=CARTESIAN_POINT ( 'NONE',  ( 5.129365358145452802, 41.91296950070222493, -69.99827769498368468 ) ) ;
#86105=( NAMED_UNIT ( * ) SI_UNIT ( $, .STERADIAN. ) SOLID_ANGLE_UNIT ( ) );
#86107=CARTESIAN_POINT ( 'NONE',  ( 36.45193875802095107, 40.26000571314290255, -57.68880871784696751 ) ) ;
#86147=EDGE_CURVE ( 'NONE', #7244, #58869, #31921, .T. ) ;
#86168=( NAMED_UNIT ( * ) SI_UNIT ( $, .STERADIAN. ) SOLID_ANGLE_UNIT ( ) );
#86171=CARTESIAN_POINT ( 'NONE',  ( 18.91781669292794987, 48.00000000000000000, 62.18610382930901892 ) ) ;
#86191=CARTESIAN_POINT ( 'NONE',  ( 9.609938133605346877, 50.00000000000000000, -77.63956163932782317 ) ) ;
#86212=CARTESIAN_POINT ( 'NONE',  ( -6.426572956751082977, 41.32129836830301173, -58.37301679283319800 ) ) ;
#86228=PRESENTATION_STYLE_ASSIGNMENT (( #85686 ) ) ;
#86230=CARTESIAN_POINT ( 'NONE',  ( 7.149999999999998579, 41.65000000000000568, -59.82695526683419729 ) ) ;
#86231=CARTESIAN_POINT ( 'NONE',  ( -15.50526908267491066, 41.99999999999999289, 57.69562748408483088 ) ) ;
#86235=VERTEX_POINT ( 'NONE', #57121 ) ;
#86256=CARTESIAN_POINT ( 'NONE',  ( 7.176538911681105581, 40.00000000337644224, -70.93639500526144559 ) ) ;
#86278=CARTESIAN_POINT ( 'NONE',  ( -11.90609530896320045, -5.000000000000002665, -79.26133957281672338 ) ) ;
#86279=CARTESIAN_POINT ( 'NONE',  ( 17.91929324317266037, -4.333298119783741242, -0.09842992273139013204 ) ) ;
#86295=VERTEX_POINT ( 'NONE', #74370 ) ;
#86317=VERTEX_POINT ( 'NONE', #100778 ) ;
#86327=CARTESIAN_POINT ( 'NONE',  ( -8.812315315237404079, -5.000000000000578204, -14.88097931263728313 ) ) ;
#86352=CARTESIAN_POINT ( 'NONE',  ( 19.48449119670739549, 49.99674463650651290, 60.21304372869956012 ) ) ;
#86364=CARTESIAN_POINT ( 'NONE',  ( -7.500000000000004441, 23.94542680926433320, -45.46585527945179450 ) ) ;
#86376=CARTESIAN_POINT ( 'NONE',  ( -18.93379861527105135, 49.15505328154679887, 62.08065835375955288 ) ) ;
#86377=( NAMED_UNIT ( * ) PLANE_ANGLE_UNIT ( ) SI_UNIT ( $, .RADIAN. ) );
#86378=CARTESIAN_POINT ( 'NONE',  ( 5.563666575369232703, 41.08730259753766489, -70.97074977071341095 ) ) ;
#86392=CARTESIAN_POINT ( 'NONE',  ( -6.990291106834061630, -2.999999999999999556, -4.028951842967198438 ) ) ;
#86396=CARTESIAN_POINT ( 'NONE',  ( -2.617478844990583031, -3.000000000000002665, -94.73972676610416954 ) ) ;
#86406=EDGE_CURVE ( 'NONE', #9002, #81288, #42937, .T. ) ;
#86426=CARTESIAN_POINT ( 'NONE',  ( 1.517883041479706208E-15, -5.000000000000000888, -97.00000000000000000 ) ) ;
#86437=CARTESIAN_POINT ( 'NONE',  ( -12.13034742782428133, 49.99999999999999289, -93.82352941176471006 ) ) ;
#86455=ORIENTED_EDGE ( 'NONE', *, *, #64377, .T. ) ;
#86466=CARTESIAN_POINT ( 'NONE',  ( -37.36680950590233863, 18.64316884713579725, 10.04205104295027517 ) ) ;
#86475=CARTESIAN_POINT ( 'NONE',  ( -56.10217589899048107, 39.42619182724450866, -33.37224010391948781 ) ) ;
#86492=CARTESIAN_POINT ( 'NONE',  ( 11.68767211932491712, 50.00000000000000000, -81.85902538600508649 ) ) ;
#86502=CARTESIAN_POINT ( 'NONE',  ( -7.996668423981797780, 47.99999999999999289, -78.85453280025085121 ) ) ;
#86509=( NAMED_UNIT ( * ) SI_UNIT ( $, .STERADIAN. ) SOLID_ANGLE_UNIT ( ) );
#86517=CARTESIAN_POINT ( 'NONE',  ( -6.190137073498123144, 41.32597146626896034, -70.92513718978732129 ) ) ;
#86529=CARTESIAN_POINT ( 'NONE',  ( -17.53252671428359477, 45.00000000000000000, 63.43329252951189545 ) ) ;
#86549=CARTESIAN_POINT ( 'NONE',  ( 7.010778207173779641, 41.61257717850156013, -59.09056268933341727 ) ) ;
#86568=CARTESIAN_POINT ( 'NONE',  ( -6.876313068558442154, -4.333298119783861146, 16.54772121373820326 ) ) ;
#86577=CARTESIAN_POINT ( 'NONE',  ( 11.54772599577024295, 50.00000000000000000, 62.20121126512098186 ) ) ;
#86583=CARTESIAN_POINT ( 'NONE',  ( -6.771436230215871710, 41.75941352900127157, -59.18670869008018087 ) ) ;
#86587=EDGE_CURVE ( 'NONE', #54991, #94321, #13940, .T. ) ;
#86594=CARTESIAN_POINT ( 'NONE',  ( 18.07381427182019706, 50.00000000000000000, 61.79284943879029157 ) ) ;
#86617=CARTESIAN_POINT ( 'NONE',  ( 5.504993149140188002, 41.95607710206238039, -69.87068889203474953 ) ) ;
#86637=CARTESIAN_POINT ( 'NONE',  ( 17.50000000000002487, 44.85000000000000853, 62.61746187599675295 ) ) ;
#86639=CARTESIAN_POINT ( 'NONE',  ( 33.09872316835808448, 40.69672373397799703, -62.13666886876760032 ) ) ;
#86655=CARTESIAN_POINT ( 'NONE',  ( 9.739726766104286781, 48.00000000000000000, -82.38252115500969808 ) ) ;
#86669=EDGE_CURVE ( 'NONE', #22777, #70585, #53942, .T. ) ;
#86696=CARTESIAN_POINT ( 'NONE',  ( -18.83251367839346457, 50.00000000000000000, 60.81264960944136533 ) ) ;
#86710=( LENGTH_UNIT ( ) NAMED_UNIT ( * ) SI_UNIT ( .MILLI., .METRE. ) );
#86735=CARTESIAN_POINT ( 'NONE',  ( 15.35331269684644617, -5.000000000000000000, -5.840831470021132787 ) ) ;
#86736=CARTESIAN_POINT ( 'NONE',  ( -6.526057575926256682, 41.69808020043258523, -58.86835240465277508 ) ) ;
#86757=CARTESIAN_POINT ( 'NONE',  ( 6.780292695530274472, 41.80198870715022252, -59.33023448964987523 ) ) ;
#86758=CARTESIAN_POINT ( 'NONE',  ( -59.23741894013591036, 42.00000000000000711, -7.754160006507100356 ) ) ;
#86764=B_SPLINE_CURVE_WITH_KNOTS ( 'NONE', 3,
 ( #44625, #77513, #3626, #45679, #69951, #12226, #94776, #45156 ),
 .UNSPECIFIED., .F., .F.,
 ( 4, 2, 2, 4 ),
 ( 0.000000000000000000, 0.5000000000000000000, 0.7500000000000000000, 1.000000000000000000 ),
 .UNSPECIFIED. ) ;
#86786=CARTESIAN_POINT ( 'NONE',  ( 7.321078409834592904, 40.29402549786116339, -70.66288766115398801 ) ) ;
#86791=CARTESIAN_POINT ( 'NONE',  ( -10.67808697576670873, -5.000000000000000888, -77.27709671284311810 ) ) ;
#86804=CARTESIAN_POINT ( 'NONE',  ( -12.76706325321399049, -5.000000000000002665, -81.58101990454278507 ) ) ;
#86805=CARTESIAN_POINT ( 'NONE',  ( 15.83991689176772866, -4.333298119783770552, 8.379008989516183448 ) ) ;
#86810=FILL_AREA_STYLE_COLOUR ( '', #53098 ) ;
#86832=( NAMED_UNIT ( * ) PLANE_ANGLE_UNIT ( ) SI_UNIT ( $, .RADIAN. ) );
#86871=CARTESIAN_POINT ( 'NONE',  ( 19.45280783995336193, 49.97908042910276549, 60.60017717165798246 ) ) ;
#86892=VERTEX_POINT ( 'NONE', #93131 ) ;
#86897=CARTESIAN_POINT ( 'NONE',  ( 6.208655437490365969, 40.93126392761964638, -71.11611063721394999 ) ) ;
#86900=CARTESIAN_POINT ( 'NONE',  ( 12.50000000000000533, -3.000000000000000000, -55.73109925765190553 ) ) ;
#86913=CARTESIAN_POINT ( 'NONE',  ( 5.293242423775784466, 18.43190769382419703, -37.80783146079790669 ) ) ;
#86918=CARTESIAN_POINT ( 'NONE',  ( -9.739726766101606259, -5.000000000000002665, -82.38252115500968387 ) ) ;
#86948=CARTESIAN_POINT ( 'NONE',  ( 8.716351559230176349, -4.999999999999999112, 5.062179317057519334 ) ) ;
#86954=CARTESIAN_POINT ( 'NONE',  ( -5.363597346089342466, 41.33266196706077267, -58.39526881795508473 ) ) ;
#86960=CARTESIAN_POINT ( 'NONE',  ( 9.312033689592260188, 50.00000000000000000, -94.29807022305527653 ) ) ;
#86982=CARTESIAN_POINT ( 'NONE',  ( -10.04205104296119622, 18.64316884715858080, 37.36680950591986772 ) ) ;
#86990=CARTESIAN_POINT ( 'NONE',  ( -5.921793164125095821, 39.42528690638199862, 64.79870964707900782 ) ) ;
#87008=CARTESIAN_POINT ( 'NONE',  ( 1.308996937483428491, 49.99999999999999289, -95.00000000000001421 ) ) ;
#87021=CARTESIAN_POINT ( 'NONE',  ( 9.499926694067500677, -5.000000000000000888, -20.04229455990067166 ) ) ;
#87037=CARTESIAN_POINT ( 'NONE',  ( -5.225680118539934860, 40.98154234353523151, -70.87362174390516145 ) ) ;
#87064=CARTESIAN_POINT ( 'NONE',  ( 7.081808280621250340, 41.46696771993406827, -58.88886753944292707 ) ) ;
#87078=CARTESIAN_POINT ( 'NONE',  ( 11.74288065822411831, -4.879695075740994703, -12.55922237203875191 ) ) ;
#87095=CARTESIAN_POINT ( 'NONE',  ( -28.00203968317432057, 50.00000000000000000, 56.72941417029706201 ) ) ;
#87102=CARTESIAN_POINT ( 'NONE',  ( -6.846707577100250575, 41.84866040025745093, -59.70429183036502252 ) ) ;
#87104=CARTESIAN_POINT ( 'NONE',  ( 10.50000000000000711, -5.000000000000000000, -77.33514508527181874 ) ) ;
#87119=CARTESIAN_POINT ( 'NONE',  ( -5.500000000000007994, 42.00000000000000000, -68.91429205818155879 ) ) ;
#87121=CARTESIAN_POINT ( 'NONE',  ( 45.43595897156877328, 50.00000000000001421, 43.65914459177244566 ) ) ;
#87136=CARTESIAN_POINT ( 'NONE',  ( 12.50000000000000178, -3.000000000000001332, -35.13068384735336736 ) ) ;
#87152=CARTESIAN_POINT ( 'NONE',  ( 17.50000000000002132, 44.85000000000000853, 64.09953197957062798 ) ) ;
#87174=FACE_OUTER_BOUND ( 'NONE', #9647, .T. ) ;
#87197=CARTESIAN_POINT ( 'NONE',  ( -5.105409892807596606, -2.846581877981202879, -18.47267145302658164 ) ) ;
#87201=PLANE ( 'NONE',  #30991 ) ;
#87211=CARTESIAN_POINT ( 'NONE',  ( -52.56483885390523625, 40.83906611473335602, -38.23529411764705088 ) ) ;
#87212=CARTESIAN_POINT ( 'NONE',  ( -17.96390936993321930, 50.00000000000000000, 61.93590888982013354 ) ) ;
#87240=CARTESIAN_POINT ( 'NONE',  ( -10.50000000000000178, -5.000000000000000000, -34.12705335493774328 ) ) ;
#87252=EDGE_LOOP ( 'NONE', ( #12918, #89187, #80076, #101502 ) ) ;
#87254=CARTESIAN_POINT ( 'NONE',  ( -6.075687308901098760, 41.99394926078448265, -68.91429205814512216 ) ) ;
#87260=CARTESIAN_POINT ( 'NONE',  ( -5.897540648542782371, 41.82858959817294675, -58.91931066433214426 ) ) ;
#87277=CARTESIAN_POINT ( 'NONE',  ( 29.83308852626540641, 42.00000000008230927, -51.76085035116526711 ) ) ;
#87308=CARTESIAN_POINT ( 'NONE',  ( -12.23812927463290023, -4.553267922722016081, -76.78892216552449668 ) ) ;
#87326=CARTESIAN_POINT ( 'NONE',  ( -9.937561876414743978, -5.000000000000002665, -76.56466736914423166 ) ) ;
#87361=CARTESIAN_POINT ( 'NONE',  ( 8.369914041613107258, 42.00000000000000000, -59.54702718917638293 ) ) ;
#87374=( BOUNDED_SURFACE ( )  B_SPLINE_SURFACE ( 2, 3, ( 
 ( #87152, #19796, #62352, #103845 ),
 ( #86637, #28958, #54750, #37569 ),
 ( #67374, #85564, #77460, #45630 ) ),
 .UNSPECIFIED., .F., .F., .T. ) 
 B_SPLINE_SURFACE_WITH_KNOTS ( ( 3, 3 ),
 ( 4, 4 ),
 ( 0.000000000000000000, 1.000000000000000000 ),
 ( 0.04485000000000000792, 0.04800000000000000100 ),
 .UNSPECIFIED. ) 
 GEOMETRIC_REPRESENTATION_ITEM ( )  RATIONAL_B_SPLINE_SURFACE ( (
 ( 1.000000000000000000, 1.000000000000000000, 1.000000000000000000, 1.000000000000000000),
 ( 1.857142857142858317, 1.857142857142858317, 1.857142857142858317, 1.857142857142858317),
 ( 1.000000000000000000, 1.000000000000000000, 1.000000000000000000, 1.000000000000000000) ) ) 
 REPRESENTATION_ITEM ( '' )  SURFACE ( )  );
#87402=CARTESIAN_POINT ( 'NONE',  ( 18.91781669292794987, 48.00000000000000000, 62.18610382930901892 ) ) ;
#87425=CARTESIAN_POINT ( 'NONE',  ( -19.47898085236668919, 49.99431953961255459, 60.29633468442251854 ) ) ;
#87427=CARTESIAN_POINT ( 'NONE',  ( 5.211029210576866078, 40.56334907184437810, -70.92280024200073285 ) ) ;
#87430=CARTESIAN_POINT ( 'NONE',  ( 12.50000000000000000, -3.000000000000000000, -11.21398294031086706 ) ) ;
#87440=CARTESIAN_POINT ( 'NONE',  ( 5.221666942817044799, 7.014479873995792758, -27.48209584563044316 ) ) ;
#87441=CARTESIAN_POINT ( 'NONE',  ( 4.205882352941182845, -5.000000000000000000, -72.69916451482998809 ) ) ;
#87445=CARTESIAN_POINT ( 'NONE',  ( 7.996668422910687468, -3.000000000000002665, -91.14546720082027775 ) ) ;
#87447=SURFACE_STYLE_FILL_AREA ( #30823 ) ;
#87459=CARTESIAN_POINT ( 'NONE',  ( -25.52709155447669076, 43.61749475787997454, -75.40605120386278770 ) ) ;
#87461=ORIENTED_EDGE ( 'NONE', *, *, #100790, .F. ) ;
#87471=MECHANICAL_DESIGN_GEOMETRIC_PRESENTATION_REPRESENTATION('',(#94398),#16867);
#87488=CARTESIAN_POINT ( 'NONE',  ( 7.054522925320324767, 41.71556257522360767, -59.55896313260247865 ) ) ;
#87506=CARTESIAN_POINT ( 'NONE',  ( -38.36535705883633085, 18.64316884711714195, -5.022013495247519721 ) ) ;
#87513=CARTESIAN_POINT ( 'NONE',  ( -63.23885718349010432, 38.95363886516651775, -7.929982538254300550 ) ) ;
#87529=CARTESIAN_POINT ( 'NONE',  ( -1.308996937483426715, 48.00000000000000000, -95.00000000000000000 ) ) ;
#87535=CARTESIAN_POINT ( 'NONE',  ( 3.294249609603385309, 39.99999999999999289, -70.27378291343094929 ) ) ;
#87541=CONICAL_SURFACE ( 'NONE', #39341, 18.72828050308589454, 0.7292773806962717931 ) ;
#87543=CARTESIAN_POINT ( 'NONE',  ( 0.000000000000000000, 0.000000000000000000, 0.000000000000000000 ) ) ;
#87545=CARTESIAN_POINT ( 'NONE',  ( 8.678535172863940161, -4.999999999999999112, -16.67878089796255381 ) ) ;
#87590=CARTESIAN_POINT ( 'NONE',  ( 6.943035990376878352, 41.50417910381163011, -58.81491866537869129 ) ) ;
#87591=ADVANCED_FACE ( 'NONE', ( #9996 ), #65174, .T. ) ;
#87610=CARTESIAN_POINT ( 'NONE',  ( 7.500000000000007105, 40.00000000000000000, -62.89165061482969321 ) ) ;
#87611=ORIENTED_EDGE ( 'NONE', *, *, #72484, .T. ) ;
#87620=( GEOMETRIC_REPRESENTATION_CONTEXT ( 3 ) GLOBAL_UNCERTAINTY_ASSIGNED_CONTEXT ( ( #25807 ) ) GLOBAL_UNIT_ASSIGNED_CONTEXT ( ( #106682, #65168, #33898 ) ) REPRESENTATION_CONTEXT ( 'NONE', 'WORKASPACE' ) );
#87623=CARTESIAN_POINT ( 'NONE',  ( -5.957442974701830707, 49.99999999999999289, 65.00000000000000000 ) ) ;
#87627=CARTESIAN_POINT ( 'NONE',  ( 12.13955930136260442, -4.660274349647991698, -76.81824564200809391 ) ) ;
#87635=CARTESIAN_POINT ( 'NONE',  ( 19.14172393082469981, 50.00000000000001421, 60.39347634864844849 ) ) ;
#87649=CARTESIAN_POINT ( 'NONE',  ( 56.29065232361070059, 49.99999999999999289, -28.72822482865823801 ) ) ;
#87709=EDGE_LOOP ( 'NONE', ( #56821, #89082, #43708, #88100 ) ) ;
#87715=ORIENTED_EDGE ( 'NONE', *, *, #38965, .F. ) ;
#87724=CARTESIAN_POINT ( 'NONE',  ( 4.175893272575848414, -4.999999999999998224, 7.137815226408912750 ) ) ;
#87729=CARTESIAN_POINT ( 'NONE',  ( -5.182201362424698310, 2.673072912720999561, -23.53106308636114008 ) ) ;
#87731=DIRECTION ( 'NONE',  ( 1.160749806054361473E-16, 0.000000000000000000, -1.000000000000000000 ) ) ;
#87744=CARTESIAN_POINT ( 'NONE',  ( -28.55298245902970677, 43.39596509286685944, -71.24613896942491920 ) ) ;
#87745=CARTESIAN_POINT ( 'NONE',  ( -18.20729755737727373, 50.00000000000000000, 61.62669174679179918 ) ) ;
#87753=PRESENTATION_STYLE_ASSIGNMENT (( #54823 ) ) ;
#87770=CARTESIAN_POINT ( 'NONE',  ( 7.069742150690448312, 41.66287055390499461, -69.58314084581829206 ) ) ;
#87780=CARTESIAN_POINT ( 'NONE',  ( -5.625019081819781164, 41.66287055468434630, -70.61600276915974916 ) ) ;
#87841=CARTESIAN_POINT ( 'NONE',  ( -12.13034742782428133, 42.00000299511174973, -93.82352941176471006 ) ) ;
#87845=ADVANCED_FACE ( 'NONE', ( #78846 ), #39048, .T. ) ;
#87860=CARTESIAN_POINT ( 'NONE',  ( 8.922269033012840467, -5.000000000000000000, 5.219866590718108768 ) ) ;
#87865=( NAMED_UNIT ( * ) SI_UNIT ( $, .STERADIAN. ) SOLID_ANGLE_UNIT ( ) );
#87899=CARTESIAN_POINT ( 'NONE',  ( 14.22021666642421955, -5.000000000000000000, 8.714242330525232560 ) ) ;
#87914=COLOUR_RGB ( '', 0.08235294, 0.09019608, 0.10196078) ;
#87923=CARTESIAN_POINT ( 'NONE',  ( 19.45330446674461911, 49.97940989288292002, 60.59551982431160866 ) ) ;
#87946=CARTESIAN_POINT ( 'NONE',  ( -19.44925841602305283, 49.97667730683129861, 60.63295307910983922 ) ) ;
#87953=CARTESIAN_POINT ( 'NONE',  ( 12.49955057316562090, -4.332870170068738425, -12.71907580248059233 ) ) ;
#87972=CARTESIAN_POINT ( 'NONE',  ( -1.308996937480702005, -3.000000000000002665, -95.00000000000000000 ) ) ;
#87982=CARTESIAN_POINT ( 'NONE',  ( 5.692357205178650403, -4.313020517866006820, -16.93296622886375147 ) ) ;
#87984=CARTESIAN_POINT ( 'NONE',  ( -26.92780252270988939, 43.51495311933407351, -73.48039199225773643 ) ) ;
#87997=CARTESIAN_POINT ( 'NONE',  ( -64.91565662652770641, 40.83906611473043569, 6.815324757234163755 ) ) ;
#88023=CARTESIAN_POINT ( 'NONE',  ( 34.55566962155668875, 42.66456075483809229, -62.99380848079916007 ) ) ;
#88035=CARTESIAN_POINT ( 'NONE',  ( 38.36535705883633085, 18.64316884711714550, -5.022013495247578341 ) ) ;
#88042=CARTESIAN_POINT ( 'NONE',  ( 63.17898818519600468, 39.42583325260841320, 15.56321689764842908 ) ) ;
#88059=CARTESIAN_POINT ( 'NONE',  ( -8.737863884121431113, 48.00000000000000000, -79.96381019768850251 ) ) ;
#88075=CARTESIAN_POINT ( 'NONE',  ( 9.339269934323091604, -5.000000000000000000, -18.52512058521576677 ) ) ;
#88080=CARTESIAN_POINT ( 'NONE',  ( -17.49999999999997513, 45.00000000000000711, 64.09953197936602010 ) ) ;
#88091=CARTESIAN_POINT ( 'NONE',  ( 1.517883041479706208E-15, -5.000000000000000888, -97.00000000000000000 ) ) ;
#88100=ORIENTED_EDGE ( 'NONE', *, *, #91739, .T. ) ;
#88107=CARTESIAN_POINT ( 'NONE',  ( -12.50000000000000000, 25.10944952739952996, -42.56876883562922842 ) ) ;
#88120=CARTESIAN_POINT ( 'NONE',  ( 7.237253906321553742, 41.05631881893103952, -58.62831218766484653 ) ) ;
#88128=CARTESIAN_POINT ( 'NONE',  ( 7.500000000016720847, 43.33959969848655192, -60.00534814812574780 ) ) ;
#88137=CARTESIAN_POINT ( 'NONE',  ( 7.500000000000007105, 40.00000000000000000, -59.28631038546474485 ) ) ;
#88151=CARTESIAN_POINT ( 'NONE',  ( -56.06936961859863544, 49.99999999999999289, -33.41736086620520751 ) ) ;
#88155=CARTESIAN_POINT ( 'NONE',  ( 12.23630716935516816, -4.549675231767582595, -76.78946638291472482 ) ) ;
#88162=CARTESIAN_POINT ( 'NONE',  ( 18.12922454741385891, 50.00000000000001421, 61.72358472360003390 ) ) ;
#88173=( LENGTH_UNIT ( ) NAMED_UNIT ( * ) SI_UNIT ( .MILLI., .METRE. ) );
#88203=CARTESIAN_POINT ( 'NONE',  ( 7.251496294514814700, 41.03131494657971956, -58.65726288480846051 ) ) ;
#88228=CARTESIAN_POINT ( 'NONE',  ( -9.739726766104285005, 48.00000000000000000, -82.38252115500968387 ) ) ;
#88234=B_SPLINE_CURVE_WITH_KNOTS ( 'NONE', 3,
 ( #80181, #21986, #87770, #88300, #46764, #96397, #71040, #5769 ),
 .UNSPECIFIED., .F., .F.,
 ( 4, 2, 2, 4 ),
 ( 0.000000000000000000, 0.5000000000000000000, 0.7500000000000000000, 1.000000000000000000 ),
 .UNSPECIFIED. ) ;
#88238=CARTESIAN_POINT ( 'NONE',  ( -7.493949047870493096, 40.57569111244914950, -68.91429205788598722 ) ) ;
#88250=CARTESIAN_POINT ( 'NONE',  ( 5.219866590718106991, -5.000000000000000000, 8.922269033012842243 ) ) ;
#88271=CARTESIAN_POINT ( 'NONE',  ( -40.47244160127206669, 40.24842158074789467, -54.85959184083456819 ) ) ;
#88272=CARTESIAN_POINT ( 'NONE',  ( -18.14538688196167726, 50.00000000000000711, 61.70354622640617492 ) ) ;
#88278=CARTESIAN_POINT ( 'NONE',  ( 17.50000000000004974, 49.99999999999836575, 59.86364615470527184 ) ) ;
#88287=SURFACE_STYLE_FILL_AREA ( #61907 ) ;
#88300=CARTESIAN_POINT ( 'NONE',  ( 6.965116047733301841, 41.61856606189723351, -70.00485699918135651 ) ) ;
#88328=CARTESIAN_POINT ( 'NONE',  ( -18.91781669292785395, 48.00000000000000000, 62.18610382930904734 ) ) ;
#88338=CARTESIAN_POINT ( 'NONE',  ( 6.346112353299384168, 41.86049394308200533, -59.13213732590009641 ) ) ;
#88364=STYLED_ITEM ( 'NONE', ( #5355 ), #96508 ) ;
#88366=CARTESIAN_POINT ( 'NONE',  ( 16.52731600354976393, 43.98685737190850631, -87.77869701378344303 ) ) ;
#88373=CARTESIAN_POINT ( 'NONE',  ( -12.49723740359457658, -3.303264067464895870, -76.71011700628434937 ) ) ;
#88390=CARTESIAN_POINT ( 'NONE',  ( -4.175893272572330339, -5.000000000001136868, -7.137815226410158864 ) ) ;
#88395=CARTESIAN_POINT ( 'NONE',  ( 0.000000000000000000, -5.000000000000000000, 0.000000000000000000 ) ) ;
#88439=LINE ( 'NONE', #81376, #59982 ) ;
#88454=CARTESIAN_POINT ( 'NONE',  ( 19.36135695977271709, 49.91008391659885035, 61.13655276434777619 ) ) ;
#88477=CARTESIAN_POINT ( 'NONE',  ( -6.075687308901098760, 41.99394926078448265, -68.91429205814512216 ) ) ;
#88484=FILL_AREA_STYLE ('',( #45899 ) ) ;
#88496=CARTESIAN_POINT ( 'NONE',  ( 2.093983074874242067, -3.000000000000000444, -7.791781413346524410 ) ) ;
#88500=CARTESIAN_POINT ( 'NONE',  ( -8.737863884124131175, -5.000000000000002665, -79.96381019768853093 ) ) ;
#88502=B_SPLINE_CURVE_WITH_KNOTS ( 'NONE', 3,
 ( #99374, #72979, #24490, #82140, #89724, #40624, #40105, #64393, #90785, #16898, #73510, #66492, #98334, #105884, #48703 ),
 .UNSPECIFIED., .F., .F.,
 ( 4, 1, 1, 1, 1, 1, 1, 1, 2, 2, 4 ),
 ( 0.000000000000000000, 0.2500000000000872080, 0.3750000000001318390, 0.4375000000001538214, 0.4687500000001610934, 0.4843750000001644240, 0.4921875000001630918, 0.4960937500001587064, 0.4980468750001556533, 0.5000000000001525446, 1.000000000000000000 ),
 .UNSPECIFIED. ) ;
#88511=CARTESIAN_POINT ( 'NONE',  ( 5.885102640078956782, -4.999999999999984901, -15.35622078683712743 ) ) ;
#88514=CARTESIAN_POINT ( 'NONE',  ( 6.201636426617084574E-15, 39.99999999999999289, -70.00365511371767013 ) ) ;
#88565=CARTESIAN_POINT ( 'NONE',  ( 51.81827666034978819, 39.42541842817299624, 39.69774341223477165 ) ) ;
#88583=CARTESIAN_POINT ( 'NONE',  ( 6.145467200819017428, 48.00000000000000000, -92.99666842291193802 ) ) ;
#88591=CARTESIAN_POINT ( 'NONE',  ( -14.63464771654506791, 41.99999999996094857, -88.44359770654935460 ) ) ;
#88613=CARTESIAN_POINT ( 'NONE',  ( 9.500000000000000000, -5.000000000000000000, -20.99851272547260095 ) ) ;
#88620=CARTESIAN_POINT ( 'NONE',  ( 7.179418447820448357, 41.32597146628941687, -70.21787980165106546 ) ) ;
#88624=CARTESIAN_POINT ( 'NONE',  ( -7.500000000000007105, 40.18760986260523538, -59.65696556657620420 ) ) ;
#88629=CARTESIAN_POINT ( 'NONE',  ( -12.50000000000000533, 34.77083264068856039, -54.03046856804895270 ) ) ;
#88639=CARTESIAN_POINT ( 'NONE',  ( 7.500000000000007105, 40.19558899698767362, -59.64746577828605467 ) ) ;
#88651=VERTEX_POINT ( 'NONE', #92159 ) ;
#88674=CARTESIAN_POINT ( 'NONE',  ( 50.94745919686198476, 50.00000000000000000, -37.05882352941176094 ) ) ;
#88686=CARTESIAN_POINT ( 'NONE',  ( 19.15934361619958537, 50.00000000000000711, 60.36969726297910199 ) ) ;
#88706=CARTESIAN_POINT ( 'NONE',  ( -12.50000000000000000, 1.275975811747059652, -19.12903451213154327 ) ) ;
#88713=CARTESIAN_POINT ( 'NONE',  ( 5.500000000000641265, 42.00000000000000000, -59.88032989331720302 ) ) ;
#88754=CARTESIAN_POINT ( 'NONE',  ( -50.94745919686199898, 50.00000000000000000, -37.05882352941176805 ) ) ;
#88766=EDGE_LOOP ( 'NONE', ( #62349, #61239, #94731, #3858, #35804, #38187 ) ) ;
#88774=CARTESIAN_POINT ( 'NONE',  ( 8.000000000000000000, -3.000000000000000000, 2.094395098902537722 ) ) ;
#88793=CARTESIAN_POINT ( 'NONE',  ( -49.53030510826501853, 39.42532954496144981, -42.40708829318106865 ) ) ;
#88802=( NAMED_UNIT ( * ) SI_UNIT ( $, .STERADIAN. ) SOLID_ANGLE_UNIT ( ) );
#88809=CARTESIAN_POINT ( 'NONE',  ( -9.285084206833351672, -5.000000000000069278, -17.96579109464167345 ) ) ;
#88824=VERTEX_POINT ( 'NONE', #94192 ) ;
#88861=CARTESIAN_POINT ( 'NONE',  ( 5.701071517278371914, 41.97507531912567202, -59.34341564409904635 ) ) ;
#88913=CARTESIAN_POINT ( 'NONE',  ( 2.094395098902538610, -4.999999999999998224, -8.000000000000000000 ) ) ;
#88921=CARTESIAN_POINT ( 'NONE',  ( -12.49999999999999822, -4.999999999999999112, -9.904958390907015797 ) ) ;
#88944=B_SPLINE_CURVE_WITH_KNOTS ( 'NONE', 3,
 ( #85416, #62230, #78373, #62739 ),
 .UNSPECIFIED., .F., .F.,
 ( 4, 4 ),
 ( 0.000000000000000000, 1.000000000000000000 ),
 .UNSPECIFIED. ) ;
#88950=ORIENTED_EDGE ( 'NONE', *, *, #66422, .T. ) ;
#88976=CARTESIAN_POINT ( 'NONE',  ( 19.04909562685467606, 49.60302394437223228, 61.82637030200322670 ) ) ;
#89026=CARTESIAN_POINT ( 'NONE',  ( -17.49999999999996447, 48.00000000000000000, 62.61746187599676716 ) ) ;
#89027=DIRECTION ( 'NONE',  ( 1.000000000000000000, 0.000000000000000000, 0.000000000000000000 ) ) ;
#89034=CARTESIAN_POINT ( 'NONE',  ( 7.145220222862747939, -4.999999999999987566, -15.42794826860614954 ) ) ;
#89044=CARTESIAN_POINT ( 'NONE',  ( -14.75116209839011994, 43.55504285526384933, -90.22050492866908655 ) ) ;
#89054=SURFACE_SIDE_STYLE ('',( #71267 ) ) ;
#89059=CARTESIAN_POINT ( 'NONE',  ( -7.421727596595663279, -4.999999999998602007, -70.37058874442158185 ) ) ;
#89065=ORIENTED_EDGE ( 'NONE', *, *, #40084, .F. ) ;
#89068=CARTESIAN_POINT ( 'NONE',  ( -44.27708498590406805, 39.31679366924625185, -47.24726744788640076 ) ) ;
#89074=CARTESIAN_POINT ( 'NONE',  ( -15.02532820471274455, 41.95741948359002294, -84.73629005496447064 ) ) ;
#89077=CARTESIAN_POINT ( 'NONE',  ( 11.99999999999999467, -5.000000000000002665, -86.57079632498522415 ) ) ;
#89082=ORIENTED_EDGE ( 'NONE', *, *, #27362, .F. ) ;
#89106=ORIENTED_EDGE ( 'NONE', *, *, #54459, .T. ) ;
#89128=CARTESIAN_POINT ( 'NONE',  ( 7.298048344747715355, -5.000000000000000000, -15.50087045093206939 ) ) ;
#89153=CARTESIAN_POINT ( 'NONE',  ( 6.872826229292755329, 41.26098029407512513, -70.68506212700772551 ) ) ;
#89174=CARTESIAN_POINT ( 'NONE',  ( 7.398423646700466705, 41.20504349441435465, -59.67381333703970370 ) ) ;
#89187=ORIENTED_EDGE ( 'NONE', *, *, #29334, .T. ) ;
#89203=CARTESIAN_POINT ( 'NONE',  ( 56.06921707446437608, 40.83906611471630299, -33.41757057980699130 ) ) ;
#89230=ORIENTED_EDGE ( 'NONE', *, *, #5905, .T. ) ;
#89241=CARTESIAN_POINT ( 'NONE',  ( -12.50000000000000000, 5.730253409965417433, -23.74922892625246362 ) ) ;
#89277=MECHANICAL_DESIGN_GEOMETRIC_PRESENTATION_REPRESENTATION('',(#4893),#35960);
#89339=CARTESIAN_POINT ( 'NONE',  ( 17.50000000000002842, 51.99998113221720075, 59.93765433267320475 ) ) ;
#89344=CARTESIAN_POINT ( 'NONE',  ( 0.000000000000000000, -5.000000000000000888, -73.00000000000001421 ) ) ;
#89349=CARTESIAN_POINT ( 'NONE',  ( -7.417322861528432121, -5.000000000002099654, -16.62528780686862717 ) ) ;
#89364=ORIENTED_EDGE ( 'NONE', *, *, #3797, .T. ) ;
#89373=CARTESIAN_POINT ( 'NONE',  ( -58.90678327790172375, 48.00000000000000000, -28.11551192219426909 ) ) ;
#89400=CARTESIAN_POINT ( 'NONE',  ( 6.916165809215955917, 41.81554757990602411, -59.83173451229081508 ) ) ;
#89437=CARTESIAN_POINT ( 'NONE',  ( -7.500000000000006217, 39.99999999999122480, -59.88032989330939415 ) ) ;
#89440=VERTEX_POINT ( 'NONE', #69002 ) ;
#89450=CARTESIAN_POINT ( 'NONE',  ( -8.922269033015549411, -5.000000000000000000, -5.219866590717671784 ) ) ;
#89457=CARTESIAN_POINT ( 'NONE',  ( -12.50000000000000711, -4.999999999999999112, -55.73109925765189843 ) ) ;
#89527=CARTESIAN_POINT ( 'NONE',  ( 5.668940197363838251, 41.88723871811491506, -59.02759513106027356 ) ) ;
#89539=SURFACE_STYLE_FILL_AREA ( #31332 ) ;
#89542=EDGE_CURVE ( 'NONE', #53479, #78094, #101263, .T. ) ;
#89548=VECTOR ( 'NONE', #61398, 1000.000000000000000 ) ;
#89556=( NAMED_UNIT ( * ) PLANE_ANGLE_UNIT ( ) SI_UNIT ( $, .RADIAN. ) );
#89565=CARTESIAN_POINT ( 'NONE',  ( 6.016266904915582359, -5.000000000005062617, -16.21640811047284814 ) ) ;
#89587=CARTESIAN_POINT ( 'NONE',  ( -17.50000000000007461, 50.00318699355199925, 59.98279283212356461 ) ) ;
#89590=CARTESIAN_POINT ( 'NONE',  ( -8.641101172624390259, -5.000000000000001776, -72.37542516940096959 ) ) ;
#89608=CARTESIAN_POINT ( 'NONE',  ( 1.570796324976846403, -5.000000000000002665, -97.00000000000000000 ) ) ;
#89612=FACE_OUTER_BOUND ( 'NONE', #27142, .T. ) ;
#89614=ORIENTED_EDGE ( 'NONE', *, *, #32747, .T. ) ;
#89621=CARTESIAN_POINT ( 'NONE',  ( 1.191759989000068964, -5.000000000000000000, -98.00009052017544775 ) ) ;
#89626=ORIENTED_EDGE ( 'NONE', *, *, #53764, .T. ) ;
#89644=CARTESIAN_POINT ( 'NONE',  ( -10.86775040529106562, -4.994308969803370246, -12.56807544649716135 ) ) ;
#89665=FACE_OUTER_BOUND ( 'NONE', #78635, .T. ) ;
#89688=CARTESIAN_POINT ( 'NONE',  ( 7.044112035629908064, 41.04202961785853887, -70.72791777926931900 ) ) ;
#89693=CARTESIAN_POINT ( 'NONE',  ( -5.500000000000316192, 41.99999999999999289, -59.88032989331280476 ) ) ;
#89696=CARTESIAN_POINT ( 'NONE',  ( -61.31073388236533361, 50.00000000000000711, 14.70371094580587723 ) ) ;
#89708=CARTESIAN_POINT ( 'NONE',  ( 7.495923973900548098, 40.46140423765491079, -59.65192238623429688 ) ) ;
#89718=SHAPE_DEFINITION_REPRESENTATION ( #5361, #52881 ) ;
#89720=EDGE_LOOP ( 'NONE', ( #41664, #57419, #58085, #10506 ) ) ;
#89724=CARTESIAN_POINT ( 'NONE',  ( 13.65239908362034171, 42.97563514209416979, -91.73105433446922063 ) ) ;
#89728=CARTESIAN_POINT ( 'NONE',  ( 14.75116205807806402, 43.55504283729542436, -90.22050498408901831 ) ) ;
#89738=CARTESIAN_POINT ( 'NONE',  ( 7.347880794884118356E-15, 47.00000000000000000, -60.00000000000000000 ) ) ;
#89748=CARTESIAN_POINT ( 'NONE',  ( -6.581905802744468126, 41.48827110272019780, -70.61906944529594909 ) ) ;
#89778=CARTESIAN_POINT ( 'NONE',  ( -7.084743457969951308, 40.92373752417397270, -70.77066391255284827 ) ) ;
#89790=CARTESIAN_POINT ( 'NONE',  ( 6.503418564380250899, 41.93912275385427080, -68.91429206611401526 ) ) ;
#89808=CARTESIAN_POINT ( 'NONE',  ( 30.04542631808804387, 41.08154980029332393, -66.19663379991389718 ) ) ;
#89820=CARTESIAN_POINT ( 'NONE',  ( -25.60851123651793415, 48.00000000000000000, -75.29411764705882604 ) ) ;
#89836=CARTESIAN_POINT ( 'NONE',  ( -10.00000000000000000, -5.000000000000000000, 2.617993873628187806 ) ) ;
#89842=ORIENTED_EDGE ( 'NONE', *, *, #34331, .F. ) ;
#89860=CARTESIAN_POINT ( 'NONE',  ( 17.50000000000007105, 51.60805965402359163, 62.32523305738168773 ) ) ;
#89870=CARTESIAN_POINT ( 'NONE',  ( -7.007554382054896891, -4.192628124816097035, -17.12907408883408422 ) ) ;
#89883=ORIENTED_EDGE ( 'NONE', *, *, #20611, .F. ) ;
#89891=CARTESIAN_POINT ( 'NONE',  ( 52.56483885390522914, 49.99999999999999289, -38.23529411764705799 ) ) ;
#89896=STYLED_ITEM ( 'NONE', ( #86228 ), #93490 ) ;
#89905=VERTEX_POINT ( 'NONE', #2520 ) ;
#89973=CARTESIAN_POINT ( 'NONE',  ( -8.000000000000000000, -4.999999999999998224, -2.094395098902523955 ) ) ;
#89975=CARTESIAN_POINT ( 'NONE',  ( 7.500000000000007105, 39.99999999999998579, -68.91429205785453860 ) ) ;
#90047=CARTESIAN_POINT ( 'NONE',  ( 6.232335497085285780, 41.74193314002017985, -58.83489653296142308 ) ) ;
#90057=CARTESIAN_POINT ( 'NONE',  ( -7.500000000000000888, -3.000671055698259870, -20.99923901233272971 ) ) ;
#90060=FILL_AREA_STYLE_COLOUR ( '', #77391 ) ;
#90065=CARTESIAN_POINT ( 'NONE',  ( 17.67376586503952041, 45.00000000000000711, 62.91491236097121487 ) ) ;
#90080=CARTESIAN_POINT ( 'NONE',  ( 0.000000000000000000, 0.000000000000000000, 100.0000000000000000 ) ) ;
#90090=CARTESIAN_POINT ( 'NONE',  ( 7.340594533187418946, -3.410200195908025478, -18.44125947282588385 ) ) ;
#90092=CARTESIAN_POINT ( 'NONE',  ( 0.000000000000000000, 50.00000000000000000, -97.00000000000000000 ) ) ;
#90103=CARTESIAN_POINT ( 'NONE',  ( -28.89099332366777872, 40.83906611472644954, 58.53034795361808307 ) ) ;
#90106=CARTESIAN_POINT ( 'NONE',  ( -17.50000000000034106, 49.99999999999979394, 59.82664205501249910 ) ) ;
#90111=CARTESIAN_POINT ( 'NONE',  ( -7.500000000000001776, -4.999999999999998224, -68.91429205785460965 ) ) ;
#90124=CARTESIAN_POINT ( 'NONE',  ( -33.11567503806781332, 40.69458692646632159, -62.11412838755995836 ) ) ;
#90130=CARTESIAN_POINT ( 'NONE',  ( -7.374560640982810611, -5.000000000000002665, -94.59600210748614302 ) ) ;
#90136=EDGE_CURVE ( 'NONE', #77528, #23955, #100449, .T. ) ;
#90157=CARTESIAN_POINT ( 'NONE',  ( -9.500000000000003553, -5.000000000000000000, -68.91429205785459544 ) ) ;
#90161=FACE_OUTER_BOUND ( 'NONE', #93957, .T. ) ;
#90170=CARTESIAN_POINT ( 'NONE',  ( -11.04277565600957800, -4.986087508017872594, -12.57685066306310162 ) ) ;
#90200=EDGE_LOOP ( 'NONE', ( #86455, #67131, #46532, #28605, #28016 ) ) ;
#90211=CARTESIAN_POINT ( 'NONE',  ( 7.358395007876660898, 41.06696377170784729, -70.11547971526088929 ) ) ;
#90216=CARTESIAN_POINT ( 'NONE',  ( -6.075724000949984216, 41.99394325426889196, -59.86320218788793568 ) ) ;
#90231=CARTESIAN_POINT ( 'NONE',  ( 7.229692759409445557, 41.58551695089550293, -59.68506492437333577 ) ) ;
#90248=CARTESIAN_POINT ( 'NONE',  ( 14.01509066308681817, 42.58675651380951166, -91.23243584937777939 ) ) ;
#90258=CARTESIAN_POINT ( 'NONE',  ( 28.89099332371403861, 40.83906611472283288, 58.53034795359498332 ) ) ;
#90268=VERTEX_POINT ( 'NONE', #54647 ) ;
#90289=ORIENTED_EDGE ( 'NONE', *, *, #17824, .F. ) ;
#90297=CARTESIAN_POINT ( 'NONE',  ( 2.354743324221998613, 48.00000000000000711, -99.86073547176458476 ) ) ;
#90301=CARTESIAN_POINT ( 'NONE',  ( -6.763062896852164663, 41.48827110272769403, -70.48955655162545497 ) ) ;
#90329=CARTESIAN_POINT ( 'NONE',  ( 51.48757442383971039, 38.95383793068618417, -37.45149417477087184 ) ) ;
#90335=CARTESIAN_POINT ( 'NONE',  ( 12.50000000000000711, 34.92454988980409780, -54.26535491090573515 ) ) ;
#90340=CARTESIAN_POINT ( 'NONE',  ( -6.827804075409870777, -2.999999999999648281, -71.19745151638491620 ) ) ;
#90341=CARTESIAN_POINT ( 'NONE',  ( -52.56483885390524335, 49.99999999999999289, -38.23529411764707220 ) ) ;
#90348=CARTESIAN_POINT ( 'NONE',  ( 8.334564508160873686, 38.95383793066860534, 63.67138272020815748 ) ) ;
#90368=CARTESIAN_POINT ( 'NONE',  ( -17.49999999999997513, 45.00000000000000711, -500000.0000000000582 ) ) ;
#90392=CARTESIAN_POINT ( 'NONE',  ( 19.48979057729710718, 49.99890399319816936, 60.12824249908596386 ) ) ;
#90403=CARTESIAN_POINT ( 'NONE',  ( -6.617039711671010238, -4.368567403894508594, -16.80329192430648888 ) ) ;
#90427=CARTESIAN_POINT ( 'NONE',  ( 52.56483885390522204, 48.00000000000000000, -38.23529411764705799 ) ) ;
#90504=( LENGTH_UNIT ( ) NAMED_UNIT ( * ) SI_UNIT ( .MILLI., .METRE. ) );
#90539=DIRECTION ( 'NONE',  ( 0.000000000000000000, 1.000000000000000000, 0.000000000000000000 ) ) ;
#90572=SURFACE_STYLE_FILL_AREA ( #43091 ) ;
#90594=PRESENTATION_STYLE_ASSIGNMENT (( #16164 ) ) ;
#90607=CARTESIAN_POINT ( 'NONE',  ( -8.817541433524096917, -5.000000000000000000, -16.91981367016228788 ) ) ;
#90615=CARTESIAN_POINT ( 'NONE',  ( -17.49999999999996447, 44.85000000000000853, 62.61746187599676716 ) ) ;
#90642=CARTESIAN_POINT ( 'NONE',  ( -18.92174722983623525, 48.90933038776066155, 62.13887004286765858 ) ) ;
#90657=CARTESIAN_POINT ( 'NONE',  ( -21.47524434066147947, 41.77809834471024431, -77.71550088237076181 ) ) ;
#90663=CARTESIAN_POINT ( 'NONE',  ( -10.48543666094732352, -5.000000000000002665, -78.95657223722187723 ) ) ;
#90669=SURFACE_SIDE_STYLE ('',( #55613 ) ) ;
#90689=CARTESIAN_POINT ( 'NONE',  ( 54.95211584722589748, 38.95432885569419312, -32.68840303539023040 ) ) ;
#90727=CARTESIAN_POINT ( 'NONE',  ( 6.581905806972325301, 41.48827110309209587, -70.61906944721928880 ) ) ;
#90746=CARTESIAN_POINT ( 'NONE',  ( 7.255115585955611124, 41.55406142676530834, -69.27528320264251249 ) ) ;
#90752=CARTESIAN_POINT ( 'NONE',  ( -54.43501200699899556, 38.95383793068867817, -33.39731814188755976 ) ) ;
#90756=EDGE_CURVE ( 'NONE', #83228, #3104, #104866, .T. ) ;
#90763=CARTESIAN_POINT ( 'NONE',  ( -7.499999896686553313, -3.000070742345582797, -20.99858933621946733 ) ) ;
#90768=CARTESIAN_POINT ( 'NONE',  ( 27.57459505079161843, 18.64284798592546011, -26.76870628200340008 ) ) ;
#90785=CARTESIAN_POINT ( 'NONE',  ( 13.45452273892127870, 42.85594303034280017, -92.00308933281662860 ) ) ;
#90801=CARTESIAN_POINT ( 'NONE',  ( -42.35263604938428017, 50.00000000000000000, 46.99568999588436924 ) ) ;
#90815=CARTESIAN_POINT ( 'NONE',  ( 6.315918964083451215, 41.33387245947155719, -58.37026373930601864 ) ) ;
#90839=CARTESIAN_POINT ( 'NONE',  ( -7.113472013431297647, 40.00000000006956924, -71.00901315851918127 ) ) ;
#90849=CARTESIAN_POINT ( 'NONE',  ( -7.996135855215158905, -4.999999999999999112, 6.145819459795549555 ) ) ;
#90912=FILL_AREA_STYLE ('',( #57991 ) ) ;
#90933=CARTESIAN_POINT ( 'NONE',  ( 17.50000000000028422, 50.00000000000154898, 59.64162155654624797 ) ) ;
#90936=CARTESIAN_POINT ( 'NONE',  ( -6.236082950926880919, 41.88001960641946653, -59.13168064570682247 ) ) ;
#90943=CARTESIAN_POINT ( 'NONE',  ( -7.101747359475742982, -4.047770588416829796, -17.37629258578624203 ) ) ;
#90964=ORIENTED_EDGE ( 'NONE', *, *, #5276, .T. ) ;
#90968=CARTESIAN_POINT ( 'NONE',  ( -39.04923757935653583, 48.00000000000000000, 52.30342408741262972 ) ) ;
#91009=MECHANICAL_DESIGN_GEOMETRIC_PRESENTATION_REPRESENTATION('',(#18647),#6593);
#91013=EDGE_CURVE ( 'NONE', #21082, #31057, #20020, .T. ) ;
#91026=B_SPLINE_CURVE_WITH_KNOTS ( 'NONE', 3,
 ( #26269, #92014, #18150, #10034, #42941, #75830, #96292, #22417 ),
 .UNSPECIFIED., .F., .F.,
 ( 4, 2, 2, 4 ),
 ( 0.000000000000000000, 0.2500000000000053291, 0.5000000000000106581, 1.000000000000000000 ),
 .UNSPECIFIED. ) ;
#91091=ORIENTED_EDGE ( 'NONE', *, *, #13899, .T. ) ;
#91125=CARTESIAN_POINT ( 'NONE',  ( -11.85444436800005263, 42.00000000000000000, 90.56128410203886858 ) ) ;
#91130=FACE_OUTER_BOUND ( 'NONE', #37436, .T. ) ;
#91145=CARTESIAN_POINT ( 'NONE',  ( 4.651132217449188921, -5.000000000000000000, -15.66661053588737751 ) ) ;
#91146=STYLED_ITEM ( 'NONE', ( #20740 ), #12512 ) ;
#91152=CARTESIAN_POINT ( 'NONE',  ( 17.61582496125343411, 45.00000000000001421, 63.05442575584599751 ) ) ;
#91195=CARTESIAN_POINT ( 'NONE',  ( -17.49999999999999289, 48.58944628575790148, 64.09148194233866036 ) ) ;
#91207=CARTESIAN_POINT ( 'NONE',  ( 12.13034742782427955, 48.00000000000000000, -93.82352941176471006 ) ) ;
#91209=CARTESIAN_POINT ( 'NONE',  ( -23.97981144771549467, 41.62095615380706448, -74.33343198471487767 ) ) ;
#91216=CARTESIAN_POINT ( 'NONE',  ( -5.363597346089342466, 41.33266196706077267, -58.39526881795508473 ) ) ;
#91239=CARTESIAN_POINT ( 'NONE',  ( -20.09676425191630500, 38.95313086215059428, 60.48296960500260155 ) ) ;
#91291=CARTESIAN_POINT ( 'NONE',  ( 7.319240905726694280, 40.56016492320068068, -70.61401732095062300 ) ) ;
#91293=VERTEX_POINT ( 'NONE', #49227 ) ;
#91322=DIRECTION ( 'NONE',  ( 1.000000000000000000, 0.000000000000000000, 0.000000000000000000 ) ) ;
#91330=CARTESIAN_POINT ( 'NONE',  ( -4.852941176470593199, 9.833333333333344584, -70.80672828634229177 ) ) ;
#91353=CARTESIAN_POINT ( 'NONE',  ( -29.83308852634790043, 42.00000000000000000, -51.76085035113232635 ) ) ;
#91361=FACE_OUTER_BOUND ( 'NONE', #15820, .T. ) ;
#91365=STYLED_ITEM ( 'NONE', ( #27870 ), #70975 ) ;
#91375=CARTESIAN_POINT ( 'NONE',  ( -12.47767672221401725, -3.661475206072811517, -13.56848805978015804 ) ) ;
#91376=CARTESIAN_POINT ( 'NONE',  ( 5.756917790976764593, 48.00000000000000711, -98.90122916984913104 ) ) ;
#91378=CARTESIAN_POINT ( 'NONE',  ( -7.274973724374026673, 40.00000000004767742, -70.77553044199200372 ) ) ;
#91414=CARTESIAN_POINT ( 'NONE',  ( 12.50000000000000533, 39.74580781711993183, -64.99248152779956911 ) ) ;
#91419=CARTESIAN_POINT ( 'NONE',  ( -7.500000000000006217, 40.00000000007573675, -70.73267643392316018 ) ) ;
#91426=EDGE_LOOP ( 'NONE', ( #66490, #72718, #12207, #69484, #66233 ) ) ;
#91453=ORIENTED_EDGE ( 'NONE', *, *, #54026, .F. ) ;
#91468=CARTESIAN_POINT ( 'NONE',  ( -5.425084051525484341, 41.91238126712414669, -59.10640584780988149 ) ) ;
#91476=CARTESIAN_POINT ( 'NONE',  ( -8.480229304264785384, -5.000000000000526690, -16.24557161192316102 ) ) ;
#91525=UNCERTAINTY_MEASURE_WITH_UNIT (LENGTH_MEASURE( 1.000000000000000082E-05 ), #60614, 'distance_accuracy_value', 'NONE');
#91544=FACE_OUTER_BOUND ( 'NONE', #46702, .T. ) ;
#91577=( GEOMETRIC_REPRESENTATION_CONTEXT ( 3 ) GLOBAL_UNCERTAINTY_ASSIGNED_CONTEXT ( ( #104534 ) ) GLOBAL_UNIT_ASSIGNED_CONTEXT ( ( #26585, #2783, #76140 ) ) REPRESENTATION_CONTEXT ( 'NONE', 'WORKASPACE' ) );
#91583=CARTESIAN_POINT ( 'NONE',  ( 7.500000000000000888, -4.999999999999997335, -14.04024970282782547 ) ) ;
#91585=CARTESIAN_POINT ( 'NONE',  ( -17.49999999999997513, 49.09249047134142785, 64.04102639539493680 ) ) ;
#91606=EDGE_CURVE ( 'NONE', #7244, #53673, #25149, .T. ) ;
#91631=CARTESIAN_POINT ( 'NONE',  ( -7.006861776756331039, 41.19339244735165551, -58.48462588885441704 ) ) ;
#91650=SURFACE_SIDE_STYLE ('',( #58755 ) ) ;
#91655=CARTESIAN_POINT ( 'NONE',  ( 6.586014638021513434, 41.68775674026067435, -58.88021276518479397 ) ) ;
#91672=CARTESIAN_POINT ( 'NONE',  ( 18.22717058311603466, 45.00000000000000711, 62.43928791138841916 ) ) ;
#91678=CARTESIAN_POINT ( 'NONE',  ( -9.189739293810873733, -4.999999999999998224, -17.80227345177911502 ) ) ;
#91687=CARTESIAN_POINT ( 'NONE',  ( 37.48925363931293475, 48.00000000000000000, 53.34938573421631247 ) ) ;
#91699=CARTESIAN_POINT ( 'NONE',  ( 5.293743209220361123, -3.000000000000003109, -99.09939186120909937 ) ) ;
#91713=CARTESIAN_POINT ( 'NONE',  ( -17.50000000000292744, 50.00000000000124345, 59.64162155654736353 ) ) ;
#91729=CARTESIAN_POINT ( 'NONE',  ( -33.12584033004571893, 40.69330525349585059, -62.10061223356491666 ) ) ;
#91734=CARTESIAN_POINT ( 'NONE',  ( -9.739726766103894207, -3.000000000000002665, -82.38252115500876016 ) ) ;
#91739=EDGE_CURVE ( 'NONE', #57829, #86235, #99618, .T. ) ;
#91764=SURFACE_STYLE_FILL_AREA ( #51278 ) ;
#91772=( BOUNDED_SURFACE ( )  B_SPLINE_SURFACE ( 2, 3, ( 
 ( #68095, #91843, #99378, #50309, #17971, #66500 ),
 ( #139, #58417, #16355, #50828, #9845, #26620 ),
 ( #49240, #91330, #75649, #1201, #43294, #84284 ) ),
 .UNSPECIFIED., .F., .F., .F. ) 
 B_SPLINE_SURFACE_WITH_KNOTS ( ( 3, 3 ),
 ( 4, 2, 4 ),
 ( 0.000000000000000000, 1.000000000000000000 ),
 ( 0.07468083296558609974, 0.1199308329655860983, 0.1241808329655861021 ),
 .UNSPECIFIED. ) 
 GEOMETRIC_REPRESENTATION_ITEM ( )  RATIONAL_B_SPLINE_SURFACE ( (
 ( 1.000000000000000000, 1.000000000000000000, 1.000000000000000000, 1.000000000000000000, 1.000000000000000000, 1.000000000000000000),
 ( 1.857142857142858317, 1.857142857142858317, 1.857142857142858317, 1.857142857142858317, 1.857142857142858317, 1.857142857142858317),
 ( 1.000000000000000000, 1.000000000000000000, 1.000000000000000000, 1.000000000000000000, 1.000000000000000000, 1.000000000000000000) ) ) 
 REPRESENTATION_ITEM ( '' )  SURFACE ( )  );
#91780=B_SPLINE_CURVE_WITH_KNOTS ( 'NONE', 3,
 ( #158, #33124, #65993, #23986 ),
 .UNSPECIFIED., .F., .F.,
 ( 4, 4 ),
 ( 0.000000000000000000, 1.000000000000000000 ),
 .UNSPECIFIED. ) ;
#91792=CARTESIAN_POINT ( 'NONE',  ( -7.413000813362873309, 41.14546169070921877, -59.83891281791527916 ) ) ;
#91843=CARTESIAN_POINT ( 'NONE',  ( -7.500000000000005329, 9.833333333333344584, -68.91429205785459544 ) ) ;
#91877=CARTESIAN_POINT ( 'NONE',  ( 52.56483885390524335, 40.83906611471594061, -38.23529411764712194 ) ) ;
#91880=CARTESIAN_POINT ( 'NONE',  ( 14.07141389085968974, 41.78883774888220870, -79.52223927790954860 ) ) ;
#91897=CARTESIAN_POINT ( 'NONE',  ( -6.856834871365124151, 41.38254192121598862, -70.56142688853883271 ) ) ;
#91906=CARTESIAN_POINT ( 'NONE',  ( -5.062272329161832118, -5.000000000000001776, -8.716576110314617765 ) ) ;
#91907=CARTESIAN_POINT ( 'NONE',  ( 4.854898838401722649, 40.57569111244889370, -70.80100276615310406 ) ) ;
#91963=( LENGTH_UNIT ( ) NAMED_UNIT ( * ) SI_UNIT ( .MILLI., .METRE. ) );
#91974=FILL_AREA_STYLE ('',( #262 ) ) ;
#91999=EDGE_LOOP ( 'NONE', ( #62362, #22599, #97759, #81158 ) ) ;
#92014=CARTESIAN_POINT ( 'NONE',  ( -5.371836670387280854, 41.43594048061098079, -58.48719196077191640 ) ) ;
#92026=CARTESIAN_POINT ( 'NONE',  ( -22.47385306462515331, 18.64284798593318371, -31.17447444075813223 ) ) ;
#92039=CARTESIAN_POINT ( 'NONE',  ( 22.63965596209432718, 41.71073122692603619, -76.14257482519676046 ) ) ;
#92042=CYLINDRICAL_SURFACE ( 'NONE', #53226, 8.000000000000000000 ) ;
#92094=CARTESIAN_POINT ( 'NONE',  ( -39.23172258004870372, 39.86656256230372719, -53.99799038518022343 ) ) ;
#92113=ORIENTED_EDGE ( 'NONE', *, *, #44345, .T. ) ;
#92115=EDGE_CURVE ( 'NONE', #27940, #72021, #92760, .T. ) ;
#92157=DIRECTION ( 'NONE',  ( -0.000000000000000000, 1.000000000000000000, -0.000000000000000000 ) ) ;
#92159=CARTESIAN_POINT ( 'NONE',  ( -14.33580413386536812, 42.00000000000000000, -89.41414995615788541 ) ) ;
#92160=( NAMED_UNIT ( * ) PLANE_ANGLE_UNIT ( ) SI_UNIT ( $, .RADIAN. ) );
#92166=CARTESIAN_POINT ( 'NONE',  ( -7.500000000000007105, 40.00000000000000000, -58.69229087761261354 ) ) ;
#92195=AXIS2_PLACEMENT_3D ( 'NONE', #90368, #41282, #16481 ) ;
#92201=CARTESIAN_POINT ( 'NONE',  ( 1.347801180098172180, -3.000000000000003109, -100.0000000000007105 ) ) ;
#92218=CARTESIAN_POINT ( 'NONE',  ( -17.49999999999995737, 51.99999999999994316, 59.82664205501144039 ) ) ;
#92237=CARTESIAN_POINT ( 'NONE',  ( 5.036189802310915731, -3.000000000000002665, -93.73786388412167980 ) ) ;
#92271=CARTESIAN_POINT ( 'NONE',  ( 19.47704209976909695, 49.99346651654762042, 60.32563227602115319 ) ) ;
#92282=CARTESIAN_POINT ( 'NONE',  ( -7.500000000000002665, 9.462792962020666110, -29.31754814678773968 ) ) ;
#92297=CARTESIAN_POINT ( 'NONE',  ( -7.268970507964822581, 41.22981623788603400, -58.87267832762033493 ) ) ;
#92308=B_SPLINE_CURVE_WITH_KNOTS ( 'NONE', 3,
 ( #18851, #1538, #59281, #98647 ),
 .UNSPECIFIED., .F., .F.,
 ( 4, 4 ),
 ( 0.000000000000000000, 1.000000000000000000 ),
 .UNSPECIFIED. ) ;
#92370=CIRCLE ( 'NONE', #25277, 15.00000000000000178 ) ;
#92387=CARTESIAN_POINT ( 'NONE',  ( -2.912673042965788187E-14, 42.00000000000000000, -90.56128410203886858 ) ) ;
#92394=CARTESIAN_POINT ( 'NONE',  ( -56.56225795719330307, 40.83885343800341161, 32.16455131414174673 ) ) ;
#92409=COLOUR_RGB ( '', 0.72549020, 0.75294118, 0.79215686) ;
#92411=CARTESIAN_POINT ( 'NONE',  ( -9.999999999999989342, 49.99999999999999289, -86.30899693748770574 ) ) ;
#92413=CARTESIAN_POINT ( 'NONE',  ( 10.63258248847111709, 47.99999999999999289, -95.64586607611548175 ) ) ;
#92418=UNCERTAINTY_MEASURE_WITH_UNIT (LENGTH_MEASURE( 1.000000000000000082E-05 ), #46940, 'distance_accuracy_value', 'NONE');
#92422=CARTESIAN_POINT ( 'NONE',  ( -1.308371270545584553, -5.000000000000000000, -10.00012749751951624 ) ) ;
#92432=DIRECTION ( 'NONE',  ( 0.000000000000000000, 1.000000000000000000, 0.000000000000000000 ) ) ;
#92504=CARTESIAN_POINT ( 'NONE',  ( -11.91432047182415133, 48.00000000000000000, 64.17585289259233150 ) ) ;
#92514=EDGE_CURVE ( 'NONE', #78362, #37165, #54508, .T. ) ;
#92520=CARTESIAN_POINT ( 'NONE',  ( 17.52467020414865218, 50.00000000000000000, 63.14993973816012129 ) ) ;
#92540=ORIENTED_EDGE ( 'NONE', *, *, #43505, .F. ) ;
#92541=( NAMED_UNIT ( * ) SI_UNIT ( $, .STERADIAN. ) SOLID_ANGLE_UNIT ( ) );
#92546=CARTESIAN_POINT ( 'NONE',  ( 11.91432047181420195, 49.99999999997997691, 64.17585289263315929 ) ) ;
#92571=CARTESIAN_POINT ( 'NONE',  ( 40.55775739592876050, 39.72826581815989044, -52.22352489735080638 ) ) ;
#92587=CARTESIAN_POINT ( 'NONE',  ( 5.036189802310016006, 50.00000000000001421, -93.73786388411662074 ) ) ;
#92632=CARTESIAN_POINT ( 'NONE',  ( -19.50010530980351220, 50.00000000000000000, 59.90637122617393828 ) ) ;
#92706=( GEOMETRIC_REPRESENTATION_CONTEXT ( 3 ) GLOBAL_UNCERTAINTY_ASSIGNED_CONTEXT ( ( #75349 ) ) GLOBAL_UNIT_ASSIGNED_CONTEXT ( ( #4103, #92160, #86105 ) ) REPRESENTATION_CONTEXT ( 'NONE', 'WORKASPACE' ) );
#92726=AXIS2_PLACEMENT_3D ( 'NONE', #95433, #39730, #4832 ) ;
#92746=CARTESIAN_POINT ( 'NONE',  ( -13.83769416168977173, -3.000000000000002665, -79.05569278143936174 ) ) ;
#92760=LINE ( 'NONE', #28071, #41400 ) ;
#92783=CARTESIAN_POINT ( 'NONE',  ( -2.617478844990583031, -3.000000000000002665, -94.73972676610416954 ) ) ;
#92791=CARTESIAN_POINT ( 'NONE',  ( 15.51786670351831354, -4.332661967059896035, 9.509450810727432923 ) ) ;
#92816=CARTESIAN_POINT ( 'NONE',  ( 4.852941176470594975, -4.999999999999998224, -70.80672828634229177 ) ) ;
#92838=CARTESIAN_POINT ( 'NONE',  ( -7.493767324785338246, 40.39058438512729055, -59.41312847858032598 ) ) ;
#92873=B_SPLINE_SURFACE_WITH_KNOTS ( 'NONE', 3, 3, ( 
 ( #96217, #61738, #39038, #37477, #87590, #103761, #70869, #71922 ),
 ( #95153, #62269, #13675, #4534, #87064, #20780, #46584, #88120 ),
 ( #29898, #29383, #86549, #70341, #30969, #103237, #63848, #79482 ),
 ( #21286, #94634, #53614, #5594, #46066, #78950, #30427, #71380 ),
 ( #104281, #22346, #55191, #14200, #117, #74037, #72965, #640 ),
 ( #16885, #41154, #33088, #8774, #105872, #97777, #57312, #82124 ),
 ( #24989, #90231, #23397, #89174, #7174, #40088, #89708, #88639 ),
 ( #15806, #56238, #105356, #40612, #33607, #48688, #16336, #24476 ) ),
 .UNSPECIFIED., .F., .F., .F.,
 ( 4, 2, 2, 4 ),
 ( 4, 2, 2, 4 ),
 ( 0.000000000000000000, 0.2500000000000000000, 0.5000000000000000000, 1.000000000000000000 ),
 ( 0.000000000000000000, 0.2500000000000000000, 0.5000000000000000000, 1.000000000000000000 ),
 .UNSPECIFIED. ) ;
#92896=ORIENTED_EDGE ( 'NONE', *, *, #29334, .F. ) ;
#92898=CARTESIAN_POINT ( 'NONE',  ( -4.707696486720360340, 49.99999999999999289, -99.43546650844932344 ) ) ;
#92906=CARTESIAN_POINT ( 'NONE',  ( 19.13866731016917910, 49.71730248559679666, 61.67331676224903703 ) ) ;
#92923=CARTESIAN_POINT ( 'NONE',  ( 72.41885610122542971, 42.00000000000000000, -55.65414010180089832 ) ) ;
#92933=CARTESIAN_POINT ( 'NONE',  ( 64.91136071154012654, 40.83917339310983863, 6.834607325964931590 ) ) ;
#92944=CARTESIAN_POINT ( 'NONE',  ( -1.735558044533041189, 41.99999999999999289, -69.74083754112251654 ) ) ;
#92954=CARTESIAN_POINT ( 'NONE',  ( 9.596002107493083244, 50.00000000000000000, -92.37456064097861486 ) ) ;
#92955=CARTESIAN_POINT ( 'NONE',  ( -12.48764691435734875, -3.515361478854691857, -13.73627036880986019 ) ) ;
#92964=CARTESIAN_POINT ( 'NONE',  ( 6.123233995736763324E-16, 48.00000000000000000, -95.00000000000000000 ) ) ;
#92979=CARTESIAN_POINT ( 'NONE',  ( -6.238184438393528986, 40.55825027053369070, -71.19044207184282413 ) ) ;
#92993=CARTESIAN_POINT ( 'NONE',  ( -17.91081636847285807, 45.00000000000001421, 62.63222563193455983 ) ) ;
#93002=CARTESIAN_POINT ( 'NONE',  ( 12.50000000000000000, -2.999999999999996891, -14.34180675897363955 ) ) ;
#93003=VERTEX_POINT ( 'NONE', #27604 ) ;
#93023=CARTESIAN_POINT ( 'NONE',  ( 10.50000000000000178, -5.000000000000000000, -12.52300748975612166 ) ) ;
#93034=B_SPLINE_CURVE_WITH_KNOTS ( 'NONE', 3,
 ( #88713, #72516, #22416, #39112, #79550, #14805, #96291, #5662, #13742, #21355 ),
 .UNSPECIFIED., .F., .F.,
 ( 4, 2, 2, 2, 4 ),
 ( 0.000000000000000000, 0.5000000000000000000, 0.7500000000000000000, 0.8750000000000000000, 1.000000000000000000 ),
 .UNSPECIFIED. ) ;
#93043=CARTESIAN_POINT ( 'NONE',  ( 9.500000000000007105, -5.000000000000000000, -52.94236561372729000 ) ) ;
#93049=CARTESIAN_POINT ( 'NONE',  ( -28.89099332390824770, 48.00000000000000000, 58.53034795347328867 ) ) ;
#93063=CARTESIAN_POINT ( 'NONE',  ( 17.58776036026792156, 49.99999999999999289, 62.73861743982075723 ) ) ;
#93082=CARTESIAN_POINT ( 'NONE',  ( 6.965116047733301841, 41.61856606189723351, -70.00485699918135651 ) ) ;
#93083=CARTESIAN_POINT ( 'NONE',  ( -52.56483885390515098, 49.99999999999999289, -38.23529411764716457 ) ) ;
#93108=CARTESIAN_POINT ( 'NONE',  ( 34.83748305993398731, 40.47757374547448705, -59.82462169405419417 ) ) ;
#93117=ORIENTED_EDGE ( 'NONE', *, *, #54459, .F. ) ;
#93125=CARTESIAN_POINT ( 'NONE',  ( 7.996668422916345165, 49.99999999999455014, -91.14546720080639375 ) ) ;
#93131=CARTESIAN_POINT ( 'NONE',  ( 18.91791044776121211, 45.00000000000000711, 62.18611311450882795 ) ) ;
#93137=CARTESIAN_POINT ( 'NONE',  ( -5.036189803708991164, -3.000000000000003109, -93.73786388354257326 ) ) ;
#93173=CARTESIAN_POINT ( 'NONE',  ( 7.499940182179008374, -3.043015538677189546, -20.22995127276277927 ) ) ;
#93184=CARTESIAN_POINT ( 'NONE',  ( -14.90155531858861870, 42.58002643027919731, -90.01374843399875658 ) ) ;
#93215=CARTESIAN_POINT ( 'NONE',  ( -6.635365861734280557, 41.60399665121233426, -58.75656553345891098 ) ) ;
#93233=CARTESIAN_POINT ( 'NONE',  ( 6.982951203957191488, 41.78396383201351938, -59.69785475688320275 ) ) ;
#93234=CARTESIAN_POINT ( 'NONE',  ( -5.022013495303277786, 18.64316884711714550, 38.36535705883633085 ) ) ;
#93242=CARTESIAN_POINT ( 'NONE',  ( 5.903046305060341226, 41.64520863941469031, -58.65814346794659428 ) ) ;
#93243=CARTESIAN_POINT ( 'NONE',  ( -7.500000000000008882, 42.00000000000000711, -65.90297133633691828 ) ) ;
#93275=( GEOMETRIC_REPRESENTATION_CONTEXT ( 3 ) GLOBAL_UNCERTAINTY_ASSIGNED_CONTEXT ( ( #74217 ) ) GLOBAL_UNIT_ASSIGNED_CONTEXT ( ( #106532, #73085, #14867 ) ) REPRESENTATION_CONTEXT ( 'NONE', 'WORKASPACE' ) );
#93281=B_SPLINE_CURVE_WITH_KNOTS ( 'NONE', 3,
 ( #92964, #4491, #93515, #51963, #101596, #103191, #84878, #10964, #85414, #21244, #53572, #76775, #86502, #12564, #70294, #36376, #2877, #62226 ),
 .UNSPECIFIED., .F., .F.,
 ( 4, 2, 2, 2, 2, 2, 2, 2, 4 ),
 ( 0.5000000000000000000, 0.5625000000000000000, 0.6250000000000000000, 0.6875000000000000000, 0.7500000000000000000, 0.8125000000000000000, 0.8750000000000000000, 0.9375000000000000000, 1.000000000000000000 ),
 .UNSPECIFIED. ) ;
#93287=CARTESIAN_POINT ( 'NONE',  ( -12.67000837003889124, -5.000000000000002665, -88.76274061127951143 ) ) ;
#93326=CARTESIAN_POINT ( 'NONE',  ( 9.739726766104286781, -3.000000000000002665, -87.61747884499031613 ) ) ;
#93335=STYLED_ITEM ( 'NONE', ( #9802 ), #51070 ) ;
#93336=ORIENTED_EDGE ( 'NONE', *, *, #24958, .T. ) ;
#93338=CARTESIAN_POINT ( 'NONE',  ( -13.76503154704160714, -4.999999999998556710, -10.95334723230942942 ) ) ;
#93361=FILL_AREA_STYLE_COLOUR ( '', #63061 ) ;
#93362=ORIENTED_EDGE ( 'NONE', *, *, #85377, .T. ) ;
#93363=CARTESIAN_POINT ( 'NONE',  ( 8.990409435383423187, -4.999999999999999112, -71.93151781320761984 ) ) ;
#93370=CARTESIAN_POINT ( 'NONE',  ( -11.72527720291174624, -4.890001682367673297, -12.55691480003112837 ) ) ;
#93386=ADVANCED_FACE ( 'NONE', ( #77042 ), #18849, .F. ) ;
#93391=CARTESIAN_POINT ( 'NONE',  ( -18.93991643217204057, 49.23433669341508789, 62.05747794209732859 ) ) ;
#93392=CARTESIAN_POINT ( 'NONE',  ( -7.479729137166399866, 40.83274071714285469, -59.46320924800295415 ) ) ;
#93393=CARTESIAN_POINT ( 'NONE',  ( 6.565384647267224594, 40.29402653084121511, -71.20315140851180047 ) ) ;
#93408=CARTESIAN_POINT ( 'NONE',  ( 7.090506028190232790, 41.24768140130692728, -58.61601156502441512 ) ) ;
#93410=CARTESIAN_POINT ( 'NONE',  ( 7.374560640984048732, -5.000000000000002665, -75.40399789250147933 ) ) ;
#93431=CARTESIAN_POINT ( 'NONE',  ( 26.50079164159988210, 18.64284798592797188, 27.83217509638787490 ) ) ;
#93449=( GEOMETRIC_REPRESENTATION_CONTEXT ( 3 ) GLOBAL_UNCERTAINTY_ASSIGNED_CONTEXT ( ( #96355 ) ) GLOBAL_UNIT_ASSIGNED_CONTEXT ( ( #38133, #54245, #55317 ) ) REPRESENTATION_CONTEXT ( 'NONE', 'WORKASPACE' ) );
#93452=CARTESIAN_POINT ( 'NONE',  ( -8.904581707870004692, 48.00000000000000000, -97.29851715191085759 ) ) ;
#93459=UNCERTAINTY_MEASURE_WITH_UNIT (LENGTH_MEASURE( 1.000000000000000082E-05 ), #86710, 'distance_accuracy_value', 'NONE');
#93461=CARTESIAN_POINT ( 'NONE',  ( 19.49880643229863253, 49.99998348590667518, 59.93398820729930065 ) ) ;
#93476=CARTESIAN_POINT ( 'NONE',  ( -36.40416150969235787, 41.99999999991774757, -47.37019975554808582 ) ) ;
#93484=( NAMED_UNIT ( * ) PLANE_ANGLE_UNIT ( ) SI_UNIT ( $, .RADIAN. ) );
#93490=ADVANCED_FACE ( 'NONE', ( #11762 ), #3702, .T. ) ;
#93505=CARTESIAN_POINT ( 'NONE',  ( -12.48571098547292912, -3.549409519532933377, -13.69689515574851058 ) ) ;
#93509=CARTESIAN_POINT ( 'NONE',  ( -7.320748600891240798, 41.41789230214724427, -68.91429205797308555 ) ) ;
#93515=CARTESIAN_POINT ( 'NONE',  ( -2.617478843592799365, 48.00000000000000000, -94.73972676668314818 ) ) ;
#93528=CARTESIAN_POINT ( 'NONE',  ( -6.035340075855088138, 41.06696377143527599, -71.06135861415590682 ) ) ;
#93572=EDGE_CURVE ( 'NONE', #9732, #65010, #96764, .T. ) ;
#93573=CARTESIAN_POINT ( 'NONE',  ( 11.04959452034190903, -4.985681094987538309, -12.57702150655598849 ) ) ;
#93582=CARTESIAN_POINT ( 'NONE',  ( 7.500000000000000000, -4.999999999999999112, -20.99851272547259384 ) ) ;
#93590=CARTESIAN_POINT ( 'NONE',  ( -6.771649247693060758, 41.86512631648978555, -59.59160522040796337 ) ) ;
#93597=CARTESIAN_POINT ( 'NONE',  ( 7.500000000000007105, 11.33333333333401427, -68.91429205785459544 ) ) ;
#93625=CARTESIAN_POINT ( 'NONE',  ( 6.629186139556361823, 41.56975587237539571, -70.49374931123308841 ) ) ;
#93626=CARTESIAN_POINT ( 'NONE',  ( -61.09659575455685143, 50.00000000000000000, -16.41787579824995902 ) ) ;
#93628=CARTESIAN_POINT ( 'NONE',  ( 12.50000000000000533, -3.000000000000000888, -55.91956093573309516 ) ) ;
#93638=UNCERTAINTY_MEASURE_WITH_UNIT (LENGTH_MEASURE( 1.000000000000000082E-05 ), #32748, 'distance_accuracy_value', 'NONE');
#93647=ORIENTED_EDGE ( 'NONE', *, *, #35422, .T. ) ;
#93651=CARTESIAN_POINT ( 'NONE',  ( 42.29757377725155010, 39.52300599983767171, -49.89852198136856742 ) ) ;
#93655=FILL_AREA_STYLE_COLOUR ( '', #29530 ) ;
#93665=CARTESIAN_POINT ( 'NONE',  ( 12.13034742782428133, 49.99999999999999289, -93.82352941176471006 ) ) ;
#93667=CARTESIAN_POINT ( 'NONE',  ( -3.140974613988893882, 50.00000000000000000, -96.68767211932436112 ) ) ;
#93684=CARTESIAN_POINT ( 'NONE',  ( 5.469234054728515204, 41.99717949937266326, -59.59612150530382735 ) ) ;
#93708=( LENGTH_UNIT ( ) NAMED_UNIT ( * ) SI_UNIT ( .MILLI., .METRE. ) );
#93717=FILL_AREA_STYLE_COLOUR ( '', #18671 ) ;
#93723=CARTESIAN_POINT ( 'NONE',  ( -14.33580413386536812, 42.00000000000000000, -89.41414995615788541 ) ) ;
#93725=CARTESIAN_POINT ( 'NONE',  ( 7.751021933904854500, 50.00000000000000711, -95.64136895019579754 ) ) ;
#93729=ORIENTED_EDGE ( 'NONE', *, *, #99234, .T. ) ;
#93730=CARTESIAN_POINT ( 'NONE',  ( 1.591643166428094558, 50.00000000000000711, -73.00000000000002842 ) ) ;
#93737=ORIENTED_EDGE ( 'NONE', *, *, #69720, .F. ) ;
#93745=CARTESIAN_POINT ( 'NONE',  ( -5.129365589857098229, 41.91296976309557465, -69.99827694586697646 ) ) ;
#93750=CARTESIAN_POINT ( 'NONE',  ( -13.99014087154248109, -5.000000000000000000, 8.603192084578022758 ) ) ;
#93751=CARTESIAN_POINT ( 'NONE',  ( -6.870856496050642193, 41.24229779879266999, -58.43742256236558319 ) ) ;
#93758=CARTESIAN_POINT ( 'NONE',  ( 12.50000000000000355, 1.275975694136318506, -19.12903438635300546 ) ) ;
#93769=CARTESIAN_POINT ( 'NONE',  ( 6.592587067551453295, 41.82481096192319825, -59.20696708569246880 ) ) ;
#93770=CARTESIAN_POINT ( 'NONE',  ( -23.57730434126679597, 18.64316884711713485, 30.67950393662591324 ) ) ;
#93777=CARTESIAN_POINT ( 'NONE',  ( 5.668094422307954794, 41.44782620818911312, -58.47096533207623992 ) ) ;
#93793=( GEOMETRIC_REPRESENTATION_CONTEXT ( 3 ) GLOBAL_UNCERTAINTY_ASSIGNED_CONTEXT ( ( #84339 ) ) GLOBAL_UNIT_ASSIGNED_CONTEXT ( ( #55653, #7121, #103707 ) ) REPRESENTATION_CONTEXT ( 'NONE', 'WORKASPACE' ) );
#93798=CARTESIAN_POINT ( 'NONE',  ( 7.500000000000005329, 40.00000000000068923, -68.91429205785459544 ) ) ;
#93816=CARTESIAN_POINT ( 'NONE',  ( 8.572890873561295422, -5.000000000000002665, -75.22730630429822440 ) ) ;
#93842=VERTEX_POINT ( 'NONE', #2879 ) ;
#93849=MECHANICAL_DESIGN_GEOMETRIC_PRESENTATION_REPRESENTATION('',(#105917),#5987);
#93865=CARTESIAN_POINT ( 'NONE',  ( -18.16578424161952654, -4.332661967060594144, -1.112710490969183175 ) ) ;
#93888=CARTESIAN_POINT ( 'NONE',  ( 19.50011280463133545, 50.00000000000000000, 59.90639435984937222 ) ) ;
#93902=( NAMED_UNIT ( * ) PLANE_ANGLE_UNIT ( ) SI_UNIT ( $, .RADIAN. ) );
#93914=CARTESIAN_POINT ( 'NONE',  ( -19.31778612519895688, 49.87566157773895270, 61.28311047971154579 ) ) ;
#93915=CARTESIAN_POINT ( 'NONE',  ( 6.457005528859116161, 41.52802923978755700, -70.63630686878374831 ) ) ;
#93921=COLOUR_RGB ( '', 0.66274510, 0.83137255, 0.94901961) ;
#93922=EDGE_CURVE ( 'NONE', #81281, #10685, #37758, .T. ) ;
#93930=CARTESIAN_POINT ( 'NONE',  ( 5.238621724886622033, 9.104318317904928293, -29.37793476824274919 ) ) ;
#93933=CARTESIAN_POINT ( 'NONE',  ( -4.651132217449170270, -5.000000000000000000, -15.66661053588738106 ) ) ;
#93936=CARTESIAN_POINT ( 'NONE',  ( 7.374560640985523996, -5.000000000000002665, -94.59600210749707117 ) ) ;
#93957=EDGE_LOOP ( 'NONE', ( #78414, #65673, #22349, #10740 ) ) ;
#93967=EDGE_CURVE ( 'NONE', #25935, #67790, #32587, .T. ) ;
#93976=CARTESIAN_POINT ( 'NONE',  ( -10.74465425721712464, 48.00000000000000000, -95.72854256505191017 ) ) ;
#94001=CARTESIAN_POINT ( 'NONE',  ( 62.40452586790289047, 40.83862041121656716, 18.42722372817474152 ) ) ;
#94014=CARTESIAN_POINT ( 'NONE',  ( -1.735558044529530664, 39.99999999999999289, -69.74083754113279099 ) ) ;
#94025=ORIENTED_EDGE ( 'NONE', *, *, #23380, .F. ) ;
#94026=CARTESIAN_POINT ( 'NONE',  ( -7.251642494156320673, 41.54835750584366849, -68.91429205799529711 ) ) ;
#94033=CARTESIAN_POINT ( 'NONE',  ( 7.036764706176849238, 40.29466777802799271, -71.06385277369803077 ) ) ;
#94047=CARTESIAN_POINT ( 'NONE',  ( -4.872636585019907152, 41.00341550150753278, -70.74912563391391984 ) ) ;
#94060=ORIENTED_EDGE ( 'NONE', *, *, #68341, .T. ) ;
#94067=ORIENTED_EDGE ( 'NONE', *, *, #80167, .F. ) ;
#94077=( GEOMETRIC_REPRESENTATION_CONTEXT ( 3 ) GLOBAL_UNCERTAINTY_ASSIGNED_CONTEXT ( ( #94715 ) ) GLOBAL_UNIT_ASSIGNED_CONTEXT ( ( #38904, #31365, #49081 ) ) REPRESENTATION_CONTEXT ( 'NONE', 'WORKASPACE' ) );
#94090=CARTESIAN_POINT ( 'NONE',  ( 10.50000000000000533, -5.000000000000000000, -55.73109922009992800 ) ) ;
#94100=CARTESIAN_POINT ( 'NONE',  ( -15.83991689165957517, -4.333298119783902003, 8.379008989716211886 ) ) ;
#94102=CARTESIAN_POINT ( 'NONE',  ( 6.123233995736763324E-16, 48.00000000000000000, -95.00000000000000000 ) ) ;
#94115=CARTESIAN_POINT ( 'NONE',  ( -6.711450970696149376, 41.78336452847950966, -59.19447405778233673 ) ) ;
#94128=B_SPLINE_CURVE_WITH_KNOTS ( 'NONE', 3,
 ( #75609, #75063, #99333, #10857, #1156, #34129 ),
 .UNSPECIFIED., .F., .F.,
 ( 4, 2, 4 ),
 ( 0.000000000000000000, 0.5000000000000000000, 1.000000000000000000 ),
 .UNSPECIFIED. ) ;
#94135=SURFACE_STYLE_FILL_AREA ( #6168 ) ;
#94145=FILL_AREA_STYLE_COLOUR ( '', #31107 ) ;
#94147=CARTESIAN_POINT ( 'NONE',  ( 6.528715076640351000, 41.70354536979574078, -70.35321457523596678 ) ) ;
#94150=CARTESIAN_POINT ( 'NONE',  ( -37.84772257691307829, 50.00000000000000000, 50.69408796163851605 ) ) ;
#94165=( GEOMETRIC_REPRESENTATION_CONTEXT ( 3 ) GLOBAL_UNCERTAINTY_ASSIGNED_CONTEXT ( ( #30866 ) ) GLOBAL_UNIT_ASSIGNED_CONTEXT ( ( #11343, #42670, #10295 ) ) REPRESENTATION_CONTEXT ( 'NONE', 'WORKASPACE' ) );
#94192=CARTESIAN_POINT ( 'NONE',  ( 10.50000000000000178, -5.000000000000000000, -12.52300748975612166 ) ) ;
#94193=CARTESIAN_POINT ( 'NONE',  ( 52.56483885390524335, 49.99999999999999289, -38.23529411764707220 ) ) ;
#94195=CARTESIAN_POINT ( 'NONE',  ( -2.617478844992341180, 49.99999999999999289, -75.26027323389158141 ) ) ;
#94204=ORIENTED_EDGE ( 'NONE', *, *, #84869, .T. ) ;
#94223=CARTESIAN_POINT ( 'NONE',  ( -5.209583662784837088, 5.600999057173902784, -26.19773573556262392 ) ) ;
#94242=CARTESIAN_POINT ( 'NONE',  ( -18.87830327030985345, 49.99999999999999289, 60.75080805445377763 ) ) ;
#94247=EDGE_CURVE ( 'NONE', #18823, #26788, #56792, .T. ) ;
#94265=CARTESIAN_POINT ( 'NONE',  ( 6.062025480873725947, 50.00000000000000000, -74.52240934977429276 ) ) ;
#94284=CARTESIAN_POINT ( 'NONE',  ( -6.338673264423879239, 41.81695718870634693, -59.02782128990620691 ) ) ;
#94294=ORIENTED_EDGE ( 'NONE', *, *, #82894, .T. ) ;
#94308=CARTESIAN_POINT ( 'NONE',  ( 7.754160006592983656, 42.00000000000000711, 59.23741894013591036 ) ) ;
#94321=VERTEX_POINT ( 'NONE', #54234 ) ;
#94337=CARTESIAN_POINT ( 'NONE',  ( 7.499999999993815614, 40.28819020807626572, -69.28872355931217442 ) ) ;
#94340=ORIENTED_EDGE ( 'NONE', *, *, #25446, .T. ) ;
#94342=DIRECTION ( 'NONE',  ( 0.000000000000000000, 1.000000000000000000, 0.000000000000000000 ) ) ;
#94344=CARTESIAN_POINT ( 'NONE',  ( -7.150000000000001243, 41.64999999999999147, -68.91429205801802027 ) ) ;
#94345=CARTESIAN_POINT ( 'NONE',  ( -14.90155531858861870, 42.58002643027919021, -90.01374843399875658 ) ) ;
#94359=CARTESIAN_POINT ( 'NONE',  ( -13.14930780082137396, -5.000000000000002665, -86.33530272370370540 ) ) ;
#94387=SURFACE_STYLE_FILL_AREA ( #3779 ) ;
#94395=ORIENTED_EDGE ( 'NONE', *, *, #91013, .T. ) ;
#94396=CARTESIAN_POINT ( 'NONE',  ( -8.369914041613094824, 42.00000000000000000, -59.54702718917638293 ) ) ;
#94398=STYLED_ITEM ( 'NONE', ( #100001 ), #38431 ) ;
#94408=CARTESIAN_POINT ( 'NONE',  ( -17.39901153685596924, -5.000000000000000888, 2.593512410382273536 ) ) ;
#94434=CARTESIAN_POINT ( 'NONE',  ( 19.49140471140582775, 49.99885313499811446, 60.08881260961068449 ) ) ;
#94447=CARTESIAN_POINT ( 'NONE',  ( -7.500000000000003553, 11.93422428098184263, -34.62196993281244062 ) ) ;
#94460=CARTESIAN_POINT ( 'NONE',  ( 6.040020869836456363, 40.93519827235615338, -71.09856442099673757 ) ) ;
#94471=CARTESIAN_POINT ( 'NONE',  ( 5.322129082409281509, 24.97845467789381857, -43.70420610338506151 ) ) ;
#94472=CARTESIAN_POINT ( 'NONE',  ( 12.48545062700847019, -3.553405299047675658, -13.69229322019752537 ) ) ;
#94474=STYLED_ITEM ( 'NONE', ( #55381 ), #27260 ) ;
#94479=CARTESIAN_POINT ( 'NONE',  ( -1.570796324976843295, -5.000000000000002665, -97.00000000000000000 ) ) ;
#94497=ADVANCED_FACE ( 'NONE', ( #87174 ), #37810, .T. ) ;
#94512=CARTESIAN_POINT ( 'NONE',  ( 3.122594241928703163, -5.000000000000000888, -73.30485703407919118 ) ) ;
#94530=CARTESIAN_POINT ( 'NONE',  ( 18.91781669292794987, 48.00000000000000000, 62.18610382930901892 ) ) ;
#94537=CARTESIAN_POINT ( 'NONE',  ( 28.01586531120660339, 43.41400263758725231, -71.98455296551246363 ) ) ;
#94546=CARTESIAN_POINT ( 'NONE',  ( 51.76085035120648570, 42.00000000008225953, -29.83308852628573860 ) ) ;
#94554=CARTESIAN_POINT ( 'NONE',  ( 64.91130259009537440, 39.42582562355791254, 6.834900822117297103 ) ) ;
#94574=CARTESIAN_POINT ( 'NONE',  ( -11.99999999999999467, 50.00000000000000000, -83.42920367502570400 ) ) ;
#94601=CARTESIAN_POINT ( 'NONE',  ( -5.273744844849142410, 41.55406142698797822, -70.69180546971138313 ) ) ;
#94634=CARTESIAN_POINT ( 'NONE',  ( 7.043654982242377294, 41.66078771780808410, -59.26734080171946317 ) ) ;
#94649=CARTESIAN_POINT ( 'NONE',  ( 11.09711298024378046, -4.982652786778980492, -12.57750780562587423 ) ) ;
#94656=CARTESIAN_POINT ( 'NONE',  ( -17.82150094935625972, -4.333298119783937530, -1.872127852610514731 ) ) ;
#94668=CARTESIAN_POINT ( 'NONE',  ( 63.03617022297318329, 49.99999999997997691, -16.93907820452584545 ) ) ;
#94673=CARTESIAN_POINT ( 'NONE',  ( -5.469234196618169896, 41.99717955803384939, -59.59612311059226641 ) ) ;
#94681=CARTESIAN_POINT ( 'NONE',  ( 18.48567378316023735, 49.99999999999999289, 61.27610688997057053 ) ) ;
#94702=CARTESIAN_POINT ( 'NONE',  ( 5.385153946026782990, 41.85687303129803638, -70.29203007274306003 ) ) ;
#94715=UNCERTAINTY_MEASURE_WITH_UNIT (LENGTH_MEASURE( 1.000000000000000082E-05 ), #38904, 'distance_accuracy_value', 'NONE');
#94723=ORIENTED_EDGE ( 'NONE', *, *, #36163, .T. ) ;
#94731=ORIENTED_EDGE ( 'NONE', *, *, #54250, .T. ) ;
#94743=CARTESIAN_POINT ( 'NONE',  ( 6.145467200821944864, 49.99999999999999289, -77.00333157708759302 ) ) ;
#94769=CARTESIAN_POINT ( 'NONE',  ( -5.293182415613770786, 18.41909107384472932, -37.79627497856930773 ) ) ;
#94776=CARTESIAN_POINT ( 'NONE',  ( -6.757705282517541434, 41.35007050579768162, -70.67351639275690900 ) ) ;
#94786=EDGE_CURVE ( 'NONE', #26788, #12195, #73614, .T. ) ;
#94787=CARTESIAN_POINT ( 'NONE',  ( -17.61824857587188831, 50.00000000000002132, 62.61717692869397922 ) ) ;
#94802=CARTESIAN_POINT ( 'NONE',  ( -13.43927643640219571, 42.84659330639521357, -92.02404953342519889 ) ) ;
#94821=CARTESIAN_POINT ( 'NONE',  ( -5.754767142552475789, 41.95837106010883133, -69.99684969509513621 ) ) ;
#94827=CARTESIAN_POINT ( 'NONE',  ( -5.668093984624058557, 41.44782703750503572, -58.47096610491104229 ) ) ;
#94836=ORIENTED_EDGE ( 'NONE', *, *, #30311, .F. ) ;
#94846=CARTESIAN_POINT ( 'NONE',  ( -37.36680950590233863, 18.64316884713579725, 10.04205104295027517 ) ) ;
#94877=COLOUR_RGB ( '', 0.66274510, 0.83137255, 0.94901961) ;
#94883=( NAMED_UNIT ( * ) PLANE_ANGLE_UNIT ( ) SI_UNIT ( $, .RADIAN. ) );
#94895=CARTESIAN_POINT ( 'NONE',  ( 12.67000837003893210, -5.000000000000002665, -88.76274061128376047 ) ) ;
#94905=FILL_AREA_STYLE_COLOUR ( '', #62116 ) ;
#94913=DIRECTION ( 'NONE',  ( 0.000000000000000000, 0.000000000000000000, 1.000000000000000000 ) ) ;
#94933=CARTESIAN_POINT ( 'NONE',  ( 1.816153886384288096, 42.00000000001274714, -59.31995585001071447 ) ) ;
#94944=CARTESIAN_POINT ( 'NONE',  ( 6.648792466258503175, -5.000000000000000000, 15.29529797603218810 ) ) ;
#94945=( BOUNDED_SURFACE ( )  B_SPLINE_SURFACE ( 2, 3, ( 
 ( #67392, #59301, #41505, #74393 ),
 ( #472, #83552, #67911, #75465 ),
 ( #91145, #100274, #50126, #10718 ) ),
 .UNSPECIFIED., .F., .F., .T. ) 
 B_SPLINE_SURFACE_WITH_KNOTS ( ( 3, 3 ),
 ( 4, 4 ),
 ( 0.000000000000000000, 1.000000000000000000 ),
 ( 2.852999002495562930, 3.430186304684023302 ),
 .UNSPECIFIED. ) 
 GEOMETRIC_REPRESENTATION_ITEM ( )  RATIONAL_B_SPLINE_SURFACE ( (
 ( 1.000000000000000000, 1.000000000000000000, 1.000000000000000000, 1.000000000000000000),
 ( 1.857142857142858317, 1.857142857142858317, 1.857142857142858317, 1.857142857142858317),
 ( 1.000000000000000000, 1.000000000000000000, 1.000000000000000000, 1.000000000000000000) ) ) 
 REPRESENTATION_ITEM ( '' )  SURFACE ( )  );
#94966=CARTESIAN_POINT ( 'NONE',  ( 18.95131366490356939, 49.31567518127548766, 62.02443497815841056 ) ) ;
#94992=CARTESIAN_POINT ( 'NONE',  ( -18.92655221378187491, 49.02800889251220440, 62.11188204109627264 ) ) ;
#94994=CARTESIAN_POINT ( 'NONE',  ( 6.855074334103434808, 40.29457790742911527, -71.16068745972087584 ) ) ;
#94997=CARTESIAN_POINT ( 'NONE',  ( 10.50000000000000711, -5.000000000000000000, -55.73109925765190553 ) ) ;
#95008=CARTESIAN_POINT ( 'NONE',  ( 5.302285649869180162, 20.37004371428214000, -39.55474687996256478 ) ) ;
#95009=CARTESIAN_POINT ( 'NONE',  ( 12.48649638673671802, -3.535767641867485711, -13.71266585591266818 ) ) ;
#95013=CARTESIAN_POINT ( 'NONE',  ( 6.145467200820721843, -5.000000000000002665, -77.00333157708637088 ) ) ;
#95048=CARTESIAN_POINT ( 'NONE',  ( -6.256238905932293370, -3.000000000000353495, -71.20382035666706599 ) ) ;
#95052=CARTESIAN_POINT ( 'NONE',  ( -2.354803500934599558, 48.00000000000000000, -100.0000000000000000 ) ) ;
#95057=CARTESIAN_POINT ( 'NONE',  ( -42.47818524942086071, 39.50286766178945186, -49.65699901859316867 ) ) ;
#95064=CARTESIAN_POINT ( 'NONE',  ( 30.58918467992911872, 43.16177272848633351, -68.44682372717235808 ) ) ;
#95074=CARTESIAN_POINT ( 'NONE',  ( 51.76085035121451483, 41.99999999999999289, 29.83308852632746522 ) ) ;
#95083=CARTESIAN_POINT ( 'NONE',  ( -28.75528690196496839, 39.42481417973143465, 58.36921663661286175 ) ) ;
#95114=CARTESIAN_POINT ( 'NONE',  ( -7.500000000000007105, -4.999999999999999112, -52.94236561372731131 ) ) ;
#95126=CARTESIAN_POINT ( 'NONE',  ( -5.597109339400236472, 41.52722309069373097, -70.77038831392039242 ) ) ;
#95140=ORIENTED_EDGE ( 'NONE', *, *, #79363, .T. ) ;
#95146=CARTESIAN_POINT ( 'NONE',  ( -12.50000000000000533, 27.12381979734430004, -44.66014792738449302 ) ) ;
#95153=CARTESIAN_POINT ( 'NONE',  ( 6.786616689952412074, 41.72678941544184994, -59.11526159199856068 ) ) ;
#95173=CARTESIAN_POINT ( 'NONE',  ( 7.500000000000007105, 40.00000000000000000, -58.09827136975972905 ) ) ;
#95186=CARTESIAN_POINT ( 'NONE',  ( 5.774137037018601148, 50.00000000000000000, 63.00000000000000000 ) ) ;
#95192=CARTESIAN_POINT ( 'NONE',  ( -7.049753390875842740, 41.74264178408463977, -59.69459095116845759 ) ) ;
#95193=CARTESIAN_POINT ( 'NONE',  ( 12.17614236696284813, -4.623354119923609673, -76.80722648406000985 ) ) ;
#95200=CARTESIAN_POINT ( 'NONE',  ( 18.82548581215701944, 50.00000000000000711, 60.82217600870657748 ) ) ;
#95251=B_SPLINE_CURVE_WITH_KNOTS ( 'NONE', 3,
 ( #87119, #37531, #63380, #46637, #21870, #22403 ),
 .UNSPECIFIED., .F., .F.,
 ( 4, 2, 4 ),
 ( 0.000000000000000000, 0.5000000000000000000, 1.000000000000000000 ),
 .UNSPECIFIED. ) ;
#95263=CARTESIAN_POINT ( 'NONE',  ( 5.036189802311931807, 48.00000000000000000, -93.73786388412125348 ) ) ;
#95274=CARTESIAN_POINT ( 'NONE',  ( -7.500000000000007105, 39.99999999999998579, -68.91429205786793943 ) ) ;
#95287=CARTESIAN_POINT ( 'NONE',  ( -5.221476981229875136, 6.992073347021172225, -27.46175062982092996 ) ) ;
#95301=DIRECTION ( 'NONE',  ( 0.000000000000000000, 1.000000000000000000, 0.000000000000000000 ) ) ;
#95302=CARTESIAN_POINT ( 'NONE',  ( -46.55033485923301129, 41.07609223179107261, -46.50387006460696426 ) ) ;
#95303=CARTESIAN_POINT ( 'NONE',  ( -17.57798479617512655, 49.99999999999999289, 62.77754979738582364 ) ) ;
#95337=CARTESIAN_POINT ( 'NONE',  ( -6.917891564935159998, 41.82074884801031800, -68.91429205806258551 ) ) ;
#95341=CARTESIAN_POINT ( 'NONE',  ( 3.302481927409230966, -4.999999999999999112, 16.08827426322715581 ) ) ;
#95342=CARTESIAN_POINT ( 'NONE',  ( -5.420469775605653240, 41.88321586335170821, -59.04137891894602319 ) ) ;
#95359=CARTESIAN_POINT ( 'NONE',  ( 6.986467729351123701, 41.76526144824654807, -59.56845322044426183 ) ) ;
#95360=CARTESIAN_POINT ( 'NONE',  ( 15.50526908259248593, 42.00000000004113332, 57.69562748392037577 ) ) ;
#95405=CARTESIAN_POINT ( 'NONE',  ( -14.73122683063152571, -5.000000000000002665, -81.05502296678268692 ) ) ;
#95419=CARTESIAN_POINT ( 'NONE',  ( -18.91781669292785395, 48.00000000000000000, 62.18610382930904734 ) ) ;
#95433=CARTESIAN_POINT ( 'NONE',  ( -52.56483885390523625, -79.93083296558610584, -38.23529411764706509 ) ) ;
#95474=CARTESIAN_POINT ( 'NONE',  ( 19.23821838457499922, 49.80979460016762062, 61.48217125059658628 ) ) ;
#95485=UNCERTAINTY_MEASURE_WITH_UNIT (LENGTH_MEASURE( 1.000000000000000082E-05 ), #56930, 'distance_accuracy_value', 'NONE');
#95501=CARTESIAN_POINT ( 'NONE',  ( 5.308064239167483045, 41.67430808361709182, -70.56675995020944470 ) ) ;
#95504=CARTESIAN_POINT ( 'NONE',  ( 12.49999999999999822, -4.999999999999999112, -11.21398294031200216 ) ) ;
#95523=CARTESIAN_POINT ( 'NONE',  ( 1.308996937480704670, -3.000000000000002665, -95.00000000000000000 ) ) ;
#95571=CARTESIAN_POINT ( 'NONE',  ( 6.831363830528337289, 41.73171983268898089, -59.17722554277374059 ) ) ;
#95581=CARTESIAN_POINT ( 'NONE',  ( 39.05849473363845448, 42.03646466411915839, -56.80344740562036066 ) ) ;
#95592=CARTESIAN_POINT ( 'NONE',  ( -5.022013495247517945, 18.64316884711714195, -38.36535705883633085 ) ) ;
#95597=CARTESIAN_POINT ( 'NONE',  ( 59.27210092795512253, 39.42463516292936276, 26.84561385324717264 ) ) ;
#95613=CARTESIAN_POINT ( 'NONE',  ( 8.737863884124120517, 49.99999999999999289, -90.03618980230058355 ) ) ;
#95636=DIRECTION ( 'NONE',  ( 0.000000000000000000, 0.000000000000000000, 1.000000000000000000 ) ) ;
#95665=CARTESIAN_POINT ( 'NONE',  ( -12.50000000000000711, 39.72072293383548214, -64.90088073866644436 ) ) ;
#95702=CARTESIAN_POINT ( 'NONE',  ( 7.996668423981797780, -3.000000000000003109, -78.85453280025085121 ) ) ;
#95709=CARTESIAN_POINT ( 'NONE',  ( -62.59524157943269529, 48.00000000000000000, 18.50207713769755102 ) ) ;
#95721=CARTESIAN_POINT ( 'NONE',  ( 18.79996295430579423, 50.00000000000000711, 60.85687850329983206 ) ) ;
#95732=CARTESIAN_POINT ( 'NONE',  ( 53.14262477155799758, 49.99999999999999289, 33.99861374406009418 ) ) ;
#95766=SURFACE_SIDE_STYLE ('',( #26420 ) ) ;
#95780=FILL_AREA_STYLE ('',( #103341 ) ) ;
#95787=CARTESIAN_POINT ( 'NONE',  ( 7.996668422911924701, 48.00000000000000000, -91.14546720081904141 ) ) ;
#95806=B_SPLINE_CURVE_WITH_KNOTS ( 'NONE', 3,
 ( #70893, #52571, #3508, #36448, #69315, #12114, #85494, #19734, #103263, #21313, #29925, #102194, #95702, #36968, #2957, #28341, #13702, #62812 ),
 .UNSPECIFIED., .F., .F.,
 ( 4, 2, 2, 2, 2, 2, 2, 2, 4 ),
 ( 0.5000000000000000000, 0.5625000000000000000, 0.6250000000000000000, 0.6875000000000000000, 0.7500000000000000000, 0.8125000000000000000, 0.8750000000000000000, 0.9375000000000000000, 1.000000000000000000 ),
 .UNSPECIFIED. ) ;
#95807=FILL_AREA_STYLE ('',( #61325 ) ) ;
#95814=CARTESIAN_POINT ( 'NONE',  ( 2.617993873628327250, -5.000000000000000000, 10.00000000000000000 ) ) ;
#95830=CARTESIAN_POINT ( 'NONE',  ( -16.51907061138358657, 42.00139744608743086, -87.79003255390425409 ) ) ;
#95831=CARTESIAN_POINT ( 'NONE',  ( -17.97115738240404781, 50.00000000000000711, 61.92613045224233304 ) ) ;
#95838=SURFACE_SIDE_STYLE ('',( #20938 ) ) ;
#95847=FILL_AREA_STYLE_COLOUR ( '', #82121 ) ;
#95854=STYLED_ITEM ( 'NONE', ( #70965 ), #23751 ) ;
#95859=B_SPLINE_CURVE_WITH_KNOTS ( 'NONE', 3,
 ( #10418, #75145, #1240, #34211, #58992, #91880, #18007, #9884 ),
 .UNSPECIFIED., .F., .F.,
 ( 4, 2, 2, 4 ),
 ( 0.1960348326659903384, 0.3970261244994927607, 0.5980174163329952108, 1.000000000000000000 ),
 .UNSPECIFIED. ) ;
#95869=( BOUNDED_SURFACE ( )  B_SPLINE_SURFACE ( 2, 3, ( 
 ( #6920, #39841, #65160, #87860, #54932, #13944, #15007, #23672, #14464, #106675, #79750, #89450, #5857, #24207, #22626, #55979, #71648, #63594 ),
 ( #16077, #48436, #98056, #105102, #38782, #55458, #15542, #47899, #88913, #104555, #88390, #57057, #89973, #80805, #47379, #40889, #48957, #72714 ),
 ( #7437, #80269, #6382, #39317, #106132, #73775, #81854, #64637, #72197, #31242, #97508, #32823, #105617, #31756, #40354, #73231, #32290, #7977 ) ),
 .UNSPECIFIED., .F., .T., .T. ) 
 B_SPLINE_SURFACE_WITH_KNOTS ( ( 3, 3 ),
 ( 4, 2, 2, 2, 2, 2, 2, 2, 4 ),
 ( 0.000000000000000000, 1.000000000000000000 ),
 ( 0.000000000000000000, 0.7853981633974482790, 1.570796326794896558, 2.356194490192344837, 3.141592653589793116, 3.926990816987241395, 4.712388980384689674, 5.497787143782137953, 6.283185307179586232 ),
 .UNSPECIFIED. ) 
 GEOMETRIC_REPRESENTATION_ITEM ( )  RATIONAL_B_SPLINE_SURFACE ( (
 ( 1.000000000000000000, 1.000000000000000000, 1.000000000000000000, 1.000000000000000000, 1.000000000000000000, 1.000000000000000000, 1.000000000000000000, 1.000000000000000000, 1.000000000000000000, 1.000000000000000000, 1.000000000000000000, 1.000000000000000000, 1.000000000000000000, 1.000000000000000000, 1.000000000000000000, 1.000000000000000000, 1.000000000000000000, 1.000000000000000000),
 ( 1.857142857142858317, 1.857142857142858317, 1.857142857142858317, 1.857142857142858317, 1.857142857142858317, 1.857142857142858317, 1.857142857142858317, 1.857142857142858317, 1.857142857142858317, 1.857142857142858317, 1.857142857142858317, 1.857142857142858317, 1.857142857142858317, 1.857142857142858317, 1.857142857142858317, 1.857142857142858317, 1.857142857142858317, 1.857142857142858317),
 ( 1.000000000000000000, 1.000000000000000000, 1.000000000000000000, 1.000000000000000000, 1.000000000000000000, 1.000000000000000000, 1.000000000000000000, 1.000000000000000000, 1.000000000000000000, 1.000000000000000000, 1.000000000000000000, 1.000000000000000000, 1.000000000000000000, 1.000000000000000000, 1.000000000000000000, 1.000000000000000000, 1.000000000000000000, 1.000000000000000000) ) ) 
 REPRESENTATION_ITEM ( '' )  SURFACE ( )  );
#95874=CARTESIAN_POINT ( 'NONE',  ( -6.214520335144379182, 41.72338998088525841, -70.49303492603483789 ) ) ;
#95879=CARTESIAN_POINT ( 'NONE',  ( 14.78938945996223886, -5.000000000000000000, 7.149827492542583762 ) ) ;
#95885=CARTESIAN_POINT ( 'NONE',  ( -7.149999999999890221, 41.65000000000012648, -59.82695526680724640 ) ) ;
#95895=CARTESIAN_POINT ( 'NONE',  ( 6.394717868937521921, 41.92174093517635924, -59.37671486230904350 ) ) ;
#95930=FILL_AREA_STYLE ('',( #104001 ) ) ;
#95949=CARTESIAN_POINT ( 'NONE',  ( 14.82275922442112304, -4.333298119783705715, -10.06958627548034535 ) ) ;
#95979=CARTESIAN_POINT ( 'NONE',  ( 7.232205791931205496, 41.33266196706463802, -58.20097105119658920 ) ) ;
#95992=CARTESIAN_POINT ( 'NONE',  ( 1.301042606982605321E-15, -5.000000000000000000, -10.00000000000000000 ) ) ;
#96007=ORIENTED_EDGE ( 'NONE', *, *, #84151, .F. ) ;
#96014=CARTESIAN_POINT ( 'NONE',  ( 19.23019573275864502, 49.80287270500782171, 61.49929745255238345 ) ) ;
#96039=CARTESIAN_POINT ( 'NONE',  ( -19.42844902724960576, 49.96150201163990801, 60.80087220774903756 ) ) ;
#96060=CARTESIAN_POINT ( 'NONE',  ( 9.999999999999994671, -3.000000000000002665, -86.30899693747679180 ) ) ;
#96070=CARTESIAN_POINT ( 'NONE',  ( 6.108201232855582141, -4.361520614648577876, -16.81796607653726383 ) ) ;
#96091=CARTESIAN_POINT ( 'NONE',  ( -4.852941176470594975, -4.999999999999998224, -70.80672828634229177 ) ) ;
#96102=CARTESIAN_POINT ( 'NONE',  ( 7.149999999999997691, 41.65000000000000568, -59.82695526683420439 ) ) ;
#96112=CARTESIAN_POINT ( 'NONE',  ( 43.55231887857613771, 41.43784824290622026, -50.62546061442120759 ) ) ;
#96124=CARTESIAN_POINT ( 'NONE',  ( 30.67950393665801556, 18.64316884713159794, -23.57730434125293328 ) ) ;
#96130=CARTESIAN_POINT ( 'NONE',  ( -63.38584389458259949, 38.95340125770254502, 6.668509187926899173 ) ) ;
#96149=CARTESIAN_POINT ( 'NONE',  ( 9.739726766101595601, 49.99999999999999289, -87.61747884500120165 ) ) ;
#96157=SURFACE_STYLE_FILL_AREA ( #72910 ) ;
#96205=CARTESIAN_POINT ( 'NONE',  ( -12.50000000000000711, 39.71451000310032953, -64.87831219546262673 ) ) ;
#96217=CARTESIAN_POINT ( 'NONE',  ( 6.738100180926640093, 41.71798714554645215, -59.05424661244425266 ) ) ;
#96226=CARTESIAN_POINT ( 'NONE',  ( 7.141975279388227626, -3.000000000000119016, -70.98863559356006192 ) ) ;
#96236=CARTESIAN_POINT ( 'NONE',  ( 7.500000000000008882, 42.00000000000000711, -72.67206406577979294 ) ) ;
#96252=MECHANICAL_DESIGN_GEOMETRIC_PRESENTATION_REPRESENTATION('',(#106612),#87620);
#96256=CARTESIAN_POINT ( 'NONE',  ( 62.91825180719526145, 50.00000000000000000, 6.605622457241173251 ) ) ;
#96260=ADVANCED_FACE ( 'NONE', ( #42875 ), #68003, .T. ) ;
#96280=CARTESIAN_POINT ( 'NONE',  ( 50.32385735845999619, 50.00000000000000711, 38.04681602700239296 ) ) ;
#96291=CARTESIAN_POINT ( 'NONE',  ( 6.916165809215955917, 41.81554757990602411, -59.83173451229081508 ) ) ;
#96292=CARTESIAN_POINT ( 'NONE',  ( -5.412925220531727533, 41.84428781238603534, -58.95471249783204115 ) ) ;
#96302=EDGE_CURVE ( 'NONE', #61410, #25935, #99958, .T. ) ;
#96305=CARTESIAN_POINT ( 'NONE',  ( 7.343811558498933856, 40.90986947426189602, -58.79603989316886725 ) ) ;
#96315=CARTESIAN_POINT ( 'NONE',  ( -12.00013170160833731, -5.000000000000000000, -83.40936345630457538 ) ) ;
#96330=CARTESIAN_POINT ( 'NONE',  ( 9.999999999999994671, 48.00000000000000000, -83.69100306252322241 ) ) ;
#96346=SURFACE_STYLE_USAGE ( .BOTH. , #54786 ) ;
#96351=CARTESIAN_POINT ( 'NONE',  ( 8.922269033010996608, -5.000000000000000000, -5.219866590717683330 ) ) ;
#96354=CARTESIAN_POINT ( 'NONE',  ( -5.288744022479204610, 17.47836613358154878, -36.94789734229802747 ) ) ;
#96355=UNCERTAINTY_MEASURE_WITH_UNIT (LENGTH_MEASURE( 1.000000000000000082E-05 ), #38133, 'distance_accuracy_value', 'NONE');
#96374=CARTESIAN_POINT ( 'NONE',  ( -17.60285536070160717, 50.00000000000000000, 62.67515953917209259 ) ) ;
#96380=CARTESIAN_POINT ( 'NONE',  ( 17.50000000000003197, 50.00117660290610644, 59.93398959461712394 ) ) ;
#96389=CARTESIAN_POINT ( 'NONE',  ( -13.43923917260470802, 42.84657065243760599, -92.02410076267699424 ) ) ;
#96397=CARTESIAN_POINT ( 'NONE',  ( 6.821510612526563655, 41.53001914900257674, -70.37925568709802349 ) ) ;
#96407=FILL_AREA_STYLE ('',( #20966 ) ) ;
#96432=CARTESIAN_POINT ( 'NONE',  ( 5.682852296829431715, 41.94661659677129961, -59.19459671036732118 ) ) ;
#96454=STYLED_ITEM ( 'NONE', ( #82167 ), #70542 ) ;
#96456=B_SPLINE_CURVE_WITH_KNOTS ( 'NONE', 3,
 ( #52030, #69820, #84940, #5086, #27282, #68777, #11029, #87078, #45558, #43947, #102179, #45030, #86028, #4553, #27816, #77914, #38019, #12099, #20794, #94649, #60685, #76837, #61205, #93573, #20258, #12621, #44492, #4024, #2946 ),
 .UNSPECIFIED., .F., .F.,
 ( 4, 2, 2, 2, 2, 1, 2, 2, 2, 2, 2, 1, 1, 2, 2, 4 ),
 ( 0.000000000000000000, 0.2500000000000769385, 0.3750000000001154077, 0.4375000000001358358, 0.4687500000001451061, 0.4843750000001488809, 0.4921875000001501577, 0.5000000000001513234, 0.6250000000001735279, 0.6875000000001847411, 0.7187500000001917355, 0.7343750000001952882, 0.7421875000001948441, 0.7460937500001922906, 0.7500000000001897371, 1.000000000000000000 ),
 .UNSPECIFIED. ) ;
#96479=CARTESIAN_POINT ( 'NONE',  ( 1.757245493114544477, -4.333298119783830060, 17.83319508841386281 ) ) ;
#96480=CARTESIAN_POINT ( 'NONE',  ( 51.48757442383973881, 38.95383793068620548, -37.45149417477089315 ) ) ;
#96487=FACE_OUTER_BOUND ( 'NONE', #2214, .T. ) ;
#96489=CARTESIAN_POINT ( 'NONE',  ( 12.00013170160833909, -5.000000000000000000, -86.59063654373593977 ) ) ;
#96505=MECHANICAL_DESIGN_GEOMETRIC_PRESENTATION_REPRESENTATION('',(#31100),#44859);
#96508=ADVANCED_FACE ( 'NONE', ( #13950, #96487, #104560, #22630 ), #64136, .F. ) ;
#96527=EDGE_LOOP ( 'NONE', ( #50072, #48899, #23367, #85422 ) ) ;
#96531=CARTESIAN_POINT ( 'NONE',  ( -55.59873597034283677, 48.00000000000001421, -34.06437516161200563 ) ) ;
#96545=CARTESIAN_POINT ( 'NONE',  ( 19.36667751815805971, 49.91424520787322194, 61.11596122090848127 ) ) ;
#96568=CARTESIAN_POINT ( 'NONE',  ( -19.45839315690574622, 49.98279635927520559, 60.54808333947917021 ) ) ;
#96574=CARTESIAN_POINT ( 'NONE',  ( 10.50000000000000000, -5.000000000000000000, -11.21398294031086706 ) ) ;
#96588=CARTESIAN_POINT ( 'NONE',  ( 2.093983074874241623, -3.000000000000000444, 7.791781413346523522 ) ) ;
#96591=CARTESIAN_POINT ( 'NONE',  ( 9.999999999999996447, -5.000000000000002665, -83.69100306251233690 ) ) ;
#96604=CARTESIAN_POINT ( 'NONE',  ( 7.022229286271609361, -4.221542269094411992, -17.11103215588190807 ) ) ;
#96620=CARTESIAN_POINT ( 'NONE',  ( -6.256238905642391934, -5.000000000004484413, -71.20382033075676986 ) ) ;
#96658=CARTESIAN_POINT ( 'NONE',  ( -2.958297520906366884, 39.42457334331769658, 65.00031284538987109 ) ) ;
#96675=CARTESIAN_POINT ( 'NONE',  ( -9.739726766104285005, 48.00000000000000000, -82.38252115500968387 ) ) ;
#96680=STYLED_ITEM ( 'NONE', ( #36337 ), #105888 ) ;
#96697=PRESENTATION_STYLE_ASSIGNMENT (( #71875 ) ) ;
#96703=CARTESIAN_POINT ( 'NONE',  ( 7.758748231342716295, -5.000000000000001776, -73.00623724565090811 ) ) ;
#96706=MECHANICAL_DESIGN_GEOMETRIC_PRESENTATION_REPRESENTATION('',(#19224),#57029);
#96718=CARTESIAN_POINT ( 'NONE',  ( 6.757705285491359071, 41.35007050631321590, -70.67351639401239538 ) ) ;
#96722=ORIENTED_EDGE ( 'NONE', *, *, #43163, .F. ) ;
#96729=CARTESIAN_POINT ( 'NONE',  ( 9.797174393178825657E-16, 0.000000000000000000, -8.000000000000000000 ) ) ;
#96733=MECHANICAL_DESIGN_GEOMETRIC_PRESENTATION_REPRESENTATION('',(#21011),#51977);
#96742=MECHANICAL_DESIGN_GEOMETRIC_PRESENTATION_REPRESENTATION('',(#69184),#93275);
#96758=CARTESIAN_POINT ( 'NONE',  ( 7.500000000000007105, 42.00000000000000711, -58.09827136975972195 ) ) ;
#96764=CIRCLE ( 'NONE', #58891, 60.00000000000000000 ) ;
#96769=CARTESIAN_POINT ( 'NONE',  ( 43.69716417780046669, 40.83906611472173864, 48.48761666258860714 ) ) ;
#96774=CARTESIAN_POINT ( 'NONE',  ( -64.91565662645538737, 49.99999999999999289, 6.815324757469617190 ) ) ;
#96779=CARTESIAN_POINT ( 'NONE',  ( 12.19670133565572101, -4.599518202331234207, -76.80113241245393851 ) ) ;
#96786=CARTESIAN_POINT ( 'NONE',  ( 17.95249423762719232, 50.00000000000002132, 61.95147677239601336 ) ) ;
#96814=MECHANICAL_DESIGN_GEOMETRIC_PRESENTATION_REPRESENTATION('',(#103650),#105429);
#96838=VERTEX_POINT ( 'NONE', #82224 ) ;
#96841=CARTESIAN_POINT ( 'NONE',  ( 14.91338090413177397, 41.98696021714862781, -86.62221405687444076 ) ) ;
#96850=CARTESIAN_POINT ( 'NONE',  ( 6.980486755139912911E-15, 47.00000000000000000, -56.99999999999999289 ) ) ;
#96855=( NAMED_UNIT ( * ) SI_UNIT ( $, .STERADIAN. ) SOLID_ANGLE_UNIT ( ) );
#96861=CARTESIAN_POINT ( 'NONE',  ( -7.500000000000006217, 40.28748324523081692, -68.91429205787007106 ) ) ;
#96886=CARTESIAN_POINT ( 'NONE',  ( -37.47001784820132286, 40.63832974404387244, -58.98724207561210164 ) ) ;
#96895=CARTESIAN_POINT ( 'NONE',  ( 17.50000000000007105, 48.29516379690422667, 64.09945637124668849 ) ) ;
#96903=CARTESIAN_POINT ( 'NONE',  ( -9.537140126497302361, -5.000000000000002665, -20.99850997557460985 ) ) ;
#96905=COLOUR_RGB ( '', 0.72549020, 0.75294118, 0.79215686) ;
#96948=CARTESIAN_POINT ( 'NONE',  ( 5.425084639653764640, 41.91238126396859798, -59.10640578674440349 ) ) ;
#96949=CARTESIAN_POINT ( 'NONE',  ( 5.022013495247499293, 18.64316884711714195, -38.36535705883633085 ) ) ;
#96956=ORIENTED_EDGE ( 'NONE', *, *, #71716, .T. ) ;
#96964=EDGE_LOOP ( 'NONE', ( #24130, #11083, #22884, #71244 ) ) ;
#96985=CARTESIAN_POINT ( 'NONE',  ( -12.48044894998514742, -3.649665456917388973, -76.71620004746266375 ) ) ;
#97024=CARTESIAN_POINT ( 'NONE',  ( -6.298933871243637128, 41.33266196705881157, -58.30935828777566599 ) ) ;
#97025=CARTESIAN_POINT ( 'NONE',  ( -12.50000000000000355, -3.000000000000001776, -76.70872284621019332 ) ) ;
#97056=CARTESIAN_POINT ( 'NONE',  ( 19.43573259364688965, 49.96699249044939961, 60.75465309941666447 ) ) ;
#97080=CARTESIAN_POINT ( 'NONE',  ( -19.44565830096107106, 49.97416012492340087, 60.66528512595754563 ) ) ;
#97084=( LENGTH_UNIT ( ) NAMED_UNIT ( * ) SI_UNIT ( .MILLI., .METRE. ) );
#97087=PRESENTATION_STYLE_ASSIGNMENT (( #39407 ) ) ;
#97101=CARTESIAN_POINT ( 'NONE',  ( 8.000000000000001776, -2.999999999999999556, 1.047197551196597853 ) ) ;
#97105=CARTESIAN_POINT ( 'NONE',  ( -9.999999999999996447, -5.000000000000002665, -83.69100306252320820 ) ) ;
#97114=CARTESIAN_POINT ( 'NONE',  ( 6.618366600630476881, -4.380080200177129512, -16.79229307443610608 ) ) ;
#97148=CARTESIAN_POINT ( 'NONE',  ( -11.68767211932356531, -5.000000000000002665, -81.85902538601600043 ) ) ;
#97154=CARTESIAN_POINT ( 'NONE',  ( 7.500000000000005329, 24.91666666666666430, -71.71180648257555390 ) ) ;
#97162=CARTESIAN_POINT ( 'NONE',  ( -2.370187320824404864, -5.000000000000000000, -97.83589316745488418 ) ) ;
#97169=CARTESIAN_POINT ( 'NONE',  ( 63.23722314639035602, 38.95364102865269018, -7.942460742852443190 ) ) ;
#97190=CARTESIAN_POINT ( 'NONE',  ( 2.617478844991759868, 50.00000000000001421, -94.73972676610910071 ) ) ;
#97231=CARTESIAN_POINT ( 'NONE',  ( 7.316989716473759842, 41.06054036619742220, -70.27553886509497261 ) ) ;
#97289=CARTESIAN_POINT ( 'NONE',  ( -5.625019081819782052, 41.66287055468434630, -70.61600276915974916 ) ) ;
#97293=ORIENTED_EDGE ( 'NONE', *, *, #7981, .F. ) ;
#97309=ORIENTED_EDGE ( 'NONE', *, *, #10831, .T. ) ;
#97313=CARTESIAN_POINT ( 'NONE',  ( -12.50000000000000178, 11.21173275031592809, -29.16573290955443909 ) ) ;
#97319=CARTESIAN_POINT ( 'NONE',  ( 5.500000018435954097, 42.00000000000000000, -68.91429207046174099 ) ) ;
#97339=FILL_AREA_STYLE ('',( #64472 ) ) ;
#97347=CARTESIAN_POINT ( 'NONE',  ( 16.51905981272399870, 42.00139749746809059, -87.79004739960677739 ) ) ;
#97359=CARTESIAN_POINT ( 'NONE',  ( -52.56483885390523625, 48.00000000000000000, -38.23529411764706509 ) ) ;
#97375=SURFACE_STYLE_FILL_AREA ( #29007 ) ;
#97380=PRESENTATION_STYLE_ASSIGNMENT (( #14870 ) ) ;
#97398=CARTESIAN_POINT ( 'NONE',  ( 17.50000000000567368, 49.98040874966400082, 61.78610620011910726 ) ) ;
#97406=CARTESIAN_POINT ( 'NONE',  ( -7.500000000000007105, 11.33333333333400006, -68.91429205785459544 ) ) ;
#97408=CARTESIAN_POINT ( 'NONE',  ( -9.509302320691752186, -5.000000000000001776, -19.39567712392218368 ) ) ;
#97432=CARTESIAN_POINT ( 'NONE',  ( -23.38163988261910831, 48.00000000000000000, 60.94087333798633210 ) ) ;
#97448=CARTESIAN_POINT ( 'NONE',  ( 10.51296777078104050, 50.00000000000000000, -92.64705882352942012 ) ) ;
#97461=CARTESIAN_POINT ( 'NONE',  ( 6.236082931826281595, 41.88001976074639998, -59.13168102063718123 ) ) ;
#97474=EDGE_LOOP ( 'NONE', ( #18169, #75216, #98413, #23663 ) ) ;
#97490=CARTESIAN_POINT ( 'NONE',  ( -12.12055188808705708, -4.677944472895712913, -76.82403236456319462 ) ) ;
#97508=CARTESIAN_POINT ( 'NONE',  ( -4.175893272573466319, -3.000000000000000000, -7.137815226411295733 ) ) ;
#97515=CARTESIAN_POINT ( 'NONE',  ( -10.50000000000000000, -5.000000000000000000, -8.595933841506989026 ) ) ;
#97519=( GEOMETRIC_REPRESENTATION_CONTEXT ( 3 ) GLOBAL_UNCERTAINTY_ASSIGNED_CONTEXT ( ( #13753 ) ) GLOBAL_UNIT_ASSIGNED_CONTEXT ( ( #69387, #21914, #44582 ) ) REPRESENTATION_CONTEXT ( 'NONE', 'WORKASPACE' ) );
#97539=DIRECTION ( 'NONE',  ( 0.000000000000000000, 0.7456561006171790185, 0.6663309835302448914 ) ) ;
#97575=CARTESIAN_POINT ( 'NONE',  ( 0.000000000000000000, -4.999999999999999112, 8.000000000000000000 ) ) ;
#97582=FILL_AREA_STYLE ('',( #50110 ) ) ;
#97587=CARTESIAN_POINT ( 'NONE',  ( 6.907083959255992056, 41.55068448857264940, -58.85924345847777062 ) ) ;
#97614=CARTESIAN_POINT ( 'NONE',  ( -7.016701986871722418, -4.999999999999999112, -15.40549185441076396 ) ) ;
#97618=CARTESIAN_POINT ( 'NONE',  ( 7.791781413346524410, -3.000000000000000444, 2.093983074874241623 ) ) ;
#97633=CARTESIAN_POINT ( 'NONE',  ( 7.468840097761512808, -3.123202671104334360, -19.53083092318933822 ) ) ;
#97636=CARTESIAN_POINT ( 'NONE',  ( -43.54556210147816842, 41.43866363024021382, -50.63474964717280358 ) ) ;
#97651=DIRECTION ( 'NONE',  ( 0.000000000000000000, 1.000000000000000000, 0.000000000000000000 ) ) ;
#97675=CARTESIAN_POINT ( 'NONE',  ( 2.617478844991767861, -5.000000000000002665, -75.26027323389092771 ) ) ;
#97676=CARTESIAN_POINT ( 'NONE',  ( -5.929271424378248057, 41.34548848424987000, -58.36914649109142772 ) ) ;
#97682=ORIENTED_EDGE ( 'NONE', *, *, #56763, .T. ) ;
#97689=CARTESIAN_POINT ( 'NONE',  ( -4.692623589391090810, -5.000000000000000000, -97.18000954721273388 ) ) ;
#97698=ORIENTED_EDGE ( 'NONE', *, *, #59216, .F. ) ;
#97701=CARTESIAN_POINT ( 'NONE',  ( -7.225703553025883963, -5.000000000000000888, -73.19314196553557395 ) ) ;
#97729=CARTESIAN_POINT ( 'NONE',  ( -51.48757442383523397, 38.95383793070303113, -37.45149417477429665 ) ) ;
#97730=CARTESIAN_POINT ( 'NONE',  ( -6.951447413152005872, 41.73217189154441087, -59.36631701933644933 ) ) ;
#97752=CARTESIAN_POINT ( 'NONE',  ( 6.846597144391294520, 41.54610357422821920, -70.31839272398791252 ) ) ;
#97759=ORIENTED_EDGE ( 'NONE', *, *, #30119, .T. ) ;
#97777=CARTESIAN_POINT ( 'NONE',  ( 7.479728634662563103, 40.83274492738546257, -59.46320897030336283 ) ) ;
#97798=ORIENTED_EDGE ( 'NONE', *, *, #30119, .F. ) ;
#97799=STYLED_ITEM ( 'NONE', ( #65969 ), #75757 ) ;
#97856=CARTESIAN_POINT ( 'NONE',  ( -5.500000000000006217, 42.00000000000000000, -59.88032989329961708 ) ) ;
#97915=CARTESIAN_POINT ( 'NONE',  ( -2.094395098902661179, -4.999999999999998224, 8.000000000000000000 ) ) ;
#97931=CARTESIAN_POINT ( 'NONE',  ( 5.902962692465450800, 41.87327339699978523, -59.02279353628206593 ) ) ;
#97946=CARTESIAN_POINT ( 'NONE',  ( 17.50000000000003197, 51.99999999999912603, 59.56761335715597028 ) ) ;
#97950=B_SPLINE_SURFACE_WITH_KNOTS ( 'NONE', 3, 3, ( 
 ( #66268, #68414, #27456, #85117, #11202, #74350, #428, #17207 ),
 ( #27989, #71053, #61389, #4733, #37671, #54308, #61931, #37131 ),
 ( #101823, #3676, #3136, #4201, #44674, #45720, #5267, #95337 ),
 ( #62973, #95874, #21999, #36609, #68952, #70531, #69997, #103424 ),
 ( #62446, #21472, #13330, #20443, #54852, #28506, #29573, #102898 ),
 ( #87780, #78083, #19899, #94821, #29062, #53802, #77561, #87254 ),
 ( #46255, #79141, #45209, #44136, #38193, #60856, #103943, #30089 ),
 ( #77019, #36081, #20967, #93745, #52741, #85664, #69474, #102358 ) ),
 .UNSPECIFIED., .F., .F., .F.,
 ( 4, 2, 2, 4 ),
 ( 4, 2, 2, 4 ),
 ( 0.000000000000000000, 0.2500000000000000000, 0.5000000000000000000, 1.000000000000000000 ),
 ( 0.000000000000000000, 0.2500000000000000000, 0.5000000000000000000, 1.000000000000000000 ),
 .UNSPECIFIED. ) ;
#97956=CARTESIAN_POINT ( 'NONE',  ( -9.499999896953589484, -5.000000000000002665, -20.99851281918368784 ) ) ;
#97979=CARTESIAN_POINT ( 'NONE',  ( -55.22048556080177661, 48.00000000000000000, 34.80214219306111545 ) ) ;
#98005=CARTESIAN_POINT ( 'NONE',  ( 5.484632749660399931, 41.99999999999999289, -59.73832504088978368 ) ) ;
#98056=CARTESIAN_POINT ( 'NONE',  ( 4.175893272575848414, -4.999999999999998224, 7.137815226408912750 ) ) ;
#98057=DIRECTION ( 'NONE',  ( 0.000000000000000000, 1.000000000000000000, 0.000000000000000000 ) ) ;
#98063=CARTESIAN_POINT ( 'NONE',  ( -12.50000000000000711, -3.000000000000000000, -79.51734232575269345 ) ) ;
#98065=B_SPLINE_CURVE_WITH_KNOTS ( 'NONE', 3,
 ( #92632, #101789, #9573, #84555, #76439, #2551, #3637, #62937, #79628, #12764, #102321, #37097, #71014, #29537, #94242, #38155, #69960, #21431, #86696, #53250, #104432, #103387, #102860, #103905, #30581, #87745, #13826, #55343, #88272, #63476, #29027, #30050, #61891, #28472, #95831, #5228, #87212, #37633, #12238, #38664, #21960, #4165, #54815, #71532, #70496, #94787, #46738, #96374, #22503, #95303, #5745, #14349, #20931, #47256, #62409, #80155, #36573, #69440, #61350, #79106 ),
 .UNSPECIFIED., .F., .F.,
 ( 4, 1, 1, 1, 1, 1, 1, 2, 2, 1, 1, 1, 1, 1, 2, 2, 2, 1, 1, 1, 1, 2, 2, 1, 1, 1, 2, 2, 1, 2, 2, 1, 1, 1, 2, 2, 1, 1, 1, 1, 2, 2, 4 ),
 ( 0.000000000000000000, 0.06250000000007288614, 0.09375000000010748347, 0.1093750000001247752, 0.1171875000001345590, 0.1210937500001394579, 0.1230468750001419004, 0.1240234375001431216, 0.1250000000001443290, 0.1875000000001278977, 0.2187500000001189882, 0.2343750000001152134, 0.2421875000001140199, 0.2460937500001134093, 0.2480468750001131040, 0.2500000000001127987, 0.3750000000001774136, 0.4375000000002063905, 0.4687500000002197686, 0.4843750000002270961, 0.4921875000002307043, 0.4960937500002312595, 0.5000000000002318146, 0.5312500000002529088, 0.5468750000002652323, 0.5546875000002742251, 0.5585937500002765566, 0.5625000000002788880, 0.5937500000002960965, 0.6093750000003039791, 0.6250000000003118616, 0.6875000000003395062, 0.7187500000003508305, 0.7343750000003561595, 0.7421875000003588241, 0.7500000000003614886, 0.8125000000003130829, 0.8437500000002844391, 0.8593750000002658984, 0.8671875000002566836, 0.8710937500002481348, 0.8750000000002395861, 1.000000000000000000 ),
 .UNSPECIFIED. ) ;
#98071=CARTESIAN_POINT ( 'NONE',  ( 0.000000000000000000, -5.000000000000000888, -73.00000000000001421 ) ) ;
#98107=CARTESIAN_POINT ( 'NONE',  ( -63.45785145800994798, 47.99999999999999289, -14.99006954567219196 ) ) ;
#98111=EDGE_CURVE ( 'NONE', #712, #25935, #72619, .T. ) ;
#98135=CARTESIAN_POINT ( 'NONE',  ( 5.662865377646750353, 41.84935275029727819, -58.94136771051215362 ) ) ;
#98150=CARTESIAN_POINT ( 'NONE',  ( 17.53356643429805573, 45.00000000000002842, 63.42504839209897938 ) ) ;
#98157=CARTESIAN_POINT ( 'NONE',  ( -9.402149768019080867, -5.000000000000001776, -18.95237023718975422 ) ) ;
#98177=CARTESIAN_POINT ( 'NONE',  ( 5.076160773007416083, -4.320849473519435158, -17.10810059243997472 ) ) ;
#98180=CARTESIAN_POINT ( 'NONE',  ( -35.64423825752726316, 42.51604778590805722, -61.49727402875218019 ) ) ;
#98190=CARTESIAN_POINT ( 'NONE',  ( -51.78317192877783981, 40.83906611472826853, 39.73656039209301838 ) ) ;
#98194=CARTESIAN_POINT ( 'NONE',  ( -17.50000000000251887, 49.98040874965850122, 61.78610620011964016 ) ) ;
#98197=CARTESIAN_POINT ( 'NONE',  ( -9.500000025475724641, -4.999999999999998224, -69.85526497430338111 ) ) ;
#98214=CARTESIAN_POINT ( 'NONE',  ( 3.140974613991526887, -5.000000000000002665, -96.68767211932356531 ) ) ;
#98219=CARTESIAN_POINT ( 'NONE',  ( 7.500000000000005329, 42.83333333333328596, -68.91429205785459544 ) ) ;
#98230=CARTESIAN_POINT ( 'NONE',  ( -11.76475894966304026, -5.000000000000000888, -79.34634670506437715 ) ) ;
#98298=CARTESIAN_POINT ( 'NONE',  ( 7.251642494156181229, 41.54835750584383192, -68.91429206127320128 ) ) ;
#98300=ORIENTED_EDGE ( 'NONE', *, *, #93967, .F. ) ;
#98304=CARTESIAN_POINT ( 'NONE',  ( -7.439204957583139155, 40.67212726423260705, -59.07661279408126376 ) ) ;
#98310=CARTESIAN_POINT ( 'NONE',  ( -19.50010530980351220, 50.00000000000000000, 59.90637122617393828 ) ) ;
#98312=CARTESIAN_POINT ( 'NONE',  ( 12.49989493515518646, 18.64301898209307140, -36.27145154709465658 ) ) ;
#98334=CARTESIAN_POINT ( 'NONE',  ( 13.20204525318317401, 42.70098935138261709, -92.35018848971670025 ) ) ;
#98361=SURFACE_SIDE_STYLE ('',( #72491 ) ) ;
#98382=( BOUNDED_SURFACE ( )  B_SPLINE_SURFACE ( 2, 3, ( 
 ( #56938, #96895, #79636, #6266, #48319, #6809, #71538, #15431, #39204, #105509, #15967, #72605, #104441, #32714, #89860, #64533, #106563, #81213, #65583, #72081, #23029, #39727, #65050, #89339, #24621, #55863, #23560, #40240, #22510, #97946 ),
 ( #14891, #98468, #47786, #73116, #80689, #13834, #24096, #48845, #81738, #5753, #31649, #56404, #97398, #106021, #38674, #7861, #40768, #7328, #57469, #32167, #73659, #46746, #30591, #96380, #55350, #88278, #60047, #11984, #90933, #43825 ),
 ( #58008, #17045, #98989, #68101, #33236, #8401, #85356, #82828, #41304, #36843, #76187, #92906, #36320, #60571, #44369, #49920, #28221, #74190, #102062, #69710, #90392, #25152, #269, #93461, #2830, #66110, #3911, #35784, #10906, #3378 ) ),
 .UNSPECIFIED., .F., .F., .F. ) 
 B_SPLINE_SURFACE_WITH_KNOTS ( ( 3, 3 ),
 ( 4, 2, 2, 2, 2, 2, 2, 2, 2, 2, 2, 2, 2, 2, 4 ),
 ( 0.000000000000000000, 1.000000000000000000 ),
 ( 0.000000000000000000, 0.0008794597212711405482, 0.001758919442542281096, 0.002638379163813421753, 0.003078109024448992190, 0.003517838885084562193, 0.003957568745720132196, 0.004397298606355702633, 0.005276758327626843506, 0.006156218048897984380, 0.006595947909533553949, 0.006650914142113000145, 0.006705880374692446341, 0.006815812839851338734, 0.007035677770169124386 ),
 .UNSPECIFIED. ) 
 GEOMETRIC_REPRESENTATION_ITEM ( )  RATIONAL_B_SPLINE_SURFACE ( (
 ( 1.000000000000000000, 1.000000000000000000, 1.000000000000000000, 1.000000000000000000, 1.000000000000000000, 1.000000000000000000, 1.000000000000000000, 1.000000000000000000, 1.000000000000000000, 1.000000000000000000, 1.000000000000000000, 1.000000000000000000, 1.000000000000000000, 1.000000000000000000, 1.000000000000000000, 1.000000000000000000, 1.000000000000000000, 1.000000000000000000, 1.000000000000000000, 1.000000000000000000, 1.000000000000000000, 1.000000000000000000, 1.000000000000000000, 1.000000000000000000, 1.000000000000000000, 1.000000000000000000, 1.000000000000000000, 1.000000000000000000, 1.000000000000000000, 1.000000000000000000),
 ( 1.857142857142858317, 1.857142857142858317, 1.857142857142858317, 1.857142857142858317, 1.857142857142858317, 1.857142857142858317, 1.857142857142858317, 1.857142857142858317, 1.857142857142858317, 1.857142857142858317, 1.857142857142858317, 1.857142857142858317, 1.857142857142858317, 1.857142857142858317, 1.857142857142858317, 1.857142857142858317, 1.857142857142858317, 1.857142857142858317, 1.857142857142858317, 1.857142857142858317, 1.857142857142858317, 1.857142857142858317, 1.857142857142858317, 1.857142857142858317, 1.857142857142858317, 1.857142857142858317, 1.857142857142858317, 1.857142857142858317, 1.857142857142858317, 1.857142857142858317),
 ( 1.000000000000000000, 1.000000000000000000, 1.000000000000000000, 1.000000000000000000, 1.000000000000000000, 1.000000000000000000, 1.000000000000000000, 1.000000000000000000, 1.000000000000000000, 1.000000000000000000, 1.000000000000000000, 1.000000000000000000, 1.000000000000000000, 1.000000000000000000, 1.000000000000000000, 1.000000000000000000, 1.000000000000000000, 1.000000000000000000, 1.000000000000000000, 1.000000000000000000, 1.000000000000000000, 1.000000000000000000, 1.000000000000000000, 1.000000000000000000, 1.000000000000000000, 1.000000000000000000, 1.000000000000000000, 1.000000000000000000, 1.000000000000000000, 1.000000000000000000) ) ) 
 REPRESENTATION_ITEM ( '' )  SURFACE ( )  );
#98386=CARTESIAN_POINT ( 'NONE',  ( -8.841337832402279773, 48.00000000000001421, -97.17444126923535919 ) ) ;
#98390=CARTESIAN_POINT ( 'NONE',  ( -7.500000000000006217, 40.00000000000056133, -69.29143328409377034 ) ) ;
#98413=ORIENTED_EDGE ( 'NONE', *, *, #39209, .F. ) ;
#98463=CARTESIAN_POINT ( 'NONE',  ( 16.51905981272399870, 42.00139749746809059, -87.79004739960677739 ) ) ;
#98468=CARTESIAN_POINT ( 'NONE',  ( 17.49999999999444000, 48.26617306479607095, 62.61753806993364435 ) ) ;
#98477=CARTESIAN_POINT ( 'NONE',  ( 5.406991766687864853, 42.00000000000000000, -69.18631089694002867 ) ) ;
#98478=CARTESIAN_POINT ( 'NONE',  ( -9.256208135401527315, -5.000000000000035527, -17.97305361429047821 ) ) ;
#98502=CARTESIAN_POINT ( 'NONE',  ( -11.91432047182415133, 48.00000000000000000, 64.17585289259233150 ) ) ;
#98529=CARTESIAN_POINT ( 'NONE',  ( 23.70473373808798101, 41.64033039645621415, -74.70427921067390287 ) ) ;
#98647=CARTESIAN_POINT ( 'NONE',  ( -17.49999999999997513, 45.00000000000000711, 64.09953197936602010 ) ) ;
#98648=CARTESIAN_POINT ( 'NONE',  ( 55.65414010178471926, 42.00000000000000000, 72.41885610124163009 ) ) ;
#98658=CARTESIAN_POINT ( 'NONE',  ( 6.641837668257388749, 41.74662779905570176, -59.04567176600482270 ) ) ;
#98670=CARTESIAN_POINT ( 'NONE',  ( 17.50000000000002842, 45.00000000000000711, 64.09953197936602010 ) ) ;
#98676=CARTESIAN_POINT ( 'NONE',  ( -8.759832293797922276, -5.000000000000000000, -16.81557763462109278 ) ) ;
#98696=CARTESIAN_POINT ( 'NONE',  ( -43.02643730873325012, 41.50233601984075449, -51.34842824453740207 ) ) ;
#98710=CARTESIAN_POINT ( 'NONE',  ( -19.50000000000149925, 49.99999999999985789, 59.64162155654717168 ) ) ;
#98714=AXIS2_PLACEMENT_3D ( 'NONE', #88395, #64642, #14469 ) ;
#98715=CARTESIAN_POINT ( 'NONE',  ( -7.500000017879060010, -4.999999999997784883, -69.80246344213135501 ) ) ;
#98725=CARTESIAN_POINT ( 'NONE',  ( -20.13249097554416167, 41.84298886347988855, -79.53117214682279723 ) ) ;
#98731=CARTESIAN_POINT ( 'NONE',  ( -2.617478844992371823, -5.000000000000002665, -75.26027323389158141 ) ) ;
#98748=CARTESIAN_POINT ( 'NONE',  ( 7.814555105279644920, -5.000000000000000000, -95.45731198298756226 ) ) ;
#98792=CARTESIAN_POINT ( 'NONE',  ( -7.087005865465108911, 41.65067171707818261, -59.33604907184044919 ) ) ;
#98793=CARTESIAN_POINT ( 'NONE',  ( 6.912476950049422086, 40.56175661822392442, -71.08408186712233601 ) ) ;
#98814=CARTESIAN_POINT ( 'NONE',  ( 7.354130389523831468, 40.93126280921548243, -70.29718522916981271 ) ) ;
#98832=CARTESIAN_POINT ( 'NONE',  ( 12.49989493515518646, 18.64301898209307140, -36.27145154709465658 ) ) ;
#98846=COLOUR_RGB ( '', 0.08235294, 0.09019608, 0.10196078) ;
#98867=CARTESIAN_POINT ( 'NONE',  ( -6.392921701574284299, 41.54610357429506706, -70.64273452805430509 ) ) ;
#98873=CARTESIAN_POINT ( 'NONE',  ( 7.126148245860624009, 41.12758397993106740, -58.55282951229289523 ) ) ;
#98890=B_SPLINE_CURVE_WITH_KNOTS ( 'NONE', 3,
 ( #101093, #59051, #67671, #1303, #27251, #68750, #84387, #10475 ),
 .UNSPECIFIED., .F., .F.,
 ( 4, 2, 2, 4 ),
 ( 0.000000000000000000, 0.5000000000000000000, 0.7500000000000000000, 1.000000000000000000 ),
 .UNSPECIFIED. ) ;
#98903=CARTESIAN_POINT ( 'NONE',  ( -7.071721883978239198, 41.30029441324972339, -70.42654640881200123 ) ) ;
#98929=CARTESIAN_POINT ( 'NONE',  ( 28.49160136855818948, 41.56004681549217139, -71.33052401751463378 ) ) ;
#98935=CARTESIAN_POINT ( 'NONE',  ( 12.50000000000000711, 41.41911216696205855, -74.42394764531675833 ) ) ;
#98954=ORIENTED_EDGE ( 'NONE', *, *, #7287, .T. ) ;
#98977=SURFACE_SIDE_STYLE ('',( #81726 ) ) ;
#98989=CARTESIAN_POINT ( 'NONE',  ( 18.91769957617489695, 48.49892424866627039, 62.17828500952007431 ) ) ;
#98997=CARTESIAN_POINT ( 'NONE',  ( -7.347171990171222689, -3.439186728100687596, -18.43985286355804831 ) ) ;
#99003=SURFACE_SIDE_STYLE ('',( #106578 ) ) ;
#99010=CARTESIAN_POINT ( 'NONE',  ( -7.500000000000000888, -3.000671055698259870, -20.99923901233272971 ) ) ;
#99024=CARTESIAN_POINT ( 'NONE',  ( 5.957442974701732119, 48.00000000000000000, 65.00000000000000000 ) ) ;
#99035=CARTESIAN_POINT ( 'NONE',  ( -34.45841046840646982, 18.64284798593094550, 17.01587130353618704 ) ) ;
#99048=CARTESIAN_POINT ( 'NONE',  ( 19.24594220831874836, 41.87959112737684109, -80.73234005663204016 ) ) ;
#99057=CARTESIAN_POINT ( 'NONE',  ( -5.500000000000006217, 42.00000000000000000, -59.88032989329961708 ) ) ;
#99106=CARTESIAN_POINT ( 'NONE',  ( -6.819782170910313468, 41.52802923942638103, -70.37695045795369708 ) ) ;
#99112=CARTESIAN_POINT ( 'NONE',  ( 5.075566108724593128, -4.332661967060489339, -17.09624963492156269 ) ) ;
#99156=CARTESIAN_POINT ( 'NONE',  ( -18.91791044776116237, 47.00000000000000000, 62.18611311450884926 ) ) ;
#99166=CARTESIAN_POINT ( 'NONE',  ( -17.49999999999997513, 45.00000000000000711, 100.0000000000000000 ) ) ;
#99209=CARTESIAN_POINT ( 'NONE',  ( -8.763666794316772979, -5.000000000000000000, -16.82232303772159909 ) ) ;
#99227=CARTESIAN_POINT ( 'NONE',  ( -39.04768351285803618, 42.03798982804668327, -56.81831037689468644 ) ) ;
#99234=EDGE_CURVE ( 'NONE', #44820, #58911, #54280, .T. ) ;
#99241=CARTESIAN_POINT ( 'NONE',  ( -17.49999999999969091, 50.00252300264565264, 59.96656198872882726 ) ) ;
#99253=CARTESIAN_POINT ( 'NONE',  ( -35.21289418190758624, 40.42438906900185458, -59.33026139110200603 ) ) ;
#99259=CARTESIAN_POINT ( 'NONE',  ( -2.617478844992338516, -5.000000000000015099, -94.73972676610841859 ) ) ;
#99260=CARTESIAN_POINT ( 'NONE',  ( -6.716227137650916390, 41.28548431013199860, -58.40643990737236635 ) ) ;
#99276=CARTESIAN_POINT ( 'NONE',  ( -11.04994576751742130, -5.000000000000000000, -91.95135554698900648 ) ) ;
#99282=VERTEX_POINT ( 'NONE', #83201 ) ;
#99283=CARTESIAN_POINT ( 'NONE',  ( 38.28344347328716424, 38.95431846541184484, 51.20698281621823611 ) ) ;
#99295=FILL_AREA_STYLE_COLOUR ( '', #92409 ) ;
#99333=CARTESIAN_POINT ( 'NONE',  ( 1.715570313355265775, -4.332661967060491115, -17.83376356531591966 ) ) ;
#99357=CARTESIAN_POINT ( 'NONE',  ( 34.45841046839812094, 18.64284798592741410, 17.01587130354588595 ) ) ;
#99374=CARTESIAN_POINT ( 'NONE',  ( 14.75116209840774495, 43.55504285524111907, -90.22050492864485705 ) ) ;
#99378=CARTESIAN_POINT ( 'NONE',  ( -7.500000000000005329, 24.91666666666666430, -68.91429205785459544 ) ) ;
#99394=CARTESIAN_POINT ( 'NONE',  ( 14.33580413386840213, 42.00000000000000000, -89.41414995614803729 ) ) ;
#99434=CARTESIAN_POINT ( 'NONE',  ( -6.846597141950445220, 41.54610357434032863, -70.31839272209531089 ) ) ;
#99452=B_SPLINE_CURVE_WITH_KNOTS ( 'NONE', 3,
 ( #32298, #39849, #94512, #70218, #3892, #28733, #65169, #24215, #57065, #96489, #104562, #55985, #15015, #11966, #77781, #36824, #6389, #86426 ),
 .UNSPECIFIED., .F., .F.,
 ( 4, 2, 2, 2, 2, 2, 2, 2, 4 ),
 ( 0.000000000000000000, 0.06250000000000000000, 0.1250000000000000000, 0.1875000000000000000, 0.2500000000000000000, 0.3125000000000000000, 0.3750000000000000000, 0.4375000000000000000, 0.5000000000000000000 ),
 .UNSPECIFIED. ) ;
#99472=CARTESIAN_POINT ( 'NONE',  ( 12.50000000000000533, 27.20916491834851669, -44.75057325027661648 ) ) ;
#99483=CARTESIAN_POINT ( 'NONE',  ( 17.50000000000002842, 48.98085210278581769, 64.05428188712279791 ) ) ;
#99508=EDGE_CURVE ( 'NONE', #21469, #58519, #102035, .T. ) ;
#99532=CARTESIAN_POINT ( 'NONE',  ( -5.675014839626371099, 41.92512469482201709, -59.11382255286373777 ) ) ;
#99534=CARTESIAN_POINT ( 'NONE',  ( 0.000000000000000000, -5.000000000000002665, -75.00000000000001421 ) ) ;
#99550=ORIENTED_EDGE ( 'NONE', *, *, #28462, .F. ) ;
#99562=CARTESIAN_POINT ( 'NONE',  ( 60.62677696746332145, 48.00000000000000000, 24.18439665019722540 ) ) ;
#99600=CARTESIAN_POINT ( 'NONE',  ( -4.910934196423679232, 41.41789156490654733, -70.63711759939612023 ) ) ;
#99610=FILL_AREA_STYLE ('',( #7937 ) ) ;
#99618=B_SPLINE_CURVE_WITH_KNOTS ( 'NONE', 3,
 ( #14076, #40492, #105234, #47514, #81458, #55589, #46984, #30847 ),
 .UNSPECIFIED., .F., .F.,
 ( 4, 2, 2, 4 ),
 ( 0.000000000000000000, 0.5000000000000000000, 0.7500000000000000000, 1.000000000000000000 ),
 .UNSPECIFIED. ) ;
#99652=CARTESIAN_POINT ( 'NONE',  ( -6.846597141950445220, 41.54610357434032863, -70.31839272209531089 ) ) ;
#99705=CARTESIAN_POINT ( 'NONE',  ( -6.770722853400887864, 41.58070589549304685, -58.79856860655606710 ) ) ;
#99724=CARTESIAN_POINT ( 'NONE',  ( 90.56128410203886858, 42.00000000000000000, 11.85444436786826472 ) ) ;
#99734=CARTESIAN_POINT ( 'NONE',  ( 6.340296234547424525, 41.77218160844339678, -58.92363273660524214 ) ) ;
#99761=CARTESIAN_POINT ( 'NONE',  ( -17.49999999999996447, 45.90000000000000568, 62.61746187599676716 ) ) ;
#99774=CARTESIAN_POINT ( 'NONE',  ( 11.78124729766429546, -3.000000000000003109, -94.38183245066619520 ) ) ;
#99792=CARTESIAN_POINT ( 'NONE',  ( -19.50000000000017053, 49.99999999999997868, 59.86364615470554895 ) ) ;
#99804=CARTESIAN_POINT ( 'NONE',  ( -23.98952478535236210, 41.62026329535294877, -74.32034878064006023 ) ) ;
#99809=CARTESIAN_POINT ( 'NONE',  ( 0.000000000000000000, -5.000000000000002665, -75.00000000000001421 ) ) ;
#99814=CARTESIAN_POINT ( 'NONE',  ( 6.392921707093107919, 41.54610357469336179, -70.64273453041053585 ) ) ;
#99861=ORIENTED_EDGE ( 'NONE', *, *, #4269, .T. ) ;
#99871=CARTESIAN_POINT ( 'NONE',  ( -7.386518100075204707, 41.27037529920123404, -59.50133825707656143 ) ) ;
#99896=CARTESIAN_POINT ( 'NONE',  ( -63.67138272020815748, 38.95383793066860534, -8.334564508068563526 ) ) ;
#99898=CARTESIAN_POINT ( 'NONE',  ( -50.94745919686192082, 50.00000000000000000, -37.05882352941185331 ) ) ;
#99941=( BOUNDED_CURVE ( )  B_SPLINE_CURVE ( 2, ( #8768, #24471, #9819, #90763, #81568 ),
 .UNSPECIFIED., .F., .F. ) 
 B_SPLINE_CURVE_WITH_KNOTS ( ( 3, 2, 3 ),
 ( 0.000000000000000000, 0.9999798024780033323, 1.000000000000000000 ),
 .UNSPECIFIED. ) 
 CURVE ( )  GEOMETRIC_REPRESENTATION_ITEM ( )  RATIONAL_B_SPLINE_CURVE ( ( 1.000000000000000666, 1.857142857142856984, 1.000000000000000000, 1.000000000000000000, 1.000000000000000000 ) ) 
 REPRESENTATION_ITEM ( '' )  );
#99953=CARTESIAN_POINT ( 'NONE',  ( -23.70422451874885184, 42.00000000000000000, -88.20421627933662023 ) ) ;
#99958=B_SPLINE_CURVE_WITH_KNOTS ( 'NONE', 3,
 ( #5080, #36945, #28874, #38013, #96226, #37484, #54130, #30437, #4546, #63330 ),
 .UNSPECIFIED., .F., .F.,
 ( 4, 2, 2, 2, 4 ),
 ( 0.000000000000000000, 0.2500000000000000000, 0.5000000000000000000, 0.7500000000000000000, 1.000000000000000000 ),
 .UNSPECIFIED. ) ;
#99962=PRESENTATION_STYLE_ASSIGNMENT (( #67079 ) ) ;
#99964=ORIENTED_EDGE ( 'NONE', *, *, #39007, .T. ) ;
#99976=CARTESIAN_POINT ( 'NONE',  ( -12.13034742782428310, 49.99999999999999289, -93.82352941176471006 ) ) ;
#99978=CARTESIAN_POINT ( 'NONE',  ( -12.48710243631036754, -3.525193987328853584, -13.72488916828378613 ) ) ;
#99979=CARTESIAN_POINT ( 'NONE',  ( -5.756917790976768146, 47.99999999999999289, -98.90122916984913104 ) ) ;
#99981=CARTESIAN_POINT ( 'NONE',  ( -7.425259529285893834, 41.08730259631308712, -69.63985907319367641 ) ) ;
#100001=PRESENTATION_STYLE_ASSIGNMENT (( #35307 ) ) ;
#100026=CARTESIAN_POINT ( 'NONE',  ( 56.90650429242290187, 38.95383793070381984, -28.99688671942671547 ) ) ;
#100038=COLOUR_RGB ( '', 0.66274510, 0.83137255, 0.94901961) ;
#100089=CARTESIAN_POINT ( 'NONE',  ( -7.022229286278467875, -4.221542269106504541, -17.11103215587112913 ) ) ;
#100093=UNCERTAINTY_MEASURE_WITH_UNIT (LENGTH_MEASURE( 1.000000000000000082E-05 ), #39456, 'distance_accuracy_value', 'NONE');
#100129=CARTESIAN_POINT ( 'NONE',  ( 19.41543580316799122, 41.87297093669189252, -80.50253431361618084 ) ) ;
#100148=CARTESIAN_POINT ( 'NONE',  ( -5.036189802311375807, 50.00000000000001421, -93.73786388411662074 ) ) ;
#100186=CARTESIAN_POINT ( 'NONE',  ( -7.150000000000001243, 41.64999999999999147, -68.91429205801802027 ) ) ;
#100219=ORIENTED_EDGE ( 'NONE', *, *, #79075, .T. ) ;
#100233=CARTESIAN_POINT ( 'NONE',  ( -4.966176470918042263, 41.64999999999998437, -70.47555194646970733 ) ) ;
#100239=CARTESIAN_POINT ( 'NONE',  ( -25.60851123651792705, 48.00000000000000000, -75.29411764705884025 ) ) ;
#100241=CARTESIAN_POINT ( 'NONE',  ( 12.50000000000000000, -2.999999999999996891, -14.34180675897363955 ) ) ;
#100245=ORIENTED_EDGE ( 'NONE', *, *, #67133, .F. ) ;
#100252=ADVANCED_FACE ( 'NONE', ( #52475 ), #75557, .T. ) ;
#100253=CARTESIAN_POINT ( 'NONE',  ( -55.65414010186720617, 42.00000000000000000, -72.41885610115910765 ) ) ;
#100274=CARTESIAN_POINT ( 'NONE',  ( 1.630169624183145149, -5.000000000000000000, -16.56347947974793655 ) ) ;
#100299=CARTESIAN_POINT ( 'NONE',  ( 9.499937800617230366, -5.000000000000023093, -20.18737470931553091 ) ) ;
#100301=( LENGTH_UNIT ( ) NAMED_UNIT ( * ) SI_UNIT ( .MILLI., .METRE. ) );
#100302=CARTESIAN_POINT ( 'NONE',  ( -13.85425718576935239, -3.000000000000002665, -90.90560122694158451 ) ) ;
#100319=CARTESIAN_POINT ( 'NONE',  ( -17.49999999999793587, 49.88162284957622461, 62.03084827767296616 ) ) ;
#100373=CARTESIAN_POINT ( 'NONE',  ( 19.49236955434526308, 49.99908790945509196, 60.06985828019035267 ) ) ;
#100386=CARTESIAN_POINT ( 'NONE',  ( -5.121894999926677627, -2.681690743133432697, -18.64842307824732970 ) ) ;
#100399=DIRECTION ( 'NONE',  ( 0.000000000000000000, 1.000000000000000000, 0.000000000000000000 ) ) ;
#100400=CARTESIAN_POINT ( 'NONE',  ( -7.395123836361360503, 40.93288475959919026, -59.01287901077084541 ) ) ;
#100430=CARTESIAN_POINT ( 'NONE',  ( 3.294249609603376872, -3.000000000000002665, -70.27378291343094929 ) ) ;
#100444=CARTESIAN_POINT ( 'NONE',  ( 11.09043181264936173, 18.64284798592871439, 36.79570967431541817 ) ) ;
#100449=( BOUNDED_CURVE ( )  B_SPLINE_CURVE ( 2, ( #19833, #4138, #69411 ),
 .UNSPECIFIED., .F., .T. ) 
 B_SPLINE_CURVE_WITH_KNOTS ( ( 3, 3 ),
 ( 0.000000000000000000, 1.000000000000000000 ),
 .UNSPECIFIED. ) 
 CURVE ( )  GEOMETRIC_REPRESENTATION_ITEM ( )  RATIONAL_B_SPLINE_CURVE ( ( 1.000000000000000000, 1.428571428571452584, 1.428571428571428825 ) ) 
 REPRESENTATION_ITEM ( '' )  );
#100483=SURFACE_STYLE_FILL_AREA ( #11461 ) ;
#100507=CARTESIAN_POINT ( 'NONE',  ( -11.68767211932491179, 50.00000000000000000, -81.85902538600507228 ) ) ;
#100512=CARTESIAN_POINT ( 'NONE',  ( -7.069742149889169269, 41.66287055432060527, -69.58314084294495672 ) ) ;
#100544=CARTESIAN_POINT ( 'NONE',  ( -18.23999450864831928, 45.00000000000000000, 62.43394949844228137 ) ) ;
#100560=STYLED_ITEM ( 'NONE', ( #99962 ), #53283 ) ;
#100574=FILL_AREA_STYLE ('',( #59610 ) ) ;
#100598=CARTESIAN_POINT ( 'NONE',  ( 23.38163988261896620, 48.00000000000000000, 60.94087333798638895 ) ) ;
#100635=CARTESIAN_POINT ( 'NONE',  ( -5.957442974701830707, 49.99999999999999289, 65.00000000000000000 ) ) ;
#100658=CARTESIAN_POINT ( 'NONE',  ( 42.22882555519233705, 39.53072919842792743, -49.99044811816536793 ) ) ;
#100663=FACE_OUTER_BOUND ( 'NONE', #96527, .T. ) ;
#100675=CARTESIAN_POINT ( 'NONE',  ( -8.737863884120026015, 49.99999999999999289, -79.96381019768847409 ) ) ;
#100709=B_SPLINE_CURVE_WITH_KNOTS ( 'NONE', 3,
 ( #103272, #7593, #29422, #40511, #7074, #89074, #53651, #70902 ),
 .UNSPECIFIED., .F., .F.,
 ( 4, 2, 2, 4 ),
 ( 0.000000000000000000, 0.4019822150283983153, 0.6029733225425960574, 0.8039644300567937441 ),
 .UNSPECIFIED. ) ;
#100747=ORIENTED_EDGE ( 'NONE', *, *, #39491, .T. ) ;
#100758=CARTESIAN_POINT ( 'NONE',  ( -7.040774328009894667, 41.35742559143615438, -58.68913211047703982 ) ) ;
#100763=ADVANCED_FACE ( 'NONE', ( #90161 ), #4697, .F. ) ;
#100778=CARTESIAN_POINT ( 'NONE',  ( -12.50000000000000711, 18.64303733123573537, -36.27143273323382999 ) ) ;
#100780=CARTESIAN_POINT ( 'NONE',  ( 90.56128410203886858, 42.00000000000000000, -11.85444436786857558 ) ) ;
#100785=ORIENTED_EDGE ( 'NONE', *, *, #55553, .F. ) ;
#100789=CARTESIAN_POINT ( 'NONE',  ( -7.500000000000007105, 42.00000000000000711, -59.28631038546422616 ) ) ;
#100790=EDGE_CURVE ( 'NONE', #71163, #56205, #80048, .T. ) ;
#100825=CARTESIAN_POINT ( 'NONE',  ( 2.751706330279339863, -3.000000000000002665, -100.0000000000000000 ) ) ;
#100826=CARTESIAN_POINT ( 'NONE',  ( -14.92100282753430562, -3.000000000000002665, -82.95543583084106842 ) ) ;
#100876=ORIENTED_EDGE ( 'NONE', *, *, #93572, .T. ) ;
#100912=CARTESIAN_POINT ( 'NONE',  ( -7.500000000000001776, 25.40357082213843753, -43.84441647605142123 ) ) ;
#100929=CARTESIAN_POINT ( 'NONE',  ( -19.07197487161970884, 49.63586355494508240, 61.78730625525749787 ) ) ;
#100930=CARTESIAN_POINT ( 'NONE',  ( -6.907083948287215946, 41.55068305711947829, -58.85924204532966542 ) ) ;
#100945=EDGE_LOOP ( 'NONE', ( #3610, #4190 ) ) ;
#100952=CARTESIAN_POINT ( 'NONE',  ( 11.99999999999999467, -5.000000000000002665, -83.42920367501479006 ) ) ;
#100973=CARTESIAN_POINT ( 'NONE',  ( 37.46714894334161983, 18.64284798592703751, 8.551881564011154069 ) ) ;
#100984=VERTEX_POINT ( 'NONE', #83527 ) ;
#100993=CARTESIAN_POINT ( 'NONE',  ( 2.354803500934599558, 48.00000000000000000, -100.0000000000000000 ) ) ;
#101026=CARTESIAN_POINT ( 'NONE',  ( 60.45578259952156941, 40.83768840997593941, 24.06212321066767501 ) ) ;
#101035=CARTESIAN_POINT ( 'NONE',  ( -9.258863595255469647, 41.99999999999999289, -70.74260034492780846 ) ) ;
#101044=CARTESIAN_POINT ( 'NONE',  ( -2.617478844990396514, 50.00000000000001421, -94.73972676610910071 ) ) ;
#101084=CARTESIAN_POINT ( 'NONE',  ( -17.55562382432310997, 45.00000000000001421, 63.27682836070874828 ) ) ;
#101087=( BOUNDED_CURVE ( )  B_SPLINE_CURVE ( 2, ( #66105, #98463, #58003 ),
 .UNSPECIFIED., .F., .F. ) 
 B_SPLINE_CURVE_WITH_KNOTS ( ( 3, 3 ),
 ( 0.000000000000000000, 1.000000000000000000 ),
 .UNSPECIFIED. ) 
 CURVE ( )  GEOMETRIC_REPRESENTATION_ITEM ( )  RATIONAL_B_SPLINE_CURVE ( ( 1.000000000000000000, 1.857142857142858317, 1.000000000000000000 ) ) 
 REPRESENTATION_ITEM ( '' )  );
#101093=CARTESIAN_POINT ( 'NONE',  ( 5.363597346073513350, 41.33266196706048845, -58.39526881795627844 ) ) ;
#101137=CARTESIAN_POINT ( 'NONE',  ( 58.90678327789231616, 48.00000000000000000, -28.11551192221969941 ) ) ;
#101151=VECTOR ( 'NONE', #31539, 1000.000000000000000 ) ;
#101177=CARTESIAN_POINT ( 'NONE',  ( 6.057904175366207511, 41.61856606260997893, -70.65344123640606711 ) ) ;
#101179=CARTESIAN_POINT ( 'NONE',  ( -57.09426686934756390, 50.00000000000000000, -27.25041924766811618 ) ) ;
#101219=CARTESIAN_POINT ( 'NONE',  ( 10.51296777078104050, 50.00000000000000000, -92.64705882352942012 ) ) ;
#101222=CARTESIAN_POINT ( 'NONE',  ( -6.043427762773251111, 50.00000000000000000, -95.48543666094653304 ) ) ;
#101234=EDGE_LOOP ( 'NONE', ( #89364, #30113, #24911, #5966, #26441 ) ) ;
#101235=CARTESIAN_POINT ( 'NONE',  ( -8.737863883542573262, -3.000000000000002665, -90.03618980370899294 ) ) ;
#101263=B_SPLINE_CURVE_WITH_KNOTS ( 'NONE', 3,
 ( #103993, #71624, #20498, #5832 ),
 .UNSPECIFIED., .F., .F.,
 ( 4, 4 ),
 ( 0.000000000000000000, 1.000000000000000000 ),
 .UNSPECIFIED. ) ;
#101284=ORIENTED_EDGE ( 'NONE', *, *, #21996, .T. ) ;
#101307=DIRECTION ( 'NONE',  ( 0.000000000000000000, -0.000000000000000000, 1.000000000000000000 ) ) ;
#101313=CARTESIAN_POINT ( 'NONE',  ( -7.026865645360749646, 41.28180592973833285, -58.57603972943267934 ) ) ;
#101330=CARTESIAN_POINT ( 'NONE',  ( 10.04205104292330475, 18.64316884715076839, 37.36680950592799633 ) ) ;
#101357=CARTESIAN_POINT ( 'NONE',  ( 7.493262089825916128, 40.00000000068802564, -69.66935728187972643 ) ) ;
#101382=MECHANICAL_DESIGN_GEOMETRIC_PRESENTATION_REPRESENTATION('',(#94474),#23885);
#101388=ADVANCED_FACE ( 'NONE', ( #91544 ), #70849, .T. ) ;
#101413=CARTESIAN_POINT ( 'NONE',  ( -6.492510984469592294, 41.78432685485347520, -59.03546988472429291 ) ) ;
#101420=CARTESIAN_POINT ( 'NONE',  ( 0.000000000000000000, -3.000000000000002665, -75.00000000000001421 ) ) ;
#101429=CARTESIAN_POINT ( 'NONE',  ( -7.549954993183457752, -4.999999999999999112, -15.49602501671512833 ) ) ;
#101436=CARTESIAN_POINT ( 'NONE',  ( -16.52732684424165654, 43.98685724163156863, -87.77868211029610279 ) ) ;
#101448=CARTESIAN_POINT ( 'NONE',  ( 14.63429600766766114, 41.99999999961375607, -88.44473994942086392 ) ) ;
#101450=CARTESIAN_POINT ( 'NONE',  ( 19.49546873405769887, 49.99968197754504473, 60.00409861388182264 ) ) ;
#101461=CARTESIAN_POINT ( 'NONE',  ( -7.500000000007254641, 42.38482959929934424, -59.14603436866633501 ) ) ;
#101469=VERTEX_POINT ( 'NONE', #96850 ) ;
#101476=CARTESIAN_POINT ( 'NONE',  ( 4.933292146132942868, 41.54835750584369691, -70.57172791956975288 ) ) ;
#101485=B_SPLINE_CURVE_WITH_KNOTS ( 'NONE', 3,
 ( #51861, #93408, #26059, #36271, #10859, #18468, #76668, #2781 ),
 .UNSPECIFIED., .F., .F.,
 ( 4, 2, 2, 4 ),
 ( 0.000000000000000000, 0.5000000000000000000, 0.7500000000000000000, 1.000000000000000000 ),
 .UNSPECIFIED. ) ;
#101492=CARTESIAN_POINT ( 'NONE',  ( -6.397334739185442487, -2.999999999999999556, 4.916373759799318677 ) ) ;
#101502=ORIENTED_EDGE ( 'NONE', *, *, #103875, .T. ) ;
#101512=CARTESIAN_POINT ( 'NONE',  ( -8.786988139152953468E-15, 18.64300841652315910, 38.36521369532682257 ) ) ;
#101533=CARTESIAN_POINT ( 'NONE',  ( -4.080003621823601989, 50.00000000000000000, -97.51073764065985472 ) ) ;
#101557=CARTESIAN_POINT ( 'NONE',  ( -7.754160006507099467, 42.00000000000000711, -59.23741894013591036 ) ) ;
#101559=( GEOMETRIC_REPRESENTATION_CONTEXT ( 3 ) GLOBAL_UNCERTAINTY_ASSIGNED_CONTEXT ( ( #37557 ) ) GLOBAL_UNIT_ASSIGNED_CONTEXT ( ( #24732, #58681, #33894 ) ) REPRESENTATION_CONTEXT ( 'NONE', 'WORKASPACE' ) );
#101565=CARTESIAN_POINT ( 'NONE',  ( -43.66105921549289093, 40.83721605545716216, 48.52424057032921212 ) ) ;
#101584=CARTESIAN_POINT ( 'NONE',  ( 7.374560640985523996, 50.00000000000000000, -75.40399789250294305 ) ) ;
#101594=ORIENTED_EDGE ( 'NONE', *, *, #38965, .T. ) ;
#101596=CARTESIAN_POINT ( 'NONE',  ( -6.145467199749144349, 47.99999999999998579, -92.99666842398180222 ) ) ;
#101600=CARTESIAN_POINT ( 'NONE',  ( 6.890281281981907924, 41.03680257675737408, -70.85895802599645776 ) ) ;
#101612=CARTESIAN_POINT ( 'NONE',  ( -6.716519851531634444, 41.04202961696241658, -70.96212009813095278 ) ) ;
#101625=CARTESIAN_POINT ( 'NONE',  ( -17.63720921189712953, 45.00000000000000711, 62.98367185064536500 ) ) ;
#101664=CARTESIAN_POINT ( 'NONE',  ( 8.737863883542576815, 47.99999999999999289, -90.03618980370899294 ) ) ;
#101673=CARTESIAN_POINT ( 'NONE',  ( 64.32759900504497352, 48.00000000000000000, -11.06576400629120549 ) ) ;
#101707=CARTESIAN_POINT ( 'NONE',  ( 6.914762299961043190, 41.79847487255189264, -69.55926079108232329 ) ) ;
#101708=CARTESIAN_POINT ( 'NONE',  ( 50.94745919686198476, 50.00000000000000000, -37.05882352941176094 ) ) ;
#101728=CARTESIAN_POINT ( 'NONE',  ( 38.73813457942127059, 39.95935930601281427, -54.64964148907081665 ) ) ;
#101745=CARTESIAN_POINT ( 'NONE',  ( -11.99999999999999467, 50.00000000000000000, -86.57079632497432442 ) ) ;
#101752=( GEOMETRIC_REPRESENTATION_CONTEXT ( 3 ) GLOBAL_UNCERTAINTY_ASSIGNED_CONTEXT ( ( #8427 ) ) GLOBAL_UNIT_ASSIGNED_CONTEXT ( ( #25031, #57887, #102490 ) ) REPRESENTATION_CONTEXT ( 'NONE', 'WORKASPACE' ) );
#101789=CARTESIAN_POINT ( 'NONE',  ( -19.49122775093939808, 50.00000000000002132, 59.91448273658983226 ) ) ;
#101809=ORIENTED_EDGE ( 'NONE', *, *, #34331, .T. ) ;
#101819=CARTESIAN_POINT ( 'NONE',  ( 7.500000000000007105, 39.99999999999998579, -68.91429205785453860 ) ) ;
#101823=CARTESIAN_POINT ( 'NONE',  ( -6.458627570771506399, 41.53001914901422964, -70.63868815569685466 ) ) ;
#101824=CARTESIAN_POINT ( 'NONE',  ( 7.500000000000006217, 39.99999999999998579, -62.89165061482851371 ) ) ;
#101829=CARTESIAN_POINT ( 'NONE',  ( -5.383907111441308402, 41.54392591541395063, -58.58678640223104139 ) ) ;
#101844=ORIENTED_EDGE ( 'NONE', *, *, #61667, .T. ) ;
#101849=CARTESIAN_POINT ( 'NONE',  ( 47.37019975555959661, 42.00000000000001421, -36.40416150955741870 ) ) ;
#101859=CARTESIAN_POINT ( 'NONE',  ( 5.971401237478955792, 41.34845901557833514, -58.36201559607086153 ) ) ;
#101870=CARTESIAN_POINT ( 'NONE',  ( 16.52731600354976393, 43.98685737190850631, -87.77869701378344303 ) ) ;
#101878=CARTESIAN_POINT ( 'NONE',  ( 7.286131463487275362, 40.29425637570631125, -70.75304884496938485 ) ) ;
#101897=CARTESIAN_POINT ( 'NONE',  ( 13.73780227957584898, -5.000000000000002665, -78.37846873787442803 ) ) ;
#101916=CARTESIAN_POINT ( 'NONE',  ( -17.49999999999997513, 51.99978697404923622, 59.99316026186820494 ) ) ;
#101920=ADVANCED_FACE ( 'NONE', ( #49202 ), #104148, .T. ) ;
#101936=CARTESIAN_POINT ( 'NONE',  ( -5.036189802311206165, -3.000000000000002665, -76.26213611587844809 ) ) ;
#101946=CARTESIAN_POINT ( 'NONE',  ( 14.99896353599399923, -4.999999999999999112, 9.191463535713378263 ) ) ;
#101967=CARTESIAN_POINT ( 'NONE',  ( 5.693345023037156949, -5.000000000005900169, -71.09407786877757474 ) ) ;
#101971=CARTESIAN_POINT ( 'NONE',  ( 0.000000000000000000, 47.00000000000000000, 0.000000000000000000 ) ) ;
#101973=CARTESIAN_POINT ( 'NONE',  ( -11.51551999166614060, -4.933705119235564318, -12.56689034858084497 ) ) ;
#101993=CARTESIAN_POINT ( 'NONE',  ( -19.24979913086533756, 49.81992999154532242, 61.45847795212542763 ) ) ;
#101995=CARTESIAN_POINT ( 'NONE',  ( 6.238189707152653973, 40.55825190858245577, -71.19044262412266733 ) ) ;
#102008=CARTESIAN_POINT ( 'NONE',  ( 5.296353609480505931, 19.09562013799879310, -38.40621394496536567 ) ) ;
#102010=CARTESIAN_POINT ( 'NONE',  ( 1.589967640017929007, -5.000000000000000000, -16.33935305251328884 ) ) ;
#102012=CARTESIAN_POINT ( 'NONE',  ( -7.374560640982810611, -5.000000000000002665, -94.59600210748614302 ) ) ;
#102020=STYLED_ITEM ( 'NONE', ( #34549 ), #83037 ) ;
#102022=CARTESIAN_POINT ( 'NONE',  ( 0.000000000000000000, 50.00000000000000000, -97.00000000000000000 ) ) ;
#102035=B_SPLINE_CURVE_WITH_KNOTS ( 'NONE', 3,
 ( #104693, #24345, #38780, #81994, #81457, #7571, #87997, #64771, #73368, #79881, #98190, #56659, #57187, #90103, #63731, #14075, #64258, #8112 ),
 .UNSPECIFIED., .F., .F.,
 ( 4, 2, 2, 2, 2, 2, 2, 2, 4 ),
 ( 0.000000000000000000, 0.06250000000001418310, 0.1250000000000283662, 0.1875000000000425493, 0.2500000000000567324, 0.3125000000000709433, 0.3750000000000852096, 0.4375000000000994205, 0.5000000000001136868 ),
 .UNSPECIFIED. ) ;
#102052=CARTESIAN_POINT ( 'NONE',  ( -12.13034742782427955, 48.00000000000000000, -93.82352941176471006 ) ) ;
#102055=EDGE_CURVE ( 'NONE', #61410, #100984, #104540, .T. ) ;
#102062=CARTESIAN_POINT ( 'NONE',  ( 19.45524037106658355, 49.98193815142445118, 60.61134026581003553 ) ) ;
#102075=CARTESIAN_POINT ( 'NONE',  ( -45.60838156032659896, 42.00000000000000000, 79.13121736029036413 ) ) ;
#102082=CARTESIAN_POINT ( 'NONE',  ( 5.937976208022995195, 40.83857947417038758, 64.79749893865751176 ) ) ;
#102103=( NAMED_UNIT ( * ) SI_UNIT ( $, .STERADIAN. ) SOLID_ANGLE_UNIT ( ) );
#102106=EDGE_CURVE ( 'NONE', #38679, #16973, #18308, .T. ) ;
#102120=SURFACE_STYLE_FILL_AREA ( #46024 ) ;
#102130=CARTESIAN_POINT ( 'NONE',  ( -6.870940789805455751, 40.00000000008640200, -71.15487332242412322 ) ) ;
#102150=CARTESIAN_POINT ( 'NONE',  ( 17.50000000000002842, 45.00000000000000711, 64.09953197936602010 ) ) ;
#102160=( BOUNDED_CURVE ( )  B_SPLINE_CURVE ( 3, ( #75074, #33592, #73480, #48674, #106379, #9281, #103, #67015, #81558, #99896, #33072, #7685, #90752, #83702 ),
 .UNSPECIFIED., .F., .T. ) 
 B_SPLINE_CURVE_WITH_KNOTS ( ( 4, 2, 2, 2, 2, 2, 4 ),
 ( 0.5000000000031382674, 0.5892633092116352778, 0.6785266184232030540, 0.7677899276347708302, 0.8570532368463388284, 0.9463165460579068267, 1.000000000000000000 ),
 .UNSPECIFIED. ) 
 CURVE ( )  GEOMETRIC_REPRESENTATION_ITEM ( )  RATIONAL_B_SPLINE_CURVE ( ( 1.420262811277154924, 1.420262811277154924, 1.420262811277154924, 1.420262811277154924, 1.420262811277154924, 1.420262811277154924, 1.420262811277154924, 1.420262811277154924, 1.420262811277154924, 1.420262811277154924, 1.420262811277154924, 1.420262811277154924, 1.420262811277154924, 1.420262811277154924 ) ) 
 REPRESENTATION_ITEM ( '' )  );
#102179=CARTESIAN_POINT ( 'NONE',  ( 11.64553472616179342, -4.906298272857039677, -12.56112232304452370 ) ) ;
#102185=ORIENTED_EDGE ( 'NONE', *, *, #35758, .F. ) ;
#102194=CARTESIAN_POINT ( 'NONE',  ( 8.737863883542576815, -3.000000000000002665, -79.96381019629100706 ) ) ;
#102204=CARTESIAN_POINT ( 'NONE',  ( -6.849721783289899335, 41.84384191736015168, -59.83401399873645232 ) ) ;
#102215=CARTESIAN_POINT ( 'NONE',  ( 17.58100359019471526, 50.00000000000000000, 62.76922408379542873 ) ) ;
#102225=DIRECTION ( 'NONE',  ( 0.8086898285216187476, 0.000000000000000000, -0.5882352941176471894 ) ) ;
#102236=CARTESIAN_POINT ( 'NONE',  ( 6.491942738476094377, 41.63185016724582965, -70.49544021083930545 ) ) ;
#102237=CARTESIAN_POINT ( 'NONE',  ( -22.66220480930539338, 50.00000000000000000, 59.06576954297837290 ) ) ;
#102260=CARTESIAN_POINT ( 'NONE',  ( 33.03967949176340113, 40.70416129926884707, -62.21519284123854021 ) ) ;
#102265=DIRECTION ( 'NONE',  ( -1.160749806054361473E-16, 0.000000000000000000, -1.000000000000000000 ) ) ;
#102270=CARTESIAN_POINT ( 'NONE',  ( 28.55297524992865377, 43.39596580573108753, -71.24614888030039594 ) ) ;
#102277=CARTESIAN_POINT ( 'NONE',  ( 3.140974613991526887, 50.00000000000000000, -73.31232788067644890 ) ) ;
#102305=CARTESIAN_POINT ( 'NONE',  ( -5.248814467633681424, 10.38896636856183520, -30.54266839283955193 ) ) ;
#102321=CARTESIAN_POINT ( 'NONE',  ( -19.16726914849938979, 50.00000000000000000, 60.35899421978155743 ) ) ;
#102340=CARTESIAN_POINT ( 'NONE',  ( -10.51296777078104050, 50.00000000000000000, -92.64705882352942012 ) ) ;
#102358=CARTESIAN_POINT ( 'NONE',  ( -5.500000000458552307, 41.99999999999999289, -68.91429205817152592 ) ) ;
#102363=CARTESIAN_POINT ( 'NONE',  ( -12.86716125047998993, -4.999999999999999112, -10.20667643956625525 ) ) ;
#102364=CARTESIAN_POINT ( 'NONE',  ( -14.33580413386536812, 42.00000000000000000, -89.41414995615788541 ) ) ;
#102382=CARTESIAN_POINT ( 'NONE',  ( 6.738100180926640093, 41.71798714554645215, -59.05424661244425266 ) ) ;
#102383=CARTESIAN_POINT ( 'NONE',  ( -59.23741894013591036, 42.00000000000000711, 7.754160006507077263 ) ) ;
#102394=CARTESIAN_POINT ( 'NONE',  ( 6.453254806564252988, 41.48539221478000627, -58.52372623101098981 ) ) ;
#102399=FILL_AREA_STYLE_COLOUR ( '', #87914 ) ;
#102415=ORIENTED_EDGE ( 'NONE', *, *, #78369, .F. ) ;
#102419=B_SPLINE_CURVE_WITH_KNOTS ( 'NONE', 3,
 ( #52541, #77364, #105221, #103625, #38907, #19176, #60148, #63179, #52012, #22204, #87459, #87984, #84927, #85461, #3479, #79867, #54515, #46456, #11013, #36419, #21681, #5975, #43932, #71769, #104682, #30833, #98180, #66344, #40475, #74427, #502, #33470, #41013, #56649, #23258, #48021, #99227, #64761, #24850, #56102, #98696, #39958, #25394, #65817, #106256, #73898, #41537, #97636, #58250, #8102, #49626, #80102 ),
 .UNSPECIFIED., .F., .F.,
 ( 4, 1, 1, 1, 1, 1, 1, 2, 2, 1, 1, 1, 1, 1, 1, 1, 1, 1, 1, 2, 2, 1, 1, 1, 1, 1, 1, 1, 1, 2, 2, 1, 1, 1, 1, 1, 1, 1, 1, 2, 2, 4 ),
 ( 0.000000000000000000, 0.1250000000000170974, 0.1875000000000253686, 0.2187500000000295597, 0.2343750000000313916, 0.2421875000000320022, 0.2460937500000320854, 0.2480468750000324463, 0.2500000000000328071, 0.3750000000000618394, 0.4375000000000762723, 0.4687500000000834888, 0.4843750000000871525, 0.4921875000000889289, 0.4960937500000900391, 0.4980468750000908162, 0.4990234375000915379, 0.4995117187500917599, 0.4997558593750915934, 0.4998779296875914824, 0.5000000000000913714, 0.5625000000001059153, 0.5937500000001132427, 0.6093750000001169065, 0.6171875000001185718, 0.6210937500001195710, 0.6230468750001201261, 0.6240234375001204592, 0.6245117187501205702, 0.6247558593751206812, 0.6250000000001206812, 0.6875000000001317835, 0.7187500000001374456, 0.7343750000001403322, 0.7421875000001415534, 0.7460937500001423306, 0.7480468750001427747, 0.7490234375001427747, 0.7495117187501424416, 0.7497558593751425526, 0.7500000000001425526, 1.000000000000000000 ),
 .UNSPECIFIED. ) ;
#102425=CARTESIAN_POINT ( 'NONE',  ( -14.01509096962760736, 42.58675651153940578, -91.23243542799710326 ) ) ;
#102437=CARTESIAN_POINT ( 'NONE',  ( 12.76706325321343094, -5.000000000000002665, -81.58101990455240582 ) ) ;
#102444=PRESENTATION_STYLE_ASSIGNMENT (( #70611 ) ) ;
#102452=CARTESIAN_POINT ( 'NONE',  ( 0.000000000000000000, 0.000000000000000000, 0.000000000000000000 ) ) ;
#102456=CARTESIAN_POINT ( 'NONE',  ( -17.49999999999997158, 51.85440564192673918, 61.62473156926974838 ) ) ;
#102475=CARTESIAN_POINT ( 'NONE',  ( 1.843592604519097344, 42.00000000000000000, -60.21617040573095636 ) ) ;
#102490=( NAMED_UNIT ( * ) SI_UNIT ( $, .STERADIAN. ) SOLID_ANGLE_UNIT ( ) );
#102491=( BOUNDED_CURVE ( )  B_SPLINE_CURVE ( 2, ( #97729, #56739, #64336 ),
 .UNSPECIFIED., .F., .F. ) 
 B_SPLINE_CURVE_WITH_KNOTS ( ( 3, 3 ),
 ( 0.000000000000000000, 1.000000000000000000 ),
 .UNSPECIFIED. ) 
 CURVE ( )  GEOMETRIC_REPRESENTATION_ITEM ( )  RATIONAL_B_SPLINE_CURVE ( ( 1.000000000000000000, 1.857142857142858317, 1.000000000000000000 ) ) 
 REPRESENTATION_ITEM ( '' )  );
#102512=CARTESIAN_POINT ( 'NONE',  ( 7.230783190336673272, -4.999999999999994671, -70.90935357140938322 ) ) ;
#102534=CARTESIAN_POINT ( 'NONE',  ( -18.92291927219337921, 48.92936808311021935, 62.13088862737573237 ) ) ;
#102536=CARTESIAN_POINT ( 'NONE',  ( 6.592082458585389659, 40.00000000377368536, -71.20206342450474324 ) ) ;
#102560=CARTESIAN_POINT ( 'NONE',  ( -7.500000000000007105, 39.99999999999999289, -65.90297133634224735 ) ) ;
#102606=SURFACE_SIDE_STYLE ('',( #12513 ) ) ;
#102609=CARTESIAN_POINT ( 'NONE',  ( 51.21652843344448769, 40.83886418554102704, -40.08891448626480525 ) ) ;
#102618=CARTESIAN_POINT ( 'NONE',  ( 15.50526908259248593, 42.00000000004113332, 57.69562748392037577 ) ) ;
#102625=CARTESIAN_POINT ( 'NONE',  ( 31.45128802944020663, 39.42551091560301302, 56.96251755607489287 ) ) ;
#102629=ORIENTED_EDGE ( 'NONE', *, *, #102055, .T. ) ;
#102637=CARTESIAN_POINT ( 'NONE',  ( -7.135888613855453144, 41.99999999999999289, -71.74865085751117988 ) ) ;
#102645=CARTESIAN_POINT ( 'NONE',  ( -9.596002107494335576, 50.00000000000000000, -77.62543935900903591 ) ) ;
#102650=CARTESIAN_POINT ( 'NONE',  ( -7.500000000000006217, 40.28748324523081692, -68.91429205787007106 ) ) ;
#102660=CARTESIAN_POINT ( 'NONE',  ( -12.50000000000000533, -3.000000000000000888, -55.91956093573308806 ) ) ;
#102670=CARTESIAN_POINT ( 'NONE',  ( -6.686882633394676034, 40.00000000008991918, -71.19596940281091690 ) ) ;
#102672=ORIENTED_EDGE ( 'NONE', *, *, #58682, .F. ) ;
#102702=FACE_OUTER_BOUND ( 'NONE', #61273, .T. ) ;
#102710=CARTESIAN_POINT ( 'NONE',  ( 7.500000000000003553, 7.934965735923709573, -31.00258070019285839 ) ) ;
#102742=CARTESIAN_POINT ( 'NONE',  ( -6.951447413152006760, 41.73217189154441087, -59.36631701933645644 ) ) ;
#102750=CARTESIAN_POINT ( 'NONE',  ( 17.72825544378323315, 50.00000000000000711, 62.31995822720367073 ) ) ;
#102769=CYLINDRICAL_SURFACE ( 'NONE', #29265, 65.00000000000000000 ) ;
#102771=CARTESIAN_POINT ( 'NONE',  ( 6.302263272061760624, 41.90661423598773894, -70.03646374312130263 ) ) ;
#102811=CARTESIAN_POINT ( 'NONE',  ( 19.53694868228239301, 43.95068891796171329, -83.64113614449196632 ) ) ;
#102817=ORIENTED_EDGE ( 'NONE', *, *, #58862, .T. ) ;
#102818=CARTESIAN_POINT ( 'NONE',  ( 5.036189802309444907, 49.99999999999999289, -76.26213611588271135 ) ) ;
#102842=CARTESIAN_POINT ( 'NONE',  ( -5.213184022122961281, 6.017063975410835930, -26.57603910408765202 ) ) ;
#102845=VERTEX_POINT ( 'NONE', #103723 ) ;
#102860=CARTESIAN_POINT ( 'NONE',  ( -18.45708139111118484, 49.99999999999999289, 61.31329639225923955 ) ) ;
#102894=CARTESIAN_POINT ( 'NONE',  ( 7.036764705882354143, 40.00000000373363207, -71.06385277390853616 ) ) ;
#102898=CARTESIAN_POINT ( 'NONE',  ( -6.503415501679381983, 41.93912328290132052, -68.91429205811094505 ) ) ;
#102902=CARTESIAN_POINT ( 'NONE',  ( -16.24780601832367566, -5.000000000000000000, 2.396121698210679885 ) ) ;
#102903=CARTESIAN_POINT ( 'NONE',  ( -6.390966761371486449, 41.59892092783731954, -58.65495520917361461 ) ) ;
#102919=CARTESIAN_POINT ( 'NONE',  ( 6.641837668257387861, 41.74662779905570176, -59.04567176600482981 ) ) ;
#102920=CARTESIAN_POINT ( 'NONE',  ( -1.905220702120325443E-14, 42.00000000000000711, -59.23741894013591036 ) ) ;
#102947=DIRECTION ( 'NONE',  ( 0.000000000000000000, 1.000000000000000000, 0.000000000000000000 ) ) ;
#102958=CARTESIAN_POINT ( 'NONE',  ( -12.01455574841702933, -4.758509052971797715, -76.85604808874542471 ) ) ;
#102959=SURFACE_STYLE_FILL_AREA ( #95930 ) ;
#102971=CARTESIAN_POINT ( 'NONE',  ( 10.50942704840527142, -5.000000000000002665, -93.01494055616910828 ) ) ;
#102981=CARTESIAN_POINT ( 'NONE',  ( 0.000000000000000000, -3.331654917651224235, 0.000000000000000000 ) ) ;
#102986=DIRECTION ( 'NONE',  ( 0.000000000000000000, 1.000000000000000000, 0.000000000000000000 ) ) ;
#102995=ADVANCED_FACE ( 'NONE', ( #36121 ), #46295, .T. ) ;
#103013=CARTESIAN_POINT ( 'NONE',  ( 7.413001015142842931, 41.14546113202533206, -59.83891282166461423 ) ) ;
#103024=CARTESIAN_POINT ( 'NONE',  ( 8.812315315240748959, -4.999999999999999112, -14.88097931264037399 ) ) ;
#103048=CARTESIAN_POINT ( 'NONE',  ( 19.28427347342524101, 49.84851643466424065, 61.37487176993018778 ) ) ;
#103059=UNCERTAINTY_MEASURE_WITH_UNIT (LENGTH_MEASURE( 1.000000000000000082E-05 ), #88173, 'distance_accuracy_value', 'NONE');
#103071=PLANE ( 'NONE',  #105660 ) ;
#103072=CARTESIAN_POINT ( 'NONE',  ( 6.541889319079672305, 41.04792457379606674, -71.02384104322176483 ) ) ;
#103078=STYLED_ITEM ( 'NONE', ( #102444 ), #68281 ) ;
#103087=CARTESIAN_POINT ( 'NONE',  ( 5.293319439299095208, 18.44834697312474958, -37.82265432997213850 ) ) ;
#103089=CARTESIAN_POINT ( 'NONE',  ( 9.235395886531431551E-16, -3.000000000000000000, -8.000000000000000000 ) ) ;
#103093=CARTESIAN_POINT ( 'NONE',  ( -9.739726766100238464, -5.000000000005447198, -87.61747884500121586 ) ) ;
#103144=CARTESIAN_POINT ( 'NONE',  ( 22.68881653401906817, 43.82530270060863131, -79.30803424116763267 ) ) ;
#103154=CARTESIAN_POINT ( 'NONE',  ( -19.32152200348980742, 18.64316884709133504, -33.52312678235660570 ) ) ;
#103162=CARTESIAN_POINT ( 'NONE',  ( -64.56209935475503414, 39.42554120405374363, -8.095817184380026177 ) ) ;
#103173=CARTESIAN_POINT ( 'NONE',  ( 7.500000000000007105, -3.000000000000000000, -68.91429205785459544 ) ) ;
#103191=CARTESIAN_POINT ( 'NONE',  ( -7.996668423981794227, 47.99999999999998579, -91.14546719974913458 ) ) ;
#103193=CARTESIAN_POINT ( 'NONE',  ( 6.315295643000387038, -5.000000000000000000, -15.34937609225130117 ) ) ;
#103204=CARTESIAN_POINT ( 'NONE',  ( -6.208652854214004257, 40.93126280863162236, -71.11611043310642799 ) ) ;
#103226=STYLED_ITEM ( 'NONE', ( #71272 ), #69099 ) ;
#103229=CARTESIAN_POINT ( 'NONE',  ( -12.50000000000000533, 34.74998583579827738, -53.99885635920711024 ) ) ;
#103237=CARTESIAN_POINT ( 'NONE',  ( 7.268969833840798422, 41.22981915269870967, -58.87267939806292816 ) ) ;
#103244=CARTESIAN_POINT ( 'NONE',  ( 7.500000000000001776, 1.559114133231479071, -21.99325844590496004 ) ) ;
#103255=CARTESIAN_POINT ( 'NONE',  ( 7.500000000000008882, 42.00000000000000711, -71.41947339647146009 ) ) ;
#103263=CARTESIAN_POINT ( 'NONE',  ( 9.999999999999996447, -3.000000000000003109, -86.30899693899574743 ) ) ;
#103268=CARTESIAN_POINT ( 'NONE',  ( -58.90678327790940472, 50.00000000004006750, -28.11551192219710771 ) ) ;
#103272=CARTESIAN_POINT ( 'NONE',  ( -12.50000000000000355, 41.59226156894883530, -76.70843802411151557 ) ) ;
#103273=CARTESIAN_POINT ( 'NONE',  ( -6.494545593174295028, 41.94144595442993761, -59.61320170350516889 ) ) ;
#103280=B_SPLINE_CURVE_WITH_KNOTS ( 'NONE', 3,
 ( #28297, #2377, #12591, #20222, #19687, #12066, #28844, #52525, #86529, #68186, #19155, #101084, #27242, #85993, #44995, #60129, #20760, #101625, #18603, #77881, #76799, #92993, #51992, #53596, #45525, #4514, #35864, #51463, #68740, #100544, #10469, #27780, #60653, #70847, #55169, #72429, #22323 ),
 .UNSPECIFIED., .F., .F.,
 ( 4, 1, 1, 1, 1, 1, 2, 2, 1, 1, 1, 2, 2, 2, 1, 1, 1, 2, 2, 1, 1, 1, 1, 2, 2, 4 ),
 ( 0.000000000000000000, 0.1249999999995662636, 0.1874999999993494093, 0.2187499999992321420, 0.2343749999991734945, 0.2421874999991536770, 0.2460937499991533439, 0.2499999999991530664, 0.3124999999992191246, 0.3437499999992522093, 0.3593749999992681965, 0.3671874999992762456, 0.3749999999992841837, 0.4999999999994025890, 0.5624999999994684252, 0.5937499999995051736, 0.6093749999995236033, 0.6171874999995341504, 0.6249999999995448086, 0.6874999999996103117, 0.7187499999996449507, 0.7343749999996623812, 0.7421874999996695976, 0.7460937499996715960, 0.7499999999996734834, 1.000000000000000000 ),
 .UNSPECIFIED. ) ;
#103298=FACE_OUTER_BOUND ( 'NONE', #83850, .T. ) ;
#103329=FILL_AREA_STYLE_COLOUR ( '', #60024 ) ;
#103341=FILL_AREA_STYLE_COLOUR ( '', #18343 ) ;
#103386=CARTESIAN_POINT ( 'NONE',  ( -22.54429944894614835, 43.83586929555325895, -79.50671238563580800 ) ) ;
#103387=CARTESIAN_POINT ( 'NONE',  ( -18.55157383485121514, 50.00000000000000000, 61.19039212642342562 ) ) ;
#103399=ORIENTED_EDGE ( 'NONE', *, *, #8767, .T. ) ;
#103424=CARTESIAN_POINT ( 'NONE',  ( -6.645598051714149967, 41.91296950070219651, -68.91429205809731684 ) ) ;
#103429=CARTESIAN_POINT ( 'NONE',  ( 10.73738285532599512, -5.000000000000000000, 12.43173891483628601 ) ) ;
#103430=CARTESIAN_POINT ( 'NONE',  ( -5.921004821993908429, 41.52415853127881462, -58.52392862547825558 ) ) ;
#103436=CARTESIAN_POINT ( 'NONE',  ( -6.951447413152006760, 41.73217189154441087, -59.36631701933645644 ) ) ;
#103447=CARTESIAN_POINT ( 'NONE',  ( -57.69562748392037577, 41.99999999991776178, 15.50526908263360681 ) ) ;
#103480=B_SPLINE_CURVE_WITH_KNOTS ( 'NONE', 3,
 ( #15773, #15241, #50637, #23366, #96703, #81026, #40055, #48656, #22843, #55673 ),
 .UNSPECIFIED., .F., .F.,
 ( 4, 2, 2, 2, 4 ),
 ( 0.000000000000000000, 0.2500000000000000000, 0.5000000000000000000, 0.7500000000000000000, 1.000000000000000000 ),
 .UNSPECIFIED. ) ;
#103483=CARTESIAN_POINT ( 'NONE',  ( -12.08750511397919247, -4.706244484278460760, -76.83407907353502253 ) ) ;
#103532=CARTESIAN_POINT ( 'NONE',  ( 8.245342207438705273, 41.99999999999999289, -58.66077168407692710 ) ) ;
#103544=ORIENTED_EDGE ( 'NONE', *, *, #93922, .F. ) ;
#103545=CARTESIAN_POINT ( 'NONE',  ( -12.76371622530477090, -4.999999999999998224, 12.10534828917588435 ) ) ;
#103565=CARTESIAN_POINT ( 'NONE',  ( 19.41389256533520324, 49.95052971997019142, 60.89323077825420683 ) ) ;
#103590=CARTESIAN_POINT ( 'NONE',  ( -19.43447931428028141, 49.96600724177113761, 60.75670255394499009 ) ) ;
#103591=CARTESIAN_POINT ( 'NONE',  ( 5.558539409542769150, 40.95021212697733404, -70.99752138050020278 ) ) ;
#103596=B_SPLINE_CURVE_WITH_KNOTS ( 'NONE', 3,
 ( #90157, #31940, #82598, #81503, #65881, #24399, #97701, #42131, #24915, #74494 ),
 .UNSPECIFIED., .F., .F.,
 ( 4, 2, 2, 2, 4 ),
 ( 0.000000000000000000, 0.2499999999999999722, 0.5000000000000000000, 0.7500000000000000000, 1.000000000000000000 ),
 .UNSPECIFIED. ) ;
#103605=CARTESIAN_POINT ( 'NONE',  ( 5.272632769170305878, 14.19522521122798331, -33.98504043590990165 ) ) ;
#103611=CARTESIAN_POINT ( 'NONE',  ( 5.036189802309102070, -5.000000000000015099, -93.73786388411730286 ) ) ;
#103625=CARTESIAN_POINT ( 'NONE',  ( -23.01379380627861693, 43.78037731197083815, -78.86126435638672660 ) ) ;
#103642=FACE_OUTER_BOUND ( 'NONE', #85528, .T. ) ;
#103650=STYLED_ITEM ( 'NONE', ( #61131 ), #19950 ) ;
#103664=CARTESIAN_POINT ( 'NONE',  ( 37.85403811240345107, 42.20638415471038485, -58.45930149705038303 ) ) ;
#103667=CARTESIAN_POINT ( 'NONE',  ( 5.500000000000007105, 42.00000000000000000, -65.90297134474647578 ) ) ;
#103671=AXIS2_PLACEMENT_3D ( 'NONE', #81491, #64808, #7611 ) ;
#103677=CARTESIAN_POINT ( 'NONE',  ( 5.022013495303141006, 18.64316884711713840, 38.36535705883633796 ) ) ;
#103685=CARTESIAN_POINT ( 'NONE',  ( 23.32141611262068892, 39.42442110531605692, 60.74505580753970690 ) ) ;
#103687=ORIENTED_EDGE ( 'NONE', *, *, #37577, .T. ) ;
#103692=VERTEX_POINT ( 'NONE', #7284 ) ;
#103707=( NAMED_UNIT ( * ) SI_UNIT ( $, .STERADIAN. ) SOLID_ANGLE_UNIT ( ) );
#103714=CARTESIAN_POINT ( 'NONE',  ( 5.469880142252465660, -5.000000000000000000, -15.44784794604731637 ) ) ;
#103723=CARTESIAN_POINT ( 'NONE',  ( 9.235395886531431551E-16, -3.000000000000000000, -8.000000000000000000 ) ) ;
#103750=CARTESIAN_POINT ( 'NONE',  ( -12.50000000000000711, 34.67384678108815166, -53.88384558013568437 ) ) ;
#103753=( BOUNDED_SURFACE ( )  B_SPLINE_SURFACE ( 2, 3, ( 
 ( #11486, #53033, #77307, #61685, #3423, #102645, #36364, #100507, #94574, #44413, #20724, #85403, #19650, #69234, #28803, #2337, #10431, #28262, #27743, #52483, #53561, #92954, #20183, #85955, #76763, #10949, #86492, #35824, #12026, #101584, #45488, #44958, #77840, #3953 ),
 ( #19114, #26664, #51424, #69750, #68151, #78355, #59543, #34756, #67630, #92411, #18560, #43347, #76231, #35278, #27198, #101044, #51951, #87008, #97190, #80470, #6581, #79420, #95613, #96149, #104758, #63790, #13079, #22282, #21756, #5014, #56175, #46008, #5534, #55130 ),
 ( #23334, #30908, #47043, #38460, #46526, #14664, #88059, #96675, #79942, #47574, #39514, #37949, #22812, #71327, #55647, #29847, #87529, #72389, #70807, #4479, #88583, #71852, #105293, #104220, #14140, #62725, #31439, #30367, #54591, #13611, #37416, #63258, #64317, #6052 ) ),
 .UNSPECIFIED., .F., .T., .F. ) 
 B_SPLINE_SURFACE_WITH_KNOTS ( ( 3, 3 ),
 ( 4, 2, 2, 2, 2, 2, 2, 2, 2, 2, 2, 2, 2, 2, 2, 2, 4 ),
 ( 0.000000000000000000, 1.000000000000000000 ),
 ( -3.141592653589793116, -2.748893571891068976, -2.356194490192344837, -1.963495408493620697, -1.570796326794896558, -1.178097245096172418, -0.7853981633974482790, -0.3926990816987241395, 0.000000000000000000, 0.3926990816987241395, 0.7853981633974482790, 1.178097245096172418, 1.570796326794896558, 1.963495408493620697, 2.356194490192344837, 2.748893571891068976, 3.141592653589793116 ),
 .UNSPECIFIED. ) 
 GEOMETRIC_REPRESENTATION_ITEM ( )  RATIONAL_B_SPLINE_SURFACE ( (
 ( 1.000000000000000000, 1.000000000000000000, 1.000000000000000000, 1.000000000000000000, 1.000000000000000000, 1.000000000000000000, 1.000000000000000000, 1.000000000000000000, 1.000000000000000000, 1.000000000000000000, 1.000000000000000000, 1.000000000000000000, 1.000000000000000000, 1.000000000000000000, 1.000000000000000000, 1.000000000000000000, 1.000000000000000000, 1.000000000000000000, 1.000000000000000000, 1.000000000000000000, 1.000000000000000000, 1.000000000000000000, 1.000000000000000000, 1.000000000000000000, 1.000000000000000000, 1.000000000000000000, 1.000000000000000000, 1.000000000000000000, 1.000000000000000000, 1.000000000000000000, 1.000000000000000000, 1.000000000000000000, 1.000000000000000000, 1.000000000000000000),
 ( 1.857142857142858317, 1.857142857142858317, 1.857142857142858317, 1.857142857142858317, 1.857142857142858317, 1.857142857142858317, 1.857142857142858317, 1.857142857142858317, 1.857142857142858317, 1.857142857142858317, 1.857142857142858317, 1.857142857142858317, 1.857142857142858317, 1.857142857142858317, 1.857142857142858317, 1.857142857142858317, 1.857142857142858317, 1.857142857142858317, 1.857142857142858317, 1.857142857142858317, 1.857142857142858317, 1.857142857142858317, 1.857142857142858317, 1.857142857142858317, 1.857142857142858317, 1.857142857142858317, 1.857142857142858317, 1.857142857142858317, 1.857142857142858317, 1.857142857142858317, 1.857142857142858317, 1.857142857142858317, 1.857142857142858317, 1.857142857142858317),
 ( 1.000000000000000000, 1.000000000000000000, 1.000000000000000000, 1.000000000000000000, 1.000000000000000000, 1.000000000000000000, 1.000000000000000000, 1.000000000000000000, 1.000000000000000000, 1.000000000000000000, 1.000000000000000000, 1.000000000000000000, 1.000000000000000000, 1.000000000000000000, 1.000000000000000000, 1.000000000000000000, 1.000000000000000000, 1.000000000000000000, 1.000000000000000000, 1.000000000000000000, 1.000000000000000000, 1.000000000000000000, 1.000000000000000000, 1.000000000000000000, 1.000000000000000000, 1.000000000000000000, 1.000000000000000000, 1.000000000000000000, 1.000000000000000000, 1.000000000000000000, 1.000000000000000000, 1.000000000000000000, 1.000000000000000000, 1.000000000000000000) ) ) 
 REPRESENTATION_ITEM ( '' )  SURFACE ( )  );
#103761=CARTESIAN_POINT ( 'NONE',  ( 7.040774347399620936, 41.35742771039598153, -58.68913404742972517 ) ) ;
#103787=CARTESIAN_POINT ( 'NONE',  ( -65.26738680890619548, 48.00000000000000000, 0.8120011905346659065 ) ) ;
#103793=CARTESIAN_POINT ( 'NONE',  ( -5.701072573891631912, 41.97507564787665757, -59.34341760267744803 ) ) ;
#103795=CARTESIAN_POINT ( 'NONE',  ( 11.94619295074513410, -4.803972694421123180, -76.87644205112506768 ) ) ;
#103813=CARTESIAN_POINT ( 'NONE',  ( 56.71111273679790088, 49.99999999999999289, 27.46638368304382993 ) ) ;
#103817=ORIENTED_EDGE ( 'NONE', *, *, #3335, .F. ) ;
#103819=CARTESIAN_POINT ( 'NONE',  ( -14.75116209839011994, 43.55504285526384933, -90.22050492866908655 ) ) ;
#103831=CARTESIAN_POINT ( 'NONE',  ( -7.036764705882398552, 40.00000000007573675, -71.06385277390853616 ) ) ;
#103840=CARTESIAN_POINT ( 'NONE',  ( -12.13034742782427955, 48.00000000000000000, -93.82352941176471006 ) ) ;
#103844=EDGE_CURVE ( 'NONE', #23955, #19635, #37803, .T. ) ;
#103845=CARTESIAN_POINT ( 'NONE',  ( 17.50000000000002132, 47.99999999999999289, 64.09953197957062798 ) ) ;
#103854=ORIENTED_EDGE ( 'NONE', *, *, #19931, .F. ) ;
#103875=EDGE_CURVE ( 'NONE', #90268, #37125, #11770, .T. ) ;
#103886=CARTESIAN_POINT ( 'NONE',  ( -5.272286809540803532, 14.23042150740707079, -34.01614571496379114 ) ) ;
#103905=CARTESIAN_POINT ( 'NONE',  ( -18.38921465765557173, 50.00000000000000000, 61.39959187812481645 ) ) ;
#103921=CARTESIAN_POINT ( 'NONE',  ( -13.18841494988442342, 42.68946335806984393, -92.36892705870020848 ) ) ;
#103936=ORIENTED_EDGE ( 'NONE', *, *, #90136, .T. ) ;
#103943=CARTESIAN_POINT ( 'NONE',  ( -5.700736385538761830, 42.00193813219923555, -69.19507739564853921 ) ) ;
#103949=CARTESIAN_POINT ( 'NONE',  ( -6.263552781412762727, 41.61160193526471573, -58.64895252977191120 ) ) ;
#103955=CARTESIAN_POINT ( 'NONE',  ( -6.831363903021533623, 41.73171925724633979, -59.17722475679354233 ) ) ;
#103966=CARTESIAN_POINT ( 'NONE',  ( 5.902962692465450800, 41.87327339699978523, -59.02279353628206593 ) ) ;
#103967=CARTESIAN_POINT ( 'NONE',  ( 10.04205104294044482, 18.64316884711816513, -37.36680950588930727 ) ) ;
#103971=EDGE_CURVE ( 'NONE', #89440, #27308, #78435, .T. ) ;
#103993=CARTESIAN_POINT ( 'NONE',  ( -12.34835181856066555, -4.332967528434497062, -12.86601580078907148 ) ) ;
#103995=CARTESIAN_POINT ( 'NONE',  ( 7.500000000000007105, -3.000000000000000000, -68.91429205785459544 ) ) ;
#104001=FILL_AREA_STYLE_COLOUR ( '', #64501 ) ;
#104016=CARTESIAN_POINT ( 'NONE',  ( 6.876313068639422710, -4.333298119783811408, 16.54772121370670135 ) ) ;
#104024=SURFACE_STYLE_FILL_AREA ( #12885 ) ;
#104025=FILL_AREA_STYLE_COLOUR ( '', #77479 ) ;
#104052=CARTESIAN_POINT ( 'NONE',  ( 6.459123244420549526, 42.00000000000000000, -59.79223455627352735 ) ) ;
#104053=CARTESIAN_POINT ( 'NONE',  ( 12.49986889690059222, -3.000000000000002665, -76.70852482682694529 ) ) ;
#104071=CARTESIAN_POINT ( 'NONE',  ( -18.91781669292785395, 48.00000000000000000, 62.18610382930904734 ) ) ;
#104086=CARTESIAN_POINT ( 'NONE',  ( 19.39022949357585546, 49.93247698687046210, 61.01543061342935914 ) ) ;
#104124=( GEOMETRIC_REPRESENTATION_CONTEXT ( 3 ) GLOBAL_UNCERTAINTY_ASSIGNED_CONTEXT ( ( #35156 ) ) GLOBAL_UNIT_ASSIGNED_CONTEXT ( ( #70053, #94883, #21023 ) ) REPRESENTATION_CONTEXT ( 'NONE', 'WORKASPACE' ) );
#104132=CARTESIAN_POINT ( 'NONE',  ( -1.308996937480704004, -4.999999999999988454, -95.00000000000001421 ) ) ;
#104148=B_SPLINE_SURFACE_WITH_KNOTS ( 'NONE', 3, 3, ( 
 ( #23919, #73475, #7674, #14711, #97752, #105334, #106372, #105850, #63829, #16310 ),
 ( #96718, #39555, #74014, #49743, #33065, #40067, #55691, #65405, #90746, #98298 ),
 ( #82651, #89153, #8223, #80507, #56760, #88620, #64869, #6628, #24455, #31478 ),
 ( #8752, #71899, #89688, #64361, #15785, #97231, #90211, #23378, #82102, #104800 ),
 ( #30952, #56215, #96, #15255, #65935, #98814, #24969, #16864, #48141, #22854 ),
 ( #81039, #7155, #72945, #31996, #91291, #11256, #43643, #44187, #77075, #78134 ),
 ( #52257, #3190, #36661, #101878, #86786, #28038, #68466, #69527, #94337, #36135 ),
 ( #76532, #60910, #86256, #69003, #28560, #33584, #35589, #101357, #77614, #93798 ) ),
 .UNSPECIFIED., .F., .F., .F.,
 ( 4, 2, 2, 4 ),
 ( 4, 2, 2, 2, 4 ),
 ( 0.000000000000000000, 0.2500000000000000000, 0.5000000000000000000, 1.000000000000000000 ),
 ( 0.000000000000000000, 0.1250000000000000000, 0.2500000000000000000, 0.5000000000000000000, 1.000000000000000000 ),
 .UNSPECIFIED. ) ;
#104163=EDGE_LOOP ( 'NONE', ( #43877, #63713, #102185, #70637, #102415, #51997 ) ) ;
#104164=SURFACE_STYLE_USAGE ( .BOTH. , #89054 ) ;
#104189=ORIENTED_EDGE ( 'NONE', *, *, #59720, .T. ) ;
#104195=CARTESIAN_POINT ( 'NONE',  ( -15.50526908267491066, 41.99999999999999289, 57.69562748408483088 ) ) ;
#104201=CARTESIAN_POINT ( 'NONE',  ( -56.56213115054879381, 39.42553718104704785, 32.16477550070589331 ) ) ;
#104220=CARTESIAN_POINT ( 'NONE',  ( 9.739726766100236688, 48.00000000000000000, -87.61747884500007899 ) ) ;
#104226=CARTESIAN_POINT ( 'NONE',  ( -16.06635273549532883, 42.44526696066479587, -88.41241673432038795 ) ) ;
#104272=CARTESIAN_POINT ( 'NONE',  ( -12.50000000000000533, 26.69172216273781117, -44.20484773317921423 ) ) ;
#104281=CARTESIAN_POINT ( 'NONE',  ( 6.951447288752834019, 41.73217225470716585, -59.36631759480938086 ) ) ;
#104286=CARTESIAN_POINT ( 'NONE',  ( 7.500000000000001776, -4.015205788346293048, -20.09376801818934766 ) ) ;
#104313=CARTESIAN_POINT ( 'NONE',  ( 56.06936961874005476, 50.00000000006009770, -33.41736086627872027 ) ) ;
#104326=CARTESIAN_POINT ( 'NONE',  ( 17.98163244489454726, 50.00000000000000000, 61.91178591759881300 ) ) ;
#104335=PLANE ( 'NONE',  #66675 ) ;
#104384=CARTESIAN_POINT ( 'NONE',  ( -7.149999999999890221, 41.65000000000012648, -59.82695526680724640 ) ) ;
#104389=CARTESIAN_POINT ( 'NONE',  ( -2.617478844988693432, 48.00000000000000000, -94.73972676610495114 ) ) ;
#104392=SURFACE_SIDE_STYLE ('',( #38630 ) ) ;
#104407=( NAMED_UNIT ( * ) PLANE_ANGLE_UNIT ( ) SI_UNIT ( $, .RADIAN. ) );
#104414=CARTESIAN_POINT ( 'NONE',  ( 5.219866590719942856, -5.000000000000000000, -8.922269033013279227 ) ) ;
#104416=CARTESIAN_POINT ( 'NONE',  ( -5.290983596874198724, 17.95105532768313594, -37.37422055138609522 ) ) ;
#104432=CARTESIAN_POINT ( 'NONE',  ( -18.66418957901244724, 50.00000000000000711, 61.03986302535336250 ) ) ;
#104441=CARTESIAN_POINT ( 'NONE',  ( 17.50000000000001066, 51.39211690089886986, 62.71362001260527563 ) ) ;
#104495=ORIENTED_EDGE ( 'NONE', *, *, #38825, .T. ) ;
#104500=CARTESIAN_POINT ( 'NONE',  ( 6.294742690869562729, 41.94828263799632850, -59.44631289860604539 ) ) ;
#104501=( GEOMETRIC_REPRESENTATION_CONTEXT ( 3 ) GLOBAL_UNCERTAINTY_ASSIGNED_CONTEXT ( ( #11363 ) ) GLOBAL_UNIT_ASSIGNED_CONTEXT ( ( #41082, #36756, #27067 ) ) REPRESENTATION_CONTEXT ( 'NONE', 'WORKASPACE' ) );
#104526=EDGE_CURVE ( 'NONE', #54991, #38679, #101087, .T. ) ;
#104533=CARTESIAN_POINT ( 'NONE',  ( -12.50000000000000355, -3.000000000000001776, -76.70872284621019332 ) ) ;
#104534=UNCERTAINTY_MEASURE_WITH_UNIT (LENGTH_MEASURE( 1.000000000000000082E-05 ), #26585, 'distance_accuracy_value', 'NONE');
#104540=( BOUNDED_CURVE ( )  B_SPLINE_CURVE ( 2, ( #103995, #47874, #5833 ),
 .UNSPECIFIED., .F., .F. ) 
 B_SPLINE_CURVE_WITH_KNOTS ( ( 3, 3 ),
 ( 0.000000000000000000, 1.000000000000000000 ),
 .UNSPECIFIED. ) 
 CURVE ( )  GEOMETRIC_REPRESENTATION_ITEM ( )  RATIONAL_B_SPLINE_CURVE ( ( 1.000000000000000000, 1.857142857142858317, 1.000000000000000000 ) ) 
 REPRESENTATION_ITEM ( '' )  );
#104555=CARTESIAN_POINT ( 'NONE',  ( -2.094395098902536390, -4.999999999999998224, -8.000000000000000000 ) ) ;
#104560=FACE_BOUND ( 'NONE', #63950, .T. ) ;
#104562=CARTESIAN_POINT ( 'NONE',  ( 11.69514296591814961, -5.000000000000000000, -88.12259424195812585 ) ) ;
#104574=EDGE_CURVE ( 'NONE', #93003, #81288, #53970, .T. ) ;
#104616=VECTOR ( 'NONE', #90539, 1000.000000000000000 ) ;
#104643=CARTESIAN_POINT ( 'NONE',  ( -19.35755210044912289, 49.90709869893811401, 61.15086111258641210 ) ) ;
#104650=VECTOR ( 'NONE', #20064, 1000.000000000000000 ) ;
#104663=CARTESIAN_POINT ( 'NONE',  ( 4.028951842967195773, -3.000000000000000444, 6.990291106834064294 ) ) ;
#104667=CARTESIAN_POINT ( 'NONE',  ( -9.999999999999992895, -3.000000000000002665, -83.69100306252320820 ) ) ;
#104671=( GEOMETRIC_REPRESENTATION_CONTEXT ( 3 ) GLOBAL_UNCERTAINTY_ASSIGNED_CONTEXT ( ( #95485 ) ) GLOBAL_UNIT_ASSIGNED_CONTEXT ( ( #56930, #83878, #42897 ) ) REPRESENTATION_CONTEXT ( 'NONE', 'WORKASPACE' ) );
#104679=CARTESIAN_POINT ( 'NONE',  ( 5.689604056830701140, -4.325321803359224226, -16.92223617908316413 ) ) ;
#104682=CARTESIAN_POINT ( 'NONE',  ( -34.55272070743144042, 42.66495351264344293, -62.99786256745820623 ) ) ;
#104693=CARTESIAN_POINT ( 'NONE',  ( -52.56483885390523625, 40.83906611473335602, -38.23529411764706509 ) ) ;
#104703=CARTESIAN_POINT ( 'NONE',  ( 0.000000000000000000, 0.000000000000000000, 0.000000000000000000 ) ) ;
#104715=CARTESIAN_POINT ( 'NONE',  ( -4.651132217449170270, -5.000000000000000000, -15.66661053588738106 ) ) ;
#104721=CARTESIAN_POINT ( 'NONE',  ( 34.56161316558368668, 42.66376877430343484, -62.98563745867910768 ) ) ;
#104739=CARTESIAN_POINT ( 'NONE',  ( 5.938258408366269947, 39.42529018484425052, 64.79746803155040880 ) ) ;
#104758=CARTESIAN_POINT ( 'NONE',  ( 9.999999999999989342, 49.99999999999999289, -86.30899693748767731 ) ) ;
#104775=CARTESIAN_POINT ( 'NONE',  ( 6.286008769881732405, -5.000000000000000000, -15.35021772302718190 ) ) ;
#104781=( LENGTH_UNIT ( ) NAMED_UNIT ( * ) SI_UNIT ( .MILLI., .METRE. ) );
#104800=CARTESIAN_POINT ( 'NONE',  ( 7.412969500702210723, 41.14559805159964156, -68.91429205978418793 ) ) ;
#104811=CARTESIAN_POINT ( 'NONE',  ( -12.50000000000000888, 33.93135344289294864, -52.79621944607910677 ) ) ;
#104831=AXIS2_PLACEMENT_3D ( 'NONE', #20445, #52743, #37133 ) ;
#104846=CARTESIAN_POINT ( 'NONE',  ( 7.500000000000007105, 42.00000000000000711, -62.89165061482971453 ) ) ;
#104857=COLOUR_RGB ( '', 0.08235294, 0.09019608, 0.10196078) ;
#104860=CARTESIAN_POINT ( 'NONE',  ( -23.38163988261890225, 49.99999999999999289, 60.94087333798560735 ) ) ;
#104866=B_SPLINE_CURVE_WITH_KNOTS ( 'NONE', 3,
 ( #79611, #87197, #5211, #69422, #87729, #12221, #13807, #94223, #102842, #5726, #38142, #46720, #38650, #13274, #95287, #12751, #45151, #70996, #102305, #78032, #103886, #78554, #71516, #96354, #104416, #4150, #30562, #63461, #22485, #85610, #94769, #11684, #4683, #37079, #69945, #29010, #20918 ),
 .UNSPECIFIED., .F., .F.,
 ( 4, 2, 2, 2, 1, 1, 1, 1, 1, 1, 2, 2, 2, 2, 1, 1, 1, 1, 1, 1, 1, 2, 2, 2, 4 ),
 ( 0.000000000000000000, 0.1250000000000049405, 0.1875000000000073552, 0.2187500000000086042, 0.2343750000000092704, 0.2421875000000095757, 0.2460937500000097145, 0.2480468750000097422, 0.2490234375000097422, 0.2495117187500097422, 0.2497558593750097700, 0.2500000000000097700, 0.3750000000000363598, 0.4375000000000498490, 0.4687500000000565659, 0.4843750000000598965, 0.4921875000000616174, 0.4960937500000625056, 0.4980468750000630052, 0.4990234375000631162, 0.4995117187500632827, 0.4997558593750633382, 0.5000000000000633937, 0.7500000000000316414, 1.000000000000000000 ),
 .UNSPECIFIED. ) ;
#104867=EDGE_CURVE ( 'NONE', #21082, #80415, #61862, .T. ) ;
#104906=B_SPLINE_CURVE_WITH_KNOTS ( 'NONE', 3,
 ( #85745, #35613, #60409, #11275, #77095, #3215, #11816, #34016, #44748, #1042, #99774, #18354, #75494, #25944, #91699, #2123, #92201, #1590, #17812, #42597, #50663, #83579, #67425, #9687, #67945, #100302, #59330, #84128, #51207, #100826, #59872, #92746, #38264, #63045 ),
 .UNSPECIFIED., .F., .F.,
 ( 4, 2, 2, 2, 2, 2, 2, 2, 2, 2, 2, 2, 2, 2, 2, 2, 4 ),
 ( 0.000000000000000000, 0.06250000000000000000, 0.1250000000000000000, 0.1875000000000000000, 0.2500000000000000000, 0.3125000000000000000, 0.3750000000000000000, 0.4375000000000000000, 0.5000000000000000000, 0.5625000000000000000, 0.6250000000000000000, 0.6875000000000000000, 0.7500000000000000000, 0.8125000000000000000, 0.8750000000000000000, 0.9375000000000000000, 1.000000000000000000 ),
 .UNSPECIFIED. ) ;
#104909=CARTESIAN_POINT ( 'NONE',  ( -7.040972322291190189, 41.74416393942964731, -59.82830748482982841 ) ) ;
#104919=CARTESIAN_POINT ( 'NONE',  ( 7.195949543451931163, 41.08281217721444278, -58.60025093677088392 ) ) ;
#104923=CARTESIAN_POINT ( 'NONE',  ( 10.51296777078104050, 50.00000000000000000, -92.64705882352942012 ) ) ;
#104929=CARTESIAN_POINT ( 'NONE',  ( 0.000000000000000000, -5.000000000000000888, -73.00000000000001421 ) ) ;
#104968=FACE_OUTER_BOUND ( 'NONE', #6189, .T. ) ;
#104995=CARTESIAN_POINT ( 'NONE',  ( -7.334017076212031583, -3.381213663715922468, -18.44266608209038338 ) ) ;
#105003=ORIENTED_EDGE ( 'NONE', *, *, #18780, .F. ) ;
#105020=CARTESIAN_POINT ( 'NONE',  ( 4.205882352941182845, -5.000000000000002665, -72.69916451482998809 ) ) ;
#105047=CARTESIAN_POINT ( 'NONE',  ( 6.494545870870014781, 41.94144576370731414, -59.61320117837396282 ) ) ;
#105072=FACE_OUTER_BOUND ( 'NONE', #18729, .T. ) ;
#105102=CARTESIAN_POINT ( 'NONE',  ( 7.137815226408910974, -4.999999999999998224, 4.175893272575850190 ) ) ;
#105112=ORIENTED_EDGE ( 'NONE', *, *, #93572, .F. ) ;
#105123=CARTESIAN_POINT ( 'NONE',  ( 1.469576158976823356E-15, 50.00000000000000000, -73.00000000000001421 ) ) ;
#105158=CARTESIAN_POINT ( 'NONE',  ( 19.09459860920181029, 49.66572022866124314, 61.74879405875589100 ) ) ;
#105169=LINE ( 'NONE', #70155, #75833 ) ;
#105191=CARTESIAN_POINT ( 'NONE',  ( 18.35799360122013724, 45.00000000000000000, 62.38167341223874018 ) ) ;
#105200=ORIENTED_EDGE ( 'NONE', *, *, #104574, .T. ) ;
#105207=CARTESIAN_POINT ( 'NONE',  ( 9.999999999999994671, -3.000000000000002665, -83.69100306252322241 ) ) ;
#105218=CARTESIAN_POINT ( 'NONE',  ( 7.499999907820169120, -3.000141485254359086, -20.99866594743181736 ) ) ;
#105221=CARTESIAN_POINT ( 'NONE',  ( -20.41470034681368872, 43.90732458266749205, -82.43442711126550648 ) ) ;
#105234=CARTESIAN_POINT ( 'NONE',  ( -7.040774328009894667, 41.35742559143615438, -58.68913211047703982 ) ) ;
#105241=CARTESIAN_POINT ( 'NONE',  ( -9.500000000000003553, -4.999999999999998224, -68.91429205785459544 ) ) ;
#105256=CARTESIAN_POINT ( 'NONE',  ( 3.140974613990258568, -5.000000000000002665, -73.31232788067565309 ) ) ;
#105259=( NAMED_UNIT ( * ) SI_UNIT ( $, .STERADIAN. ) SOLID_ANGLE_UNIT ( ) );
#105276=CARTESIAN_POINT ( 'NONE',  ( -63.01300532932567222, 38.95394457514182562, 9.559250005201390010 ) ) ;
#105293=CARTESIAN_POINT ( 'NONE',  ( 8.737863884125493641, 48.00000000000000000, -90.03618980230170621 ) ) ;
#105310=CARTESIAN_POINT ( 'NONE',  ( 9.352623941358347182, -4.999999999999999112, -18.60510039294834783 ) ) ;
#105334=CARTESIAN_POINT ( 'NONE',  ( 6.921856739985490670, 41.59435684990518922, -70.13580383465757961 ) ) ;
#105351=ORIENTED_EDGE ( 'NONE', *, *, #105959, .F. ) ;
#105356=CARTESIAN_POINT ( 'NONE',  ( 7.320805580757752118, 41.41776788117373798, -59.82972163162600054 ) ) ;
#105383=CARTESIAN_POINT ( 'NONE',  ( 51.78317192880091113, 40.83906611472102810, 39.73656039206255741 ) ) ;
#105392=CARTESIAN_POINT ( 'NONE',  ( 11.60474022311935016, -4.919048487758927557, -76.97896355670452806 ) ) ;
#105399=CARTESIAN_POINT ( 'NONE',  ( 18.61247279103750074, 50.00000000000000000, 61.10966258427338715 ) ) ;
#105401=EDGE_CURVE ( 'NONE', #71944, #67484, #65446, .T. ) ;
#105428=CARTESIAN_POINT ( 'NONE',  ( -6.503373625913253520, 41.93912930209143042, -59.84719177782724131 ) ) ;
#105429=( GEOMETRIC_REPRESENTATION_CONTEXT ( 3 ) GLOBAL_UNCERTAINTY_ASSIGNED_CONTEXT ( ( #91525 ) ) GLOBAL_UNIT_ASSIGNED_CONTEXT ( ( #60614, #60088, #102103 ) ) REPRESENTATION_CONTEXT ( 'NONE', 'WORKASPACE' ) );
#105436=DIRECTION ( 'NONE',  ( 0.000000000000000000, 1.000000000000000000, 0.000000000000000000 ) ) ;
#105447=FACE_OUTER_BOUND ( 'NONE', #32106, .T. ) ;
#105469=VERTEX_POINT ( 'NONE', #31141 ) ;
#105480=CARTESIAN_POINT ( 'NONE',  ( -7.137815226411302838, -3.000000000000000000, -4.175893272573455661 ) ) ;
#105500=CARTESIAN_POINT ( 'NONE',  ( -14.91339176601161043, 41.98696008795855050, -86.62219925848557978 ) ) ;
#105509=CARTESIAN_POINT ( 'NONE',  ( 17.50000000000006040, 51.01864103016391994, 63.17274301512998136 ) ) ;
#105517=CARTESIAN_POINT ( 'NONE',  ( -6.793650603639286523, -4.999999999999960920, -15.34177241507040002 ) ) ;
#105519=( GEOMETRIC_REPRESENTATION_CONTEXT ( 3 ) GLOBAL_UNCERTAINTY_ASSIGNED_CONTEXT ( ( #42723 ) ) GLOBAL_UNIT_ASSIGNED_CONTEXT ( ( #82239, #72561, #96855 ) ) REPRESENTATION_CONTEXT ( 'NONE', 'WORKASPACE' ) );
#105539=SURFACE_STYLE_USAGE ( .BOTH. , #16003 ) ;
#105554=CARTESIAN_POINT ( 'NONE',  ( -17.49999999999995737, 47.99999999999999289, 62.61753806507838505 ) ) ;
#105564=CARTESIAN_POINT ( 'NONE',  ( 6.777273857537102764, 41.87254887207789267, -59.70743237412717974 ) ) ;
#105617=CARTESIAN_POINT ( 'NONE',  ( -8.000000000000003553, -3.000000000000000000, -2.094395098902523511 ) ) ;
#105622=CARTESIAN_POINT ( 'NONE',  ( -10.50000000000000000, -5.000000000000000000, -34.12705337366766400 ) ) ;
#105660=AXIS2_PLACEMENT_3D ( 'NONE', #4365, #61028, #11917 ) ;
#105692=CARTESIAN_POINT ( 'NONE',  ( 5.658904754127976666, 41.71506038590904808, -58.75003921181337319 ) ) ;
#105715=CARTESIAN_POINT ( 'NONE',  ( -7.450977790876272877, -5.000000000000000000, -15.56369424074723895 ) ) ;
#105723=CARTESIAN_POINT ( 'NONE',  ( -17.49999999999996803, 47.99999999999999289, 64.09953197957064219 ) ) ;
#105734=CARTESIAN_POINT ( 'NONE',  ( -7.360438360673518865, 50.00000000000000711, -75.39006186639038276 ) ) ;
#105757=CARTESIAN_POINT ( 'NONE',  ( -7.758748231291410669, -5.000000000000001776, -73.00623724569611284 ) ) ;
#105767=CARTESIAN_POINT ( 'NONE',  ( -42.65225745549071235, 39.48366440724160498, -49.42417087154653643 ) ) ;
#105775=CARTESIAN_POINT ( 'NONE',  ( 11.68767211932355998, -5.000000000000002665, -81.85902538600510070 ) ) ;
#105796=CARTESIAN_POINT ( 'NONE',  ( -53.90990825086682037, 38.95404129820931161, 33.99650454723879278 ) ) ;
#105831=CARTESIAN_POINT ( 'NONE',  ( -6.831363903021532735, 41.73171925724633979, -59.17722475679354233 ) ) ;
#105843=VERTEX_POINT ( 'NONE', #24518 ) ;
#105850=CARTESIAN_POINT ( 'NONE',  ( 7.069742150690450089, 41.66287055390499461, -69.58314084581829206 ) ) ;
#105862=CARTESIAN_POINT ( 'NONE',  ( -54.98704968389372993, 50.00000000000000711, 30.77402402440401019 ) ) ;
#105868=EDGE_CURVE ( 'NONE', #58075, #21912, #55098, .T. ) ;
#105872=CARTESIAN_POINT ( 'NONE',  ( 7.417432790609828963, 41.15875988143464781, -59.49136470043579550 ) ) ;
#105884=CARTESIAN_POINT ( 'NONE',  ( 12.76511086933744998, 42.41840947608824308, -92.95087395602729430 ) ) ;
#105888=ADVANCED_FACE ( 'NONE', ( #39622 ), #41845, .T. ) ;
#105912=CARTESIAN_POINT ( 'NONE',  ( 5.694238939648077036, 41.34481830655865764, -58.37580827183571586 ) ) ;
#105917=STYLED_ITEM ( 'NONE', ( #77931 ), #87591 ) ;
#105949=SURFACE_SIDE_STYLE ('',( #48241 ) ) ;
#105959=EDGE_CURVE ( 'NONE', #20, #5264, #65340, .T. ) ;
#105960=CARTESIAN_POINT ( 'NONE',  ( -3.122594241999163689, -5.000000000000000888, -96.69514296588273794 ) ) ;
#105967=CARTESIAN_POINT ( 'NONE',  ( 19.51720561627331918, 41.98713188461248080, -83.66827837336637685 ) ) ;
#105983=CARTESIAN_POINT ( 'NONE',  ( 55.63518754870391803, 38.95383793067261990, 32.06611684423706521 ) ) ;
#105995=CARTESIAN_POINT ( 'NONE',  ( -8.000000000000000000, -4.999999999999998224, -2.094395098902523955 ) ) ;
#106021=CARTESIAN_POINT ( 'NONE',  ( 17.49999999999435119, 50.00908096117762369, 61.65219700478674270 ) ) ;
#106029=CARTESIAN_POINT ( 'NONE',  ( 5.129365358145452802, 41.91296950070222493, -69.99827769498368468 ) ) ;
#106030=CARTESIAN_POINT ( 'NONE',  ( -7.253185102483167945, -3.609892095628724373, -18.04361009490900614 ) ) ;
#106053=CARTESIAN_POINT ( 'NONE',  ( 65.26738680894031575, 49.99999999999999289, 0.8120011905333047730 ) ) ;
#106079=CARTESIAN_POINT ( 'NONE',  ( 22.96637035739885135, 41.68994590335805839, -75.70120662748654183 ) ) ;
#106080=CARTESIAN_POINT ( 'NONE',  ( 5.420470438621152631, 41.88321586334136981, -59.04137885805278785 ) ) ;
#106117=EDGE_CURVE ( 'NONE', #54340, #38992, #72639, .T. ) ;
#106132=CARTESIAN_POINT ( 'NONE',  ( 8.000000000000000000, -3.000000000000000000, 2.094395098902537722 ) ) ;
#106135=CARTESIAN_POINT ( 'NONE',  ( 0.000000000000000000, 0.000000000000000000, 0.000000000000000000 ) ) ;
#106143=MECHANICAL_DESIGN_GEOMETRIC_PRESENTATION_REPRESENTATION('',(#75114),#73417);
#106179=CARTESIAN_POINT ( 'NONE',  ( -59.99387666504471639, 48.00000000000000711, 25.54086645653091026 ) ) ;
#106196=CARTESIAN_POINT ( 'NONE',  ( 0.000000000000000000, -5.000000000000000000, 10.00000000000000000 ) ) ;
#106229=CARTESIAN_POINT ( 'NONE',  ( 17.53291882538153601, 45.00000000000002132, 63.43016343176445559 ) ) ;
#106238=CARTESIAN_POINT ( 'NONE',  ( 4.028951842967195773, -3.000000000000000444, -6.990291106834061630 ) ) ;
#106245=CARTESIAN_POINT ( 'NONE',  ( 63.27102371193946340, 48.00000000000000711, 15.76003347376319574 ) ) ;
#106253=CARTESIAN_POINT ( 'NONE',  ( 4.649486852896263400, -4.999999999999983125, -15.66810684149982258 ) ) ;
#106255=CARTESIAN_POINT ( 'NONE',  ( 1.469576158976823356E-15, 50.00000000000000000, -73.00000000000001421 ) ) ;
#106256=CARTESIAN_POINT ( 'NONE',  ( -43.51845134567530238, 41.44193902626327031, -50.67202077435701568 ) ) ;
#106271=CARTESIAN_POINT ( 'NONE',  ( -17.49999999999997868, 50.03360497985113398, 63.82236279035413418 ) ) ;
#106282=CARTESIAN_POINT ( 'NONE',  ( -33.64072208462274460, 40.62798226556378012, -61.41639582985341406 ) ) ;
#106292=CARTESIAN_POINT ( 'NONE',  ( 5.036189802309102070, -5.000000000000015099, -93.73786388411730286 ) ) ;
#106296=CARTESIAN_POINT ( 'NONE',  ( 7.500000000000005329, 41.41666666666666430, -71.71180648257555390 ) ) ;
#106305=CARTESIAN_POINT ( 'NONE',  ( 10.36974794996676508, -5.000000000000000000, -92.92756386271756242 ) ) ;
#106312=CARTESIAN_POINT ( 'NONE',  ( -61.12177193198483138, 38.95340872388008790, 18.06307752582379678 ) ) ;
#106330=CARTESIAN_POINT ( 'NONE',  ( -11.03328975971281345, -4.986640933236349049, -12.57657944225302593 ) ) ;
#106345=B_SPLINE_CURVE_WITH_KNOTS ( 'NONE', 3,
 ( #39448, #7049, #31374, #71780, #78817, #37878, #72837, #14596 ),
 .UNSPECIFIED., .F., .F.,
 ( 4, 2, 2, 4 ),
 ( 0.000000000000000000, 0.5000000000000000000, 0.7500000000000000000, 1.000000000000000000 ),
 .UNSPECIFIED. ) ;
#106348=CARTESIAN_POINT ( 'NONE',  ( 4.852941176470595863, 39.99999999999999289, -70.80672828634229177 ) ) ;
#106372=CARTESIAN_POINT ( 'NONE',  ( 6.965116047733301841, 41.61856606189723351, -70.00485699918137072 ) ) ;
#106379=CARTESIAN_POINT ( 'NONE',  ( -39.12903940714779338, 38.95383793066859113, 50.91589357089002732 ) ) ;
#106381=ORIENTED_EDGE ( 'NONE', *, *, #7280, .T. ) ;
#106382=CARTESIAN_POINT ( 'NONE',  ( -37.18423191224957947, 49.99999999999998579, 51.09921067703984221 ) ) ;
#106427=CARTESIAN_POINT ( 'NONE',  ( -53.52139369739177255, 50.00000000000000000, 33.73130704865319274 ) ) ;
#106470=CARTESIAN_POINT ( 'NONE',  ( -7.493261935387684147, 40.00000000000277822, -69.66936203106251924 ) ) ;
#106501=SURFACE_SIDE_STYLE ('',( #31593 ) ) ;
#106507=CARTESIAN_POINT ( 'NONE',  ( 12.50000000000000355, 39.76653967993013339, -65.06879462632775812 ) ) ;
#106510=ORIENTED_EDGE ( 'NONE', *, *, #51531, .F. ) ;
#106520=CARTESIAN_POINT ( 'NONE',  ( 17.50000000000003197, 48.94931827546790970, 64.05766423107181140 ) ) ;
#106532=( LENGTH_UNIT ( ) NAMED_UNIT ( * ) SI_UNIT ( .MILLI., .METRE. ) );
#106540=VERTEX_POINT ( 'NONE', #100233 ) ;
#106555=UNCERTAINTY_MEASURE_WITH_UNIT (LENGTH_MEASURE( 1.000000000000000082E-05 ), #76735, 'distance_accuracy_value', 'NONE');
#106563=CARTESIAN_POINT ( 'NONE',  ( 17.50000000000003197, 51.85440564192877844, 61.62473156926930073 ) ) ;
#106572=CARTESIAN_POINT ( 'NONE',  ( -9.474439531904259582, -5.000000000000035527, -19.39817504953388294 ) ) ;
#106578=SURFACE_STYLE_FILL_AREA ( #42378 ) ;
#106612=STYLED_ITEM ( 'NONE', ( #25273 ), #39919 ) ;
#106622=CARTESIAN_POINT ( 'NONE',  ( 23.88591914974023211, 41.62762614956155005, -74.45994044123901290 ) ) ;
#106627=ORIENTED_EDGE ( 'NONE', *, *, #52751, .F. ) ;
#106634=CARTESIAN_POINT ( 'NONE',  ( -6.689297301784361771, 41.36669071757170713, -70.70516774815108363 ) ) ;
#106675=CARTESIAN_POINT ( 'NONE',  ( -2.617993873628169599, -5.000000000000000000, -10.00000000000000000 ) ) ;
#106678=DIRECTION ( 'NONE',  ( 0.000000000000000000, 1.000000000000000000, 0.000000000000000000 ) ) ;
#106682=( LENGTH_UNIT ( ) NAMED_UNIT ( * ) SI_UNIT ( .MILLI., .METRE. ) );
#106687=ADVANCED_FACE ( 'NONE', ( #434 ), #67894, .T. ) ;
#106727=EDGE_CURVE ( 'NONE', #27940, #88651, #15181, .T. ) ;
#106752=CARTESIAN_POINT ( 'NONE',  ( 6.232496355896458340, 41.83455062734740437, -59.02481358918409171 ) ) ;
#106774=CARTESIAN_POINT ( 'NONE',  ( -9.483106265414438241, -5.000000000000000000, -19.87317390814893869 ) ) ;
#106781=CARTESIAN_POINT ( 'NONE',  ( -8.737863884121843228, -3.000000000000002665, -79.96381019768948306 ) ) ;
ENDSEC;
END-ISO-10303-21;
